ISO-10303-21;
HEADER;
FILE_DESCRIPTION (('STEP AP214'),
    '1' );
FILE_NAME ('Terminal Screw.step',
    '2026-10-05T22:38:29',
    ( '' ),
    ( '' ),
    'SwSTEP 2.0',
    'SolidWorks 2020',
    '' );
FILE_SCHEMA (( 'AUTOMOTIVE_DESIGN' ));
ENDSEC;

DATA;
#34=CARTESIAN_POINT ( 'NONE',  ( 11.83872066707849946, -3.141388196630700236, 8.019361746728900897 ) ) ;
#65=CARTESIAN_POINT ( 'NONE',  ( 9.833766445374623189, -5.249999999999997335, 7.659651991919251834 ) ) ;
#81=CARTESIAN_POINT ( 'NONE',  ( 11.88795122972049967, -3.601717549869600354, 8.421043941822800249 ) ) ;
#126=CARTESIAN_POINT ( 'NONE',  ( 9.549126402770998112, -2.931626221533000010, 7.902879529556599891 ) ) ;
#206=CARTESIAN_POINT ( 'NONE',  ( 11.21503032197930061, -3.256621462143499901, 8.539569492647999027 ) ) ;
#216=EDGE_CURVE ( 'NONE', #67955, #28137, #42558, .T. ) ;
#257=CARTESIAN_POINT ( 'NONE',  ( 10.64887885159599890, -2.730985436695000157, 7.651388779553199626 ) ) ;
#291=CARTESIAN_POINT ( 'NONE',  ( 11.06591429142999949, -3.980313504646230349, 8.533318907609000803 ) ) ;
#316=ORIENTED_EDGE ( 'NONE', *, *, #45064, .F. ) ;
#333=CARTESIAN_POINT ( 'NONE',  ( 10.87872469555899890, -3.497841151814999883, 8.368784980615899372 ) ) ;
#338=CARTESIAN_POINT ( 'NONE',  ( 11.47124174884019965, -4.036194082918090231, 6.184229974648999928 ) ) ;
#375=CARTESIAN_POINT ( 'NONE',  ( 11.19872335273220010, -3.650693637952500126, 6.559289673553299060 ) ) ;
#413=CARTESIAN_POINT ( 'NONE',  ( 10.96029575260939204, -3.171266584307757874, 6.746534734305131842 ) ) ;
#421=CARTESIAN_POINT ( 'NONE',  ( 10.80903300763299946, -3.402282662142699809, 6.873077781830399857 ) ) ;
#459=ORIENTED_EDGE ( 'NONE', *, *, #4248, .T. ) ;
#470=CARTESIAN_POINT ( 'NONE',  ( 10.17832996542199986, -4.602191201513400109, 6.876242273533999416 ) ) ;
#490=CARTESIAN_POINT ( 'NONE',  ( 10.90299135172148226, -3.204747416617449218, 7.862853843651285146 ) ) ;
#506=VECTOR ( 'NONE', #37555, 1000.000000000000000 ) ;
#538=ADVANCED_FACE ( 'NONE', ( #39747 ), #65951, .T. ) ;
#555=CARTESIAN_POINT ( 'NONE',  ( 11.23964560330029983, -3.608363763633400279, 8.716526793355999558 ) ) ;
#591=CARTESIAN_POINT ( 'NONE',  ( 9.218784697134999817, -3.305825103746500293, 8.574479223074998657 ) ) ;
#604=CARTESIAN_POINT ( 'NONE',  ( 11.19041504065829962, -2.975441626403999784, 8.263934892306599167 ) ) ;
#630=CARTESIAN_POINT ( 'NONE',  ( 11.97657389914466819, -4.648774973711785385, 6.404407512144051573 ) ) ;
#635=CARTESIAN_POINT ( 'NONE',  ( 11.58810207955139937, -4.796537143354000499, 7.825000000000000178 ) ) ;
#642=CARTESIAN_POINT ( 'NONE',  ( 11.19057802013490033, -5.033226574983999946, 7.524052967375959966 ) ) ;
#680=CARTESIAN_POINT ( 'NONE',  ( 11.34641504065830020, -3.195537720350400068, 8.099826052678000821 ) ) ;
#687=CARTESIAN_POINT ( 'NONE',  ( 11.51790547754520055, -2.825704134258000266, 7.462730980357120458 ) ) ;
#708=ORIENTED_EDGE ( 'NONE', *, *, #61590, .F. ) ;
#716=CARTESIAN_POINT ( 'NONE',  ( 10.46144540014562807, -3.652722274830687343, 8.303075619429563403 ) ) ;
#768=CARTESIAN_POINT ( 'NONE',  ( 11.69102897915239936, -3.743141152489600110, 6.529961657816500065 ) ) ;
#819=CARTESIAN_POINT ( 'NONE',  ( 9.621088727410999297, -4.863977618062000019, 7.427538838030949719 ) ) ;
#836=CARTESIAN_POINT ( 'NONE',  ( 10.95222191436348247, -3.562569433230172944, 8.256798586434323184 ) ) ;
#857=LINE ( 'NONE', #11681, #59166 ) ;
#908=CARTESIAN_POINT ( 'NONE',  ( 9.905747021776001304, -4.961496216383199709, 6.656252755052399550 ) ) ;
#911=CARTESIAN_POINT ( 'NONE',  ( 12.10000000000000142, -4.549997407263328242, 6.620235306175750623 ) ) ;
#952=CARTESIAN_POINT ( 'NONE',  ( 11.63349010443640097, -2.725546193138000284, 7.404690636538299842 ) ) ;
#975=EDGE_LOOP ( 'NONE', ( #66563, #2565, #7052, #21478 ) ) ;
#989=CARTESIAN_POINT ( 'NONE',  ( 10.89969598649000027, -3.111999510220800236, 6.971269690999399415 ) ) ;
#1028=CARTESIAN_POINT ( 'NONE',  ( 12.19559063708295987, -2.913481137622000006, 7.194517870904999945 ) ) ;
#1036=CARTESIAN_POINT ( 'NONE',  ( 12.05811496860034993, -2.954409148022000053, 8.035816473382100256 ) ) ;
#1066=CARTESIAN_POINT ( 'NONE',  ( 9.752229279041625176, -3.908861085869333785, 6.629812682664218748 ) ) ;
#1096=CARTESIAN_POINT ( 'NONE',  ( 11.03521345716899837, -3.075109701058799772, 6.659120737011199331 ) ) ;
#1107=CARTESIAN_POINT ( 'NONE',  ( 9.841834235717474400, -4.999591705763746674, 8.268200207948643410 ) ) ;
#1134=VECTOR ( 'NONE', #25112, 1000.000000000000114 ) ;
#1164=CARTESIAN_POINT ( 'NONE',  ( 10.65958376188599921, -4.731143729777899765, 7.034020612385399218 ) ) ;
#1166=CARTESIAN_POINT ( 'NONE',  ( 11.25851354018298522, -3.836375382625526687, 8.749999999999996447 ) ) ;
#1187=CARTESIAN_POINT ( 'NONE',  ( 11.89210538575740017, -3.157545584346100220, 7.701417844014099678 ) ) ;
#1249=CARTESIAN_POINT ( 'NONE',  ( 10.91891290906799838, -4.809406943772300380, 6.509421987543800192 ) ) ;
#1295=CARTESIAN_POINT ( 'NONE',  ( 11.70733594839949809, -3.159733897807000425, 8.462948211532999920 ) ) ;
#1339=CYLINDRICAL_SURFACE ( 'NONE', #51118, 1.250000000000000222 ) ;
#1366=CARTESIAN_POINT ( 'NONE',  ( 10.75149413291699929, -2.962184842772000337, 7.973529073237199505 ) ) ;
#1374=CARTESIAN_POINT ( 'NONE',  ( 10.98791429143000009, -3.983006558652820051, 8.391963954669400039 ) ) ;
#1401=EDGE_CURVE ( 'NONE', #46460, #36450, #58715, .T. ) ;
#1405=CARTESIAN_POINT ( 'NONE',  ( 10.43611625296362710, -3.418844976054905782, 8.154057418782388211 ) ) ;
#1411=CARTESIAN_POINT ( 'NONE',  ( 9.289886373836322875, -3.999992178805580334, 6.560153657526066162 ) ) ;
#1441=VERTEX_POINT ( 'NONE', #57891 ) ;
#1451=CARTESIAN_POINT ( 'NONE',  ( 9.748087964304161801, -3.672831456759385382, 8.717422821756882101 ) ) ;
#1508=CARTESIAN_POINT ( 'NONE',  ( 10.55826717315600050, -4.659895246859299789, 8.062357722167599050 ) ) ;
#1510=CARTESIAN_POINT ( 'NONE',  ( 11.39393020684959978, -5.250000000000000000, 7.500000000000000000 ) ) ;
#1528=CARTESIAN_POINT ( 'NONE',  ( 11.84287482311539996, -3.196874704906699893, 7.175518335304800210 ) ) ;
#1559=CARTESIAN_POINT ( 'NONE',  ( 9.284678295047999796, -4.000000000000000000, 7.500000000000000000 ) ) ;
#1593=CARTESIAN_POINT ( 'NONE',  ( 10.76693802597399952, -4.665064168510499876, 8.592736948783000983 ) ) ;
#1596=CARTESIAN_POINT ( 'NONE',  ( 12.10000000000000142, -3.261098123302581531, 6.529275711103853297 ) ) ;
#1603=CARTESIAN_POINT ( 'NONE',  ( 11.73627509987185746, -4.272452942476324012, 8.750000000000000000 ) ) ;
#1630=ORIENTED_EDGE ( 'NONE', *, *, #46199, .T. ) ;
#1638=CARTESIAN_POINT ( 'NONE',  ( 10.10434687351666661, -2.749999999999998224, 7.663624617374462211 ) ) ;
#1645=CARTESIAN_POINT ( 'NONE',  ( 9.927263540183332680, -4.629523725463626782, 6.407767014557179230 ) ) ;
#1671=CARTESIAN_POINT ( 'NONE',  ( 11.02641638348499953, -4.974961480482700260, 7.737488872214999702 ) ) ;
#1675=CARTESIAN_POINT ( 'NONE',  ( 12.09999999999999964, -4.000000000000000000, 7.500000000000000000 ) ) ;
#1710=CARTESIAN_POINT ( 'NONE',  ( 9.324126402770998467, -3.060189502158800146, 7.854398824525599565 ) ) ;
#1713=CARTESIAN_POINT ( 'NONE',  ( 11.02226222744799955, -4.880489021643899861, 6.774721295617600170 ) ) ;
#1720=CARTESIAN_POINT ( 'NONE',  ( 11.14902344389989963, -4.883530143601199747, 8.036199780531900316 ) ) ;
#1740=EDGE_CURVE ( 'NONE', #11416, #1441, #13785, .T. ) ;
#1750=CARTESIAN_POINT ( 'NONE',  ( 10.80371347217102773, -3.410708369063951029, 6.869346568680468224 ) ) ;
#1774=CARTESIAN_POINT ( 'NONE',  ( 9.579430433046999482, -4.737822807309499673, 7.955330044604899342 ) ) ;
#1818=CARTESIAN_POINT ( 'NONE',  ( 10.72726354018266548, -3.370476274536371442, 8.592232985442818105 ) ) ;
#1857=CARTESIAN_POINT ( 'NONE',  ( 10.35563399569799969, -3.138280386550500012, 7.404358731173799946 ) ) ;
#1859=CARTESIAN_POINT ( 'NONE',  ( 11.37309687351627296, -5.217465845835394411, 7.827184855449101697 ) ) ;
#1881=CARTESIAN_POINT ( 'NONE',  ( 11.57210672858429845, -4.692204557952299737, 8.020722037455799480 ) ) ;
#1902=B_SPLINE_CURVE_WITH_KNOTS ( 'NONE', 3,
 ( #39343, #11723, #23602, #6134, #59973, #44261 ),
 .UNSPECIFIED., .F., .F.,
 ( 4, 1, 1, 4 ),
 ( 0.000000000000000000, 0.3333333333333000081, 0.6666666666667000474, 1.000000000000000000 ),
 .UNSPECIFIED. ) ;
#1905=CARTESIAN_POINT ( 'NONE',  ( 10.14393020684900115, -2.750000000000000000, 7.500000000000000000 ) ) ;
#1940=CARTESIAN_POINT ( 'NONE',  ( 10.55041772631200026, -3.450375740502100275, 6.368647051112000135 ) ) ;
#1944=CARTESIAN_POINT ( 'NONE',  ( 12.09999999999999964, -4.000000000000000000, 7.500000000000000000 ) ) ;
#1973=EDGE_CURVE ( 'NONE', #57705, #2412, #32110, .T. ) ;
#2017=DIRECTION ( 'NONE',  ( -1.000000000000000000, 0.000000000000000000, 0.000000000000000000 ) ) ;
#2022=CARTESIAN_POINT ( 'NONE',  ( 10.83364828895399867, -3.239803852721999888, 7.084788038520800413 ) ) ;
#2062=CARTESIAN_POINT ( 'NONE',  ( 9.879355082327998971, -4.511005581663400044, 8.521081653687000212 ) ) ;
#2065=CARTESIAN_POINT ( 'NONE',  ( 11.41610672858429965, -4.911600290708499905, 8.185766014210599906 ) ) ;
#2074=CARTESIAN_POINT ( 'NONE',  ( 11.61718313518939993, -4.622449961306399402, 6.712912394634500401 ) ) ;
#2075=CARTESIAN_POINT ( 'NONE',  ( 11.81389666366019853, -4.045876550911099656, 6.467512203247999913 ) ) ;
#2107=CARTESIAN_POINT ( 'NONE',  ( 10.00552075086462622, -4.127043264527912925, 8.365674464137100586 ) ) ;
#2125=CARTESIAN_POINT ( 'NONE',  ( 10.48926717315599966, -4.764472860199700399, 8.151477970733999712 ) ) ;
#2130=CARTESIAN_POINT ( 'NONE',  ( 11.09393020684900044, -2.750000000000000000, 7.500000000000000000 ) ) ;
#2145=ORIENTED_EDGE ( 'NONE', *, *, #32579, .T. ) ;
#2183=B_SPLINE_SURFACE_WITH_KNOTS ( 'NONE', 3, 3, ( 
 ( #41366, #56413, #51503, #3267, #66892, #19004, #51172, #24599, #51845, #67231, #35437, #30532, #56763, #30879, #8860, #62675, #14457, #30197, #19346, #57091, #3600, #9534, #24936, #46955, #46270, #14795, #24249, #67573, #3943, #45586, #57428, #25282, #40331, #61654, #46616, #8516, #29864, #67921, #13768, #35101, #19698, #41018, #62340, #35777, #49665, #24129, #12964, #17510, #13316, #28348, #45464, #1774, #66778, #33594, #3148, #12265, #18894, #50706, #54911, #29050, #65739, #38836, #39525, #24479, #60162, #34979, #7014 ),
 ( #55610, #60849, #66081, #44782, #2803, #34288, #23092, #50016, #7711, #28701, #29397, #18202, #2125, #50362, #40219, #34638, #45801, #56296, #2461, #60501, #61536, #13651, #23785, #33941, #8399, #44441, #45121, #17862, #39178, #66428, #12610, #29744, #51047, #23444, #55262, #7356, #18549, #55950, #61195, #39878, #8055, #44719, #28282, #18484, #50640, #44378, #56227, #34225, #54850, #55544, #66016, #24066, #28990, #6949, #7642, #55890, #49602, #50298, #1710, #2396, #2740, #39810, #8336, #61132, #29680, #23720, #34574 ),
 ( #34912, #39117, #66363, #50983, #7994, #45056, #18831, #40157, #13249, #65328, #17447, #29327, #61473, #45401, #66710, #13592, #22681, #44025, #23029, #38773, #18139, #60097, #12203, #33531, #65676, #17798, #60440, #12547, #33878, #55195, #7297, #28638, #49949, #2062, #23380, #39462, #60782, #12896, #24413, #20534, #61811, #9343, #10039, #57943, #62487, #40484, #57586, #3755, #35255, #41180, #52348, #30687, #56571, #19509, #41859, #47112, #67727, #51996, #25094, #8675, #68071, #4442, #13928, #19160, #14611, #4100, #40827 ),
 ( #51659, #30022, #3419, #45741, #3080, #63165, #30352, #35598, #51324, #25435, #35929, #46425, #19851, #57241, #9694, #46768, #24754, #56912, #20188, #14270, #14946, #41516, #9011, #62827, #36271, #31040, #31378, #15294, #25781, #46079, #68411, #36619, #67387, #67051, #62152, #5826, #11758, #22252, #53727, #5138, #58975, #63859, #26475, #32753, #43590, #37302, #11077, #53043, #42216, #64889, #16660, #53387, #48485, #43239, #54067, #32412, #591, #21900, #64545, #16316, #47808, #5488, #59311, #42551, #63521, #27163, #26823 ) ),
 .UNSPECIFIED., .F., .F., .F.,
 ( 4, 4 ),
 ( 4, 1, 1, 1, 1, 1, 1, 1, 1, 1, 1, 1, 1, 1, 1, 1, 1, 1, 1, 1, 1, 1, 1, 1, 1, 1, 1, 1, 1, 1, 1, 1, 1, 1, 1, 1, 1, 1, 1, 1, 1, 1, 1, 1, 1, 1, 1, 1, 1, 1, 1, 1, 1, 1, 1, 1, 1, 1, 1, 1, 1, 1, 1, 1, 4 ),
 ( -0.02000000000000000042, 1.020000000000000018 ),
 ( -0.02000000000000000042, -0.003749999999999999861, 0.01250000000000000069, 0.02875000000000000125, 0.04499999999999999833, 0.06124999999999999889, 0.07749999999999999944, 0.09375000000000000000, 0.1100000000000000006, 0.1262500000000000011, 0.1424999999999999878, 0.1587500000000000022, 0.1749999999999999889, 0.1912500000000000033, 0.2074999999999999900, 0.2237500000000000044, 0.2399999999999999911, 0.2562499999999999778, 0.2725000000000000200, 0.2887500000000000067, 0.3049999999999999933, 0.3212499999999999800, 0.3375000000000000222, 0.3537500000000000089, 0.3699999999999999956, 0.3862499999999999822, 0.4025000000000000244, 0.4187500000000000111, 0.4349999999999999978, 0.4512499999999999845, 0.4675000000000000266, 0.4837500000000000133, 0.5000000000000000000, 0.5162499999999999867, 0.5324999999999999734, 0.5487499999999999600, 0.5649999999999999467, 0.5812500000000000444, 0.5975000000000000311, 0.6137500000000000178, 0.6300000000000000044, 0.6462499999999999911, 0.6624999999999999778, 0.6787499999999999645, 0.6949999999999999512, 0.7112500000000000488, 0.7275000000000000355, 0.7437500000000000222, 0.7600000000000000089, 0.7762499999999999956, 0.7924999999999999822, 0.8087499999999999689, 0.8249999999999999556, 0.8412500000000000533, 0.8575000000000000400, 0.8737500000000000266, 0.8900000000000000133, 0.9062500000000000000, 0.9224999999999999867, 0.9387499999999999734, 0.9549999999999999600, 0.9712499999999999467, 0.9875000000000000444, 1.003749999999999920, 1.020000000000000018 ),
 .UNSPECIFIED. ) ;
#2219=ORIENTED_EDGE ( 'NONE', *, *, #66522, .T. ) ;
#2271=CARTESIAN_POINT ( 'NONE',  ( 11.11476354018240364, -2.782534154164604256, 7.827184855449092815 ) ) ;
#2285=CARTESIAN_POINT ( 'NONE',  ( 10.74160887879199855, -4.289688213680199702, 8.745979585038000437 ) ) ;
#2338=ORIENTED_EDGE ( 'NONE', *, *, #27193, .F. ) ;
#2360=EDGE_CURVE ( 'NONE', #41699, #50813, #19462, .T. ) ;
#2361=CARTESIAN_POINT ( 'NONE',  ( 11.46949144726329983, -4.580206776679999869, 8.318725197575499664 ) ) ;
#2364=DIRECTION ( 'NONE',  ( 0.000000000000000000, 1.000000000000000000, 0.000000000000000000 ) ) ;
#2396=CARTESIAN_POINT ( 'NONE',  ( 9.298797255587999189, -2.996487526130999779, 7.542485555928790220 ) ) ;
#2399=CARTESIAN_POINT ( 'NONE',  ( 12.07656516821461068, -3.100463633631699967, 6.592171857671999646 ) ) ;
#2410=CARTESIAN_POINT ( 'NONE',  ( 11.46949144726329983, -4.580206776679999869, 8.318725197575499664 ) ) ;
#2411=CARTESIAN_POINT ( 'NONE',  ( 12.02166954483529970, -3.437903757373499847, 8.367285821793199574 ) ) ;
#2412=VERTEX_POINT ( 'NONE', #50508 ) ;
#2461=CARTESIAN_POINT ( 'NONE',  ( 10.33729229006299910, -3.131390070940299974, 8.004340253666999416 ) ) ;
#2540=CARTESIAN_POINT ( 'NONE',  ( 9.317138961223998095, -3.281636118526699786, 7.014550357332099750 ) ) ;
#2565=ORIENTED_EDGE ( 'NONE', *, *, #37644, .F. ) ;
#2622=CARTESIAN_POINT ( 'NONE',  ( 9.853076168957999315, -4.579425901182000658, 6.516130052788599691 ) ) ;
#2625=CARTESIAN_POINT ( 'NONE',  ( 12.09213512191444195, -4.803449168604846164, 7.825049263296810054 ) ) ;
#2635=ORIENTED_EDGE ( 'NONE', *, *, #64371, .T. ) ;
#2702=CARTESIAN_POINT ( 'NONE',  ( 11.93302763632549990, -5.035790660926999784, 7.977941233841399971 ) ) ;
#2720=CARTESIAN_POINT ( 'NONE',  ( 12.09999999999999964, -4.000000000000000000, 7.500000000000000000 ) ) ;
#2740=CARTESIAN_POINT ( 'NONE',  ( 9.273468108405999999, -3.033597967472499768, 7.226304214866999587 ) ) ;
#2743=CARTESIAN_POINT ( 'NONE',  ( 11.70733594839949809, -3.159733897807000425, 8.462948211532999920 ) ) ;
#2754=CARTESIAN_POINT ( 'NONE',  ( 11.49410672858429905, -4.801902424331299990, 8.103244025831999764 ) ) ;
#2755=CARTESIAN_POINT ( 'NONE',  ( 11.11257802013489915, -4.891884252872400474, 7.520762592984879369 ) ) ;
#2784=CARTESIAN_POINT ( 'NONE',  ( 9.650912690312628328, -4.805207160112336950, 7.157693560935859622 ) ) ;
#2790=CARTESIAN_POINT ( 'NONE',  ( 12.17766954483535891, -3.284117569315500251, 8.604570063127999546 ) ) ;
#2797=ORIENTED_EDGE ( 'NONE', *, *, #54179, .F. ) ;
#2803=CARTESIAN_POINT ( 'NONE',  ( 10.69190035061499877, -3.732283713685800031, 6.531924610394499453 ) ) ;
#2812=CARTESIAN_POINT ( 'NONE',  ( 11.70596535229475776, -4.908912176279685013, 7.175015064079871330 ) ) ;
#2885=CARTESIAN_POINT ( 'NONE',  ( 9.443784697134999462, -3.529509552262100058, 8.228249052908999772 ) ) ;
#2886=CARTESIAN_POINT ( 'NONE',  ( 9.290860954912000480, -3.902433532469449684, 6.578106533244199916 ) ) ;
#2930=CARTESIAN_POINT ( 'NONE',  ( 10.69809687351567362, -3.672815144550895639, 8.717465845835397076 ) ) ;
#2965=CARTESIAN_POINT ( 'NONE',  ( 10.48630484851599931, -2.961576783819000358, 7.025224608805800131 ) ) ;
#2985=CARTESIAN_POINT ( 'NONE',  ( 11.91544519387736578, -3.267573604823260869, 7.982107551664254785 ) ) ;
#3040=CARTESIAN_POINT ( 'NONE',  ( 10.99764694612700033, -5.059486515935999407, 7.077178005756699974 ) ) ;
#3080=CARTESIAN_POINT ( 'NONE',  ( 10.53590035061499997, -3.659038130401700339, 6.267064942904999825 ) ) ;
#3083=CARTESIAN_POINT ( 'NONE',  ( 10.62426357027499968, -2.745128867668000350, 7.257895958275299542 ) ) ;
#3094=CARTESIAN_POINT ( 'NONE',  ( 10.71462282008599942, -3.476853648246800432, 6.656181553372300108 ) ) ;
#3133=CARTESIAN_POINT ( 'NONE',  ( 11.68412378248529926, -4.549028353065900809, 8.538714411016998795 ) ) ;
#3148=CARTESIAN_POINT ( 'NONE',  ( 9.503442991500000048, -4.054579081944059915, 8.365291319916600798 ) ) ;
#3174=CARTESIAN_POINT ( 'NONE',  ( 12.35159063708299954, -3.174974693948799942, 7.268038553423699533 ) ) ;
#3202=ORIENTED_EDGE ( 'NONE', *, *, #10334, .T. ) ;
#3211=ORIENTED_EDGE ( 'NONE', *, *, #45064, .T. ) ;
#3234=CARTESIAN_POINT ( 'NONE',  ( 9.241501215035999195, -4.228777700933000538, 6.624106355763400344 ) ) ;
#3248=CARTESIAN_POINT ( 'NONE',  ( 11.06080513895999928, -2.973119161490000106, 8.070849345005600028 ) ) ;
#3262=CARTESIAN_POINT ( 'NONE',  ( 11.89210538575740017, -3.157545584346100220, 7.701417844014099678 ) ) ;
#3267=CARTESIAN_POINT ( 'NONE',  ( 10.79522949779699914, -3.519000825516800379, 6.778648208007999720 ) ) ;
#3278=CARTESIAN_POINT ( 'NONE',  ( 10.64601354018233081, -3.000416447002271170, 8.268183399968638270 ) ) ;
#3308=CARTESIAN_POINT ( 'NONE',  ( 10.84091290906799898, -4.722468360609500593, 6.615820196229499572 ) ) ;
#3311=EDGE_LOOP ( 'NONE', ( #16784, #34463 ) ) ;
#3360=ORIENTED_EDGE ( 'NONE', *, *, #61566, .F. ) ;
#3380=CARTESIAN_POINT ( 'NONE',  ( 10.92380110216399913, -4.973546009874400653, 8.094557215852098864 ) ) ;
#3419=CARTESIAN_POINT ( 'NONE',  ( 10.58655864498000021, -2.992894514506000192, 6.711254117843599154 ) ) ;
#3424=CARTESIAN_POINT ( 'NONE',  ( 9.946013540182333301, -4.999583552997726166, 6.731816600031359066 ) ) ;
#3431=CARTESIAN_POINT ( 'NONE',  ( 11.66225954179439839, -3.122605388210700106, 6.770980925167799036 ) ) ;
#3470=CARTESIAN_POINT ( 'NONE',  ( 10.94999293566599974, -3.279967330949900450, 6.616719557880299085 ) ) ;
#3484=CARTESIAN_POINT ( 'NONE',  ( 12.09999999999999964, -4.672781865721786332, 8.148846660984084167 ) ) ;
#3506=CARTESIAN_POINT ( 'NONE',  ( 10.88287885159599888, -3.139900861731399928, 7.602606670248799325 ) ) ;
#3537=( NAMED_UNIT ( * ) PLANE_ANGLE_UNIT ( ) SI_UNIT ( $, .RADIAN. ) );
#3552=CARTESIAN_POINT ( 'NONE',  ( 11.05518582084300050, -4.566724035220099509, 8.155074391384399490 ) ) ;
#3554=EDGE_CURVE ( 'NONE', #16603, #54112, #7094, .T. ) ;
#3555=CARTESIAN_POINT ( 'NONE',  ( 10.09393020685000053, -2.750000000000000000, 7.500000000000000000 ) ) ;
#3580=CARTESIAN_POINT ( 'NONE',  ( 11.77234208742519961, -4.554746427620499638, 6.627995351445298944 ) ) ;
#3588=PLANE ( 'NONE',  #56553 ) ;
#3593=CARTESIAN_POINT ( 'NONE',  ( 12.08902763632552002, -4.786505910413500153, 7.862914650060299770 ) ) ;
#3600=CARTESIAN_POINT ( 'NONE',  ( 10.36463399569800004, -3.138280386550500012, 7.404358731173799946 ) ) ;
#3641=CARTESIAN_POINT ( 'NONE',  ( 10.03038019923399915, -2.867101906753999785, 7.642395078236999595 ) ) ;
#3717=CARTESIAN_POINT ( 'NONE',  ( 12.03148876160955005, -4.790673964186999534, 6.677731919207799294 ) ) ;
#3755=CARTESIAN_POINT ( 'NONE',  ( 9.524747021775999301, -4.858221690000700477, 6.746879837742599584 ) ) ;
#3758=CARTESIAN_POINT ( 'NONE',  ( 10.91964694612699915, -5.186980343482999523, 7.026297514493899499 ) ) ;
#3760=CARTESIAN_POINT ( 'NONE',  ( 9.977263540182335078, -4.629523725463626782, 6.407767014557177454 ) ) ;
#3766=CARTESIAN_POINT ( 'NONE',  ( 11.47124174884019965, -4.036194082918090231, 6.184229974648999928 ) ) ;
#3769=CARTESIAN_POINT ( 'NONE',  ( 11.14533863405319991, -3.296214805808900028, 6.602238051205399749 ) ) ;
#3777=ORIENTED_EDGE ( 'NONE', *, *, #17925, .F. ) ;
#3805=CARTESIAN_POINT ( 'NONE',  ( 12.26588784977539959, -5.120865761890000201, 7.564049652083489228 ) ) ;
#3844=CARTESIAN_POINT ( 'NONE',  ( 11.05518582084300050, -4.566724035220099509, 8.155074391384399490 ) ) ;
#3893=B_SPLINE_SURFACE_WITH_KNOTS ( 'NONE', 3, 3, ( 
 ( #27765, #3174, #45824, #27410, #33001, #54315, #59215, #33697, #23197, #6415, #12016, #17964, #16904, #33352, #38234, #17618, #59563, #49416, #12367, #56317, #1187, #7118, #1528, #32658, #65491, #11317, #28456, #65840, #60604, #11660, #6073, #39283, #49770, #1881, #43839, #48736, #12715, #8422, #29765, #9100, #30439, #19601, #62916, #41265, #47203, #4880, #4533, #15387, #14361, #68505, #9785, #67820, #51750, #36017, #3844, #58036, #52089, #14015, #67135, #56999, #68162, #3506, #62579, #40920, #35685, #62243, #41610 ),
 ( #30777, #19246, #4193, #20282, #41952, #25182, #24844, #30108, #40574, #46517, #19944, #25530, #67479, #15037, #9435, #36715, #25869, #20627, #14700, #31467, #52786, #8766, #57333, #46859, #26223, #36363, #63260, #57676, #31135, #10135, #46171, #52437, #61901, #35344, #56660, #51410, #48575, #64976, #63951, #680, #37737, #63612, #32499, #47551, #16745, #6254, #22340, #21312, #20974, #54155, #16406, #59062, #16062, #11499, #15728, #42982, #68854, #42310, #333, #64289, #5912, #43678, #17090, #53814, #21991, #26912, #11164 ),
 ( #37392, #1028, #48227, #32843, #37055, #58716, #27253, #43334, #27594, #64639, #53477, #58370, #26569, #21647, #6604, #38422, #10472, #59747, #31813, #38073, #48920, #59400, #11848, #33186, #32162, #54505, #53132, #5231, #47894, #59795, #42642, #10820, #5571, #2065, #17450, #66366, #44722, #23724, #55893, #49605, #61476, #28285, #13252, #50302, #55547, #49952, #39813, #34916, #39120, #1713, #7997, #17801, #56230, #44028, #60443, #23032, #45059, #12551, #18489, #65331, #1366, #33882, #44381, #27946, #50643, #18143, #29331 ),
 ( #24069, #45406, #34228, #2399, #7300, #39465, #12206, #55198, #54853, #61135, #28642, #34577, #33534, #38776, #49257, #22684, #66714, #65679, #2743, #60786, #23383, #66020, #18834, #40161, #7645, #6954, #60100, #12899, #13595, #28993, #67730, #46771, #13931, #14614, #9346, #31043, #46083, #19854, #40488, #35258, #61814, #46428, #56574, #40831, #25438, #8678, #50986, #24757, #25784, #52351, #3758, #67390, #19512, #62155, #4103, #41519, #36623, #62830, #25097, #68074, #9697, #30025, #3083, #9014, #51327, #14274, #24417 ) ),
 .UNSPECIFIED., .F., .F., .F.,
 ( 4, 4 ),
 ( 4, 1, 1, 1, 1, 1, 1, 1, 1, 1, 1, 1, 1, 1, 1, 1, 1, 1, 1, 1, 1, 1, 1, 1, 1, 1, 1, 1, 1, 1, 1, 1, 1, 1, 1, 1, 1, 1, 1, 1, 1, 1, 1, 1, 1, 1, 1, 1, 1, 1, 1, 1, 1, 1, 1, 1, 1, 1, 1, 1, 1, 1, 1, 1, 4 ),
 ( -0.02000000000000000042, 1.020000000000000018 ),
 ( 0.008747244164287000176, 0.02453926110774999961, 0.04033127805120999970, 0.05612329499467000327, 0.07191531193812999989, 0.08770732888158999652, 0.1034993458251000087, 0.1192913627684999978, 0.1350833797120000179, 0.1508753966553999792, 0.1666674135988999994, 0.1824594305423999918, 0.1982514474858000086, 0.2140434644293000011, 0.2298354813727000179, 0.2456274983162000103, 0.2614195152596999749, 0.2772115322030999640, 0.2930035491465999842, 0.3087955660900000288, 0.3245875830334999934, 0.3403795999769999581, 0.3561716169204000026, 0.3719636338639000228, 0.3877556508073999875, 0.4035476677507999765, 0.4193396846942999967, 0.4351317016376999858, 0.4509237185811999504, 0.4667157355247000261, 0.4825077524681000152, 0.4982997694115999798, 0.5140917863550000799, 0.5298838032985000446, 0.5456758202420000092, 0.5614678371854000538, 0.5772598541289000185, 0.5930518710723000630, 0.6088438880158000277, 0.6246359049592999924, 0.6404279219027000369, 0.6562199388462000016, 0.6720119557896999662, 0.6878039727331000108, 0.7035959896765999755, 0.7193880066200000201, 0.7351800235634999847, 0.7509720405069999494, 0.7667640574504001050, 0.7825560743939000696, 0.7983480913373000032, 0.8141401082808000789, 0.8299321252243000435, 0.8457241421676999771, 0.8615161591112000528, 0.8773081760545999863, 0.8931001929981000620, 0.9088922099416000266, 0.9246842268849999602, 0.9404762438285000359, 0.9562682607720000005, 0.9720602777153999341, 0.9878522946589000098, 1.003644311601999961, 1.019436328545999970 ),
 .UNSPECIFIED. ) ;
#3921=CARTESIAN_POINT ( 'NONE',  ( 11.48656920625009903, -3.967932847735990531, 8.391549386185598536 ) ) ;
#3943=CARTESIAN_POINT ( 'NONE',  ( 10.16200081823899914, -4.767147064380999666, 7.096028062709999418 ) ) ;
#3959=EDGE_CURVE ( 'NONE', #16603, #11416, #48553, .T. ) ;
#3963=CARTESIAN_POINT ( 'NONE',  ( 11.80671024775549682, -3.379344054882541304, 6.880623181275072220 ) ) ;
#3980=CARTESIAN_POINT ( 'NONE',  ( 10.58762143724499971, -3.241588663654300095, 8.353549467159899322 ) ) ;
#4009=PRODUCT_CONTEXT ( 'NONE', #8793, 'mechanical' ) ;
#4031=CARTESIAN_POINT ( 'NONE',  ( 9.599999931441001166, -2.753634353389999845, 7.595250590283559866 ) ) ;
#4035=B_SPLINE_CURVE_WITH_KNOTS ( 'NONE', 3,
 ( #6762, #33349, #34046, #28454, #55710, #38582, #49767, #28101, #43837, #65136 ),
 .UNSPECIFIED., .F., .F.,
 ( 4, 2, 2, 2, 4 ),
 ( 0.000000000000000000, 0.2500000000000000000, 0.5000000000000000000, 0.7500000000000000000, 1.000000000000000000 ),
 .UNSPECIFIED. ) ;
#4059=CARTESIAN_POINT ( 'NONE',  ( 11.61302897915239818, -3.708003626182200030, 6.397263297997000109 ) ) ;
#4088=ORIENTED_EDGE ( 'NONE', *, *, #51445, .F. ) ;
#4100=CARTESIAN_POINT ( 'NONE',  ( 9.077265421554999492, -4.214287043487900064, 6.391527115138999626 ) ) ;
#4103=CARTESIAN_POINT ( 'NONE',  ( 10.82118582084300051, -4.836160649475099937, 8.466515260542900378 ) ) ;
#4110=CARTESIAN_POINT ( 'NONE',  ( 12.14122412107036908, -3.937930136014310190, 8.673243607771999208 ) ) ;
#4112=CARTESIAN_POINT ( 'NONE',  ( 11.56379841651039975, -4.401637675674300532, 6.432302808027999141 ) ) ;
#4150=CARTESIAN_POINT ( 'NONE',  ( 11.96989666366029859, -4.058428102321880004, 6.185029684353999357 ) ) ;
#4193=CARTESIAN_POINT ( 'NONE',  ( 12.25718044953559982, -3.110233631466100324, 7.036033215662999218 ) ) ;
#4237=CARTESIAN_POINT ( 'NONE',  ( 9.307788144226000426, -3.909067355573210278, 6.546538158064899804 ) ) ;
#4238=CARTESIAN_POINT ( 'NONE',  ( 11.86749010443640096, -3.136214309321499805, 7.435402237490909449 ) ) ;
#4241=CARTESIAN_POINT ( 'NONE',  ( 9.599999931441001166, -2.753634353389999845, 7.595250590283559866 ) ) ;
#4248=EDGE_CURVE ( 'NONE', #11948, #21230, #53509, .T. ) ;
#4271=CARTESIAN_POINT ( 'NONE',  ( 11.52812378248509795, -4.416893162838900544, 8.288725998710999576 ) ) ;
#4286=CARTESIAN_POINT ( 'NONE',  ( 12.18333460557258974, -3.837988184179999873, 6.509695444280099608 ) ) ;
#4311=CARTESIAN_POINT ( 'NONE',  ( 11.75962254157670017, -3.830327337663943510, 6.639751609450683212 ) ) ;
#4315=AXIS2_PLACEMENT_3D ( 'NONE', #30724, #15330, #36658 ) ;
#4328=ADVANCED_FACE ( 'NONE', ( #21796 ), #64782, .T. ) ;
#4331=CARTESIAN_POINT ( 'NONE',  ( 10.18034252387499983, -4.992846242613000030, 7.651982363644999730 ) ) ;
#4348=CARTESIAN_POINT ( 'NONE',  ( 11.58810207955139937, -4.796537143354000499, 7.825000000000000178 ) ) ;
#4357=ORIENTED_EDGE ( 'NONE', *, *, #57711, .T. ) ;
#4366=ORIENTED_EDGE ( 'NONE', *, *, #18176, .F. ) ;
#4367=CARTESIAN_POINT ( 'NONE',  ( 11.89043504475232815, -5.070797187771876047, 6.797261353019674601 ) ) ;
#4376=VERTEX_POINT ( 'NONE', #37533 ) ;
#4407=CARTESIAN_POINT ( 'NONE',  ( 11.43656785386840014, -5.060279460151999587, 6.786470850652599474 ) ) ;
#4442=CARTESIAN_POINT ( 'NONE',  ( 9.170138961223999630, -3.053949131563199693, 6.860686042446299204 ) ) ;
#4453=CARTESIAN_POINT ( 'NONE',  ( 11.85034208742530026, -4.630634088820300143, 6.508707709313799050 ) ) ;
#4455=CARTESIAN_POINT ( 'NONE',  ( 12.12579573085663043, -2.760622544769000264, 7.285547569258399747 ) ) ;
#4465=CARTESIAN_POINT ( 'NONE',  ( 12.09999999999999964, -4.883784007588900522, 7.174999999999999822 ) ) ;
#4491=CARTESIAN_POINT ( 'NONE',  ( 10.97769598648999967, -2.990523684589000197, 6.898940957443399746 ) ) ;
#4533=CARTESIAN_POINT ( 'NONE',  ( 11.25210807141120029, -3.959980833595939664, 6.634727177901499573 ) ) ;
#4565=ORIENTED_EDGE ( 'NONE', *, *, #40188, .F. ) ;
#4581=CARTESIAN_POINT ( 'NONE',  ( 12.18748876160954886, -4.600381688599499697, 6.875627981711399883 ) ) ;
#4613=CARTESIAN_POINT ( 'NONE',  ( 11.48146005378009882, -3.088328798999600000, 7.986817550794899745 ) ) ;
#4628=CARTESIAN_POINT ( 'NONE',  ( 11.07980110216399972, -4.739241740354600552, 7.951464549725199227 ) ) ;
#4662=ORIENTED_EDGE ( 'NONE', *, *, #29688, .F. ) ;
#4670=CARTESIAN_POINT ( 'NONE',  ( 10.53495058442699950, -3.601336184534900120, 8.421905343605699201 ) ) ;
#4687=CARTESIAN_POINT ( 'NONE',  ( 11.32145113417867677, -3.276884167680957027, 7.008885863206549161 ) ) ;
#4704=ORIENTED_EDGE ( 'NONE', *, *, #17398, .T. ) ;
#4707=CARTESIAN_POINT ( 'NONE',  ( 11.87077408945317103, -5.183263708087437749, 7.086869749530762874 ) ) ;
#4748=B_SPLINE_CURVE_WITH_KNOTS ( 'NONE', 3,
 ( #34337, #54957, #55305, #7059, #49710, #17905, #17556, #38882, #55654, #17196, #7402, #1818, #23137, #12655, #12308, #44488, #29096, #59849 ),
 .UNSPECIFIED., .F., .F.,
 ( 4, 2, 2, 2, 2, 2, 2, 2, 4 ),
 ( 0.000000000000000000, 0.1250000000000000000, 0.2500000000000000000, 0.3750000000000000000, 0.5000000000000000000, 0.6250000000000000000, 0.7500000000000000000, 0.8750000000000000000, 1.000000000000000000 ),
 .UNSPECIFIED. ) ;
#4751=CARTESIAN_POINT ( 'NONE',  ( 11.80579707368350029, -4.634832087857400751, 8.609190966793999422 ) ) ;
#4789=DIRECTION ( 'NONE',  ( -1.000000000000000000, 0.000000000000000000, 0.000000000000000000 ) ) ;
#4799=CARTESIAN_POINT ( 'NONE',  ( 11.43479632507519916, -3.442212747724900268, 6.465962698293999722 ) ) ;
#4801=CARTESIAN_POINT ( 'NONE',  ( 11.44072200990529886, -5.077092948368999714, 7.875713849677398848 ) ) ;
#4819=DIRECTION ( 'NONE',  ( 0.000000000000000000, 1.000000000000000000, 0.000000000000000000 ) ) ;
#4824=CARTESIAN_POINT ( 'NONE',  ( 11.73424042080529617, -3.455907502640803042, 8.657883396625685180 ) ) ;
#4839=CARTESIAN_POINT ( 'NONE',  ( 11.81900581613029999, -3.249313226592100534, 7.017964743997199939 ) ) ;
#4853=CARTESIAN_POINT ( 'NONE',  ( 12.10000000000000142, -4.569820763625129345, 8.269794803757207546 ) ) ;
#4880=CARTESIAN_POINT ( 'NONE',  ( 11.27672335273219950, -3.698477709264200275, 6.687976048055599421 ) ) ;
#4889=CARTESIAN_POINT ( 'NONE',  ( 11.09725056272499977, -2.683866746800999792, 7.480494252843770120 ) ) ;
#4915=B_SPLINE_CURVE_WITH_KNOTS ( 'NONE', 3,
 ( #4348, #68315, #59558, #6070, #42797, #53964, #5723, #64440, #21462, #53630, #31975, #26726, #4687, #16902, #27407, #32653, #16564, #42112, #21127, #5039, #26378, #5388, #26028, #52592, #48382, #63417, #11314, #836, #22151, #490, #68663, #37891, #15541, #31622, #48040 ),
 .UNSPECIFIED., .F., .F.,
 ( 4, 1, 1, 1, 1, 1, 1, 1, 1, 1, 1, 1, 1, 1, 1, 1, 1, 1, 1, 1, 1, 1, 1, 1, 1, 1, 1, 1, 1, 1, 1, 1, 4 ),
 ( 0.000000000000000000, 0.02634724210002143546, 0.05799096732718442282, 0.08963469255434740324, 0.1212784177813101688, 0.1529221430084731492, 0.1845658682354359148, 0.2162095934625989091, 0.2478533186897619034, 0.2794970439167246412, 0.3111407691438876633, 0.3427844943710506298, 0.3744282195980133676, 0.4060719448251763897, 0.4377156700521391275, 0.4693593952793021495, 0.5010031205064651161, 0.5326468457334281315, 0.5642905709605910980, 0.5959342961875536693, 0.6275780214147168579, 0.6592217466418798244, 0.6908654718688423957, 0.7225091970960055843, 0.7541529223229681556, 0.7857966475501313441, 0.8174403727772943107, 0.8490840980042568820, 0.8807278232314200705, 0.9123715484585830371, 0.9440152736855456084, 0.9756589989127087970, 1.000000000000000000 ),
 .UNSPECIFIED. ) ;
#4930=CARTESIAN_POINT ( 'NONE',  ( 11.47364560330029981, -3.734560974198899874, 8.324524538096799375 ) ) ;
#4974=CARTESIAN_POINT ( 'NONE',  ( 11.57299956498199833, -2.792989229543000107, 7.174999999999999822 ) ) ;
#4979=CARTESIAN_POINT ( 'NONE',  ( 10.90749413291699987, -3.211956830789300277, 7.859564368461399830 ) ) ;
#5011=CIRCLE ( 'NONE', #9501, 1.249999999999999778 ) ;
#5022=CARTESIAN_POINT ( 'NONE',  ( 9.648430433047000321, -4.854750075120300323, 8.027488966151301142 ) ) ;
#5039=CARTESIAN_POINT ( 'NONE',  ( 11.14914416493166449, -4.811858819934198728, 7.176001761109866095 ) ) ;
#5073=B_SPLINE_CURVE_WITH_KNOTS ( 'NONE', 3,
 ( #8062, #33600, #39184, #39531, #45469, #34294, #55616, #29404, #54918, #12615, #7716, #24136, #29750, #7021, #18900, #40225 ),
 .UNSPECIFIED., .F., .F.,
 ( 4, 2, 2, 2, 2, 2, 2, 4 ),
 ( 0.000000000000000000, 0.1249999999999994449, 0.2499999999999988898, 0.3749999999999983347, 0.4999999999999977796, 0.6249999999999980016, 0.7499999999999982236, 1.000000000000000000 ),
 .UNSPECIFIED. ) ;
#5103=CARTESIAN_POINT ( 'NONE',  ( 11.36272200990529946, -5.206705454565000224, 7.920925559347199219 ) ) ;
#5138=CARTESIAN_POINT ( 'NONE',  ( 9.649380199234000699, -2.730774061183999901, 7.659530259549099718 ) ) ;
#5155=CARTESIAN_POINT ( 'NONE',  ( 10.84580110216399973, -5.090698144635000588, 8.166103548914600552 ) ) ;
#5177=CARTESIAN_POINT ( 'NONE',  ( 11.93028911132391201, -5.144000659054666080, 6.940988051967041272 ) ) ;
#5190=CARTESIAN_POINT ( 'NONE',  ( 11.81389666366019853, -4.045876550911099656, 6.467512203247999913 ) ) ;
#5231=CARTESIAN_POINT ( 'NONE',  ( 11.56379841651039975, -4.401637675674300532, 6.432302808027999141 ) ) ;
#5235=ORIENTED_EDGE ( 'NONE', *, *, #47710, .F. ) ;
#5239=CARTESIAN_POINT ( 'NONE',  ( 11.10235971519489873, -3.394698737128500010, 8.506961598696999971 ) ) ;
#5274=CARTESIAN_POINT ( 'NONE',  ( 11.86486084871759950, -5.207010770456999893, 7.174999999999999822 ) ) ;
#5275=CARTESIAN_POINT ( 'NONE',  ( 11.91256651104150066, -3.901000349726440053, 8.498573944230598087 ) ) ;
#5311=CARTESIAN_POINT ( 'NONE',  ( 10.39393020684899938, -5.250000000000000000, 7.500000000000000000 ) ) ;
#5314=B_SPLINE_SURFACE_WITH_KNOTS ( 'NONE', 3, 3, ( 
 ( #52484, #36407, #19645, #31180, #30824, #25916, #31858, #42354, #4581, #25227, #9832, #14743, #46563, #52832, #63654, #57378, #47247, #67869, #62291, #15771, #36759, #4238, #68550, #25578, #51795, #68902, #20672, #42000, #63305, #57724, #15432, #52136, #58080, #10183, #19992, #41313, #31511, #4930, #26265, #47595, #62621, #37100, #15082, #35726, #21018, #46904, #40968, #58414, #36062, #10518, #9481, #68205, #14409, #20324, #3552, #24887, #46218, #67524, #57042, #9144, #41651, #62958, #23681, #2022, #44337, #64329, #45018 ),
 ( #34186, #21692, #33494, #49909, #26615, #47934, #33839, #66323, #7258, #18103, #23340, #61089, #18445, #53173, #39423, #39771, #5275, #60741, #16450, #34, #63992, #55502, #21355, #13210, #42683, #12856, #7604, #54808, #65634, #32208, #16110, #6907, #37434, #58756, #2361, #10862, #60402, #28598, #28953, #44684, #53522, #5611, #26956, #50256, #48269, #375, #43027, #37779, #60058, #12163, #28242, #49560, #1671, #22988, #17761, #39079, #12506, #55153, #65976, #55847, #56530, #20154, #7950, #51960, #24027, #40790, #41481 ),
 ( #62112, #50600, #51620, #62790, #35559, #34536, #45361, #67011, #3717, #67690, #8634, #29289, #2702, #66669, #40119, #19120, #9308, #18791, #14231, #67348, #61433, #56875, #61769, #8974, #13553, #4059, #30313, #56188, #25055, #45702, #8295, #14574, #25396, #40444, #46386, #34870, #29641, #46732, #19813, #35217, #41144, #29983, #50944, #30649, #62453, #35890, #57205, #19467, #68038, #13890, #3040, #24373, #51284, #3380, #24716, #46041, #10690, #42857, #36580, #48449, #26440, #47076, #47770, #58244, #31001, #64168, #47418 ),
 ( #42178, #53006, #16282, #15937, #20844, #31341, #42516, #37268, #27129, #37607, #36932, #48106, #52655, #57906, #4751, #58590, #21866, #26790, #58938, #26093, #63481, #32037, #57551, #9655, #63825, #53693, #68725, #52315, #11043, #4407, #32378, #53351, #5103, #10349, #21185, #25746, #5454, #555, #206, #43203, #68377, #15600, #21526, #5786, #31685, #14911, #36233, #20498, #41822, #69079, #63130, #15257, #10004, #38645, #59272, #33410, #6478, #28160, #18024, #49827, #6828, #43552, #12077, #59625, #64852, #12427, #1940 ) ),
 .UNSPECIFIED., .F., .F., .F.,
 ( 4, 4 ),
 ( 4, 1, 1, 1, 1, 1, 1, 1, 1, 1, 1, 1, 1, 1, 1, 1, 1, 1, 1, 1, 1, 1, 1, 1, 1, 1, 1, 1, 1, 1, 1, 1, 1, 1, 1, 1, 1, 1, 1, 1, 1, 1, 1, 1, 1, 1, 1, 1, 1, 1, 1, 1, 1, 1, 1, 1, 1, 1, 1, 1, 1, 1, 1, 1, 4 ),
 ( -0.02000000000000000042, 1.020000000000000018 ),
 ( 0.008747244164287000176, 0.02453926110774999961, 0.04033127805120999970, 0.05612329499467000327, 0.07191531193812999989, 0.08770732888158999652, 0.1034993458251000087, 0.1192913627684999978, 0.1350833797120000179, 0.1508753966553999792, 0.1666674135988999994, 0.1824594305423999918, 0.1982514474858000086, 0.2140434644293000011, 0.2298354813727000179, 0.2456274983162000103, 0.2614195152596999749, 0.2772115322030999640, 0.2930035491465999842, 0.3087955660900000288, 0.3245875830334999934, 0.3403795999769999581, 0.3561716169204000026, 0.3719636338639000228, 0.3877556508073999875, 0.4035476677507999765, 0.4193396846942999967, 0.4351317016376999858, 0.4509237185811999504, 0.4667157355247000261, 0.4825077524681000152, 0.4982997694115999798, 0.5140917863550000799, 0.5298838032985000446, 0.5456758202420000092, 0.5614678371854000538, 0.5772598541289000185, 0.5930518710723000630, 0.6088438880158000277, 0.6246359049592999924, 0.6404279219027000369, 0.6562199388462000016, 0.6720119557896999662, 0.6878039727331000108, 0.7035959896765999755, 0.7193880066200000201, 0.7351800235634999847, 0.7509720405069999494, 0.7667640574504001050, 0.7825560743939000696, 0.7983480913373000032, 0.8141401082808000789, 0.8299321252243000435, 0.8457241421676999771, 0.8615161591112000528, 0.8773081760545999863, 0.8931001929981000620, 0.9088922099416000266, 0.9246842268849999602, 0.9404762438285000359, 0.9562682607720000005, 0.9720602777153999341, 0.9878522946589000098, 1.003644311601999961, 1.019436328545999970 ),
 .UNSPECIFIED. ) ;
#5321=CARTESIAN_POINT ( 'NONE',  ( 11.44903032197930060, -3.496160833528699996, 8.204588308639600314 ) ) ;
#5371=CARTESIAN_POINT ( 'NONE',  ( 10.40830484851599813, -3.086535948898899928, 7.082356937474298952 ) ) ;
#5388=CARTESIAN_POINT ( 'NONE',  ( 11.09991360228957191, -4.849288934224095904, 7.706876553803710728 ) ) ;
#5403=CARTESIAN_POINT ( 'NONE',  ( 10.54184687351587613, -3.000416447002275611, 6.731816600031356401 ) ) ;
#5428=ORIENTED_EDGE ( 'NONE', *, *, #3959, .F. ) ;
#5454=CARTESIAN_POINT ( 'NONE',  ( 11.26426088462129904, -3.997280690308189666, 8.778009775371000245 ) ) ;
#5488=CARTESIAN_POINT ( 'NONE',  ( 9.092138961223998450, -2.940105638081000006, 6.783753885003399375 ) ) ;
#5501=CARTESIAN_POINT ( 'NONE',  ( 11.11656919669529842, -2.774362666861999838, 7.137881914002699446 ) ) ;
#5505=CARTESIAN_POINT ( 'NONE',  ( 10.04184687351666661, -3.000416447002275611, 6.731816600031356401 ) ) ;
#5521=CONICAL_SURFACE ( 'NONE', #11113, 0.9999998338055000602, 0.7853981908209605178 ) ;
#5534=CARTESIAN_POINT ( 'NONE',  ( 11.14902344389989963, -4.883530143601199747, 8.036199780531900316 ) ) ;
#5571=CARTESIAN_POINT ( 'NONE',  ( 11.44072200990529886, -5.077092948368999714, 7.875713849677398848 ) ) ;
#5576=CARTESIAN_POINT ( 'NONE',  ( 11.06080513895999928, -2.973119161490000106, 8.070849345005600028 ) ) ;
#5582=ORIENTED_EDGE ( 'NONE', *, *, #59360, .T. ) ;
#5611=CARTESIAN_POINT ( 'NONE',  ( 11.29718447801629999, -2.996774412198000448, 7.522119512433738997 ) ) ;
#5612=B_SPLINE_SURFACE_WITH_KNOTS ( 'NONE', 3, 3, ( 
 ( #10396, #57956, #14283, #31735, #62498, #30362, #51670, #30697, #46436, #53054, #57598, #47124, #31390, #25446, #15646, #24765, #56923, #46779, #25794, #58291, #35940, #46090, #3766, #9705, #63535, #67398, #19519, #57253, #36980, #35610, #9354, #68425, #40839, #20548, #52007 ),
 ( #36282, #67738, #52705, #19861, #4110, #68774, #41193, #10054, #14621, #20199, #52361, #4453, #68083, #15307, #63178, #20892, #42228, #31051, #41526, #36632, #62839, #4799, #26143, #14958, #47468, #25607, #15116, #51150, #67553, #30855, #3248, #36436, #15463, #57072, #61980 ),
 ( #24914, #19675, #58108, #20019, #35417, #51483, #56742, #57409, #68237, #8839, #24576, #3580, #42032, #67902, #45900, #46247, #46596, #62987, #4613, #14436, #40997, #62656, #25947, #14090, #20359, #30178, #9865, #41343, #57754, #30511, #47280, #36788, #62321, #25258, #41683 ),
 ( #67210, #14776, #68581, #19322, #31209, #52513, #40647, #20703, #35756, #63335, #36094, #10210, #9513, #9172, #51823, #4271, #3921, #52171, #46935, #43757, #48651, #31543, #22066, #43057, #10550, #59474, #59826, #58791, #6328, #47964, #64710, #68935, #26985, #59133, #11236 ) ),
 .UNSPECIFIED., .F., .F., .F.,
 ( 4, 4 ),
 ( 4, 1, 1, 1, 1, 1, 1, 1, 1, 1, 1, 1, 1, 1, 1, 1, 1, 1, 1, 1, 1, 1, 1, 1, 1, 1, 1, 1, 1, 1, 1, 1, 4 ),
 ( -0.02000000000000000042, 1.020000000000000018 ),
 ( 0.1633025096610999927, 0.1899619885200000136, 0.2166214673788000034, 0.2432809462376999965, 0.2699404250964999585, 0.2965999039553000038, 0.3232593828141999692, 0.3499188616730000145, 0.3765783405318000043, 0.4032378193906999697, 0.4298972982494999595, 0.4565567771083000048, 0.4832162559671999702, 0.5098757348260000155, 0.5365352136848999809, 0.5631946925437000262, 0.5898541714025000715, 0.6165136502614000369, 0.6431731291201999712, 0.6698326079790000165, 0.6964920868378999819, 0.7231515656967000272, 0.7498110445554999615, 0.7764705234143999268, 0.8031300022731999722, 0.8297894811320000175, 0.8564489599908999828, 0.8831084388497000282, 0.9097679177085999935, 0.9364273965674000388, 0.9630868754261999731, 0.9897463542851000495, 1.016405833144000015 ),
 .UNSPECIFIED. ) ;
#5647=ADVANCED_FACE ( 'NONE', ( #60617 ), #65852, .T. ) ;
#5659=CARTESIAN_POINT ( 'NONE',  ( 11.30133863405320049, -3.465595476214000215, 6.818303296693398963 ) ) ;
#5677=ORIENTED_EDGE ( 'NONE', *, *, #48403, .F. ) ;
#5709=CARTESIAN_POINT ( 'NONE',  ( 10.20365911260399905, -4.376739491155700712, 6.719118894894999805 ) ) ;
#5723=CARTESIAN_POINT ( 'NONE',  ( 11.46914282210477687, -3.732132604854249802, 8.332067702129235087 ) ) ;
#5765=CARTESIAN_POINT ( 'NONE',  ( 11.87299956498129916, -5.207010770456999893, 7.825000000000000178 ) ) ;
#5786=CARTESIAN_POINT ( 'NONE',  ( 11.09195391537400077, -2.942766577210000012, 6.781965272201699868 ) ) ;
#5826=CARTESIAN_POINT ( 'NONE',  ( 9.750696787962999323, -3.780328739572700325, 8.760209873321999297 ) ) ;
#5839=CARTESIAN_POINT ( 'NONE',  ( 11.68272066707849888, -2.906477115133000222, 8.161456030935699602 ) ) ;
#5861=CARTESIAN_POINT ( 'NONE',  ( 12.06914347478616811, -3.251273819902354312, 6.470125748842364466 ) ) ;
#5873=CARTESIAN_POINT ( 'NONE',  ( 12.14633327354034797, -4.864904118400500188, 8.065722083251399610 ) ) ;
#5880=B_SPLINE_SURFACE_WITH_KNOTS ( 'NONE', 3, 3, ( 
 ( #13761, #29517, #14452, #35432, #50820, #35772, #51840, #45581, #57424, #56758, #40326, #8855, #3593, #67916, #20032, #61647, #39993, #8510, #29859, #51167, #3262, #37144, #53564, #21398, #59146, #42731, #11250, #10568, #16156, #43069, #64035, #58806, #31224, #64376, #63003, #52531, #46949, #42395, #5321, #52880, #47641, #25622, #37825, #27000, #5659, #37480, #15132, #42046, #25966, #48316, #20374, #41697, #15814, #4628, #36452, #10911, #57771, #31560, #26663, #68951, #4979, #16498, #21064, #32255, #421, #15480, #10226 ),
 ( #68254, #21738, #9882, #31906, #32588, #4286, #63701, #47295, #68598, #26312, #20719, #58461, #63352, #53220, #36805, #58125, #47979, #81, #50311, #13262, #7656, #38161, #50654, #56242, #64723, #768, #23733, #34587, #2074, #8348, #61144, #16839, #39824, #2754, #2410, #22084, #12909, #18499, #34925, #24078, #40497, #45415, #61824, #55902, #66724, #24429, #18844, #40170, #11588, #45753, #43429, #32932, #27342, #45071, #8006, #34237, #29002, #6001, #19174, #29694, #50995, #61486, #59489, #23392, #6344, #3094, #54242 ),
 ( #13604, #27693, #67063, #49009, #13942, #44732, #53901, #48664, #66029, #18153, #39474, #66375, #60796, #55556, #29342, #20894, #56585, #52707, #24767, #41528, #42231, #63537, #25449, #3431, #20550, #35942, #67400, #4112, #15310, #62841, #19521, #51672, #4801, #10056, #30700, #14960, #57255, #40841, #31053, #36634, #46093, #51337, #46781, #36284, #3769, #25106, #57958, #62164, #14623, #14286, #35612, #8688, #35268, #26145, #62500, #67740, #56925, #68427, #68085, #46438, #31392, #30035, #57601, #9024, #30364, #9707, #19864 ),
 ( #4455, #20201, #41195, #9356, #41874, #52009, #52363, #25796, #47126, #63180, #47470, #68776, #37318, #49184, #27177, #47820, #48500, #58990, #1295, #5839, #53056, #952, #16330, #69129, #53742, #64903, #21916, #21234, #32087, #33115, #59675, #11092, #43253, #37659, #42565, #11427, #17016, #26490, #31737, #604, #64559, #53403, #5501, #38347, #63873, #64215, #15987, #58637, #58293, #15648, #54430, #42910, #48154, #5155, #48847, #16674, #26838, #11772, #36982, #38000, #10741, #257, #59326, #21572, #43605, #6531, #32426 ) ),
 .UNSPECIFIED., .F., .F., .F.,
 ( 4, 4 ),
 ( 4, 1, 1, 1, 1, 1, 1, 1, 1, 1, 1, 1, 1, 1, 1, 1, 1, 1, 1, 1, 1, 1, 1, 1, 1, 1, 1, 1, 1, 1, 1, 1, 1, 1, 1, 1, 1, 1, 1, 1, 1, 1, 1, 1, 1, 1, 1, 1, 1, 1, 1, 1, 1, 1, 1, 1, 1, 1, 1, 1, 1, 1, 1, 1, 4 ),
 ( -0.02000000000000000042, 1.020000000000000018 ),
 ( 0.008747244164287000176, 0.02453926110774999961, 0.04033127805120999970, 0.05612329499467000327, 0.07191531193812999989, 0.08770732888158999652, 0.1034993458251000087, 0.1192913627684999978, 0.1350833797120000179, 0.1508753966553999792, 0.1666674135988999994, 0.1824594305423999918, 0.1982514474858000086, 0.2140434644293000011, 0.2298354813727000179, 0.2456274983162000103, 0.2614195152596999749, 0.2772115322030999640, 0.2930035491465999842, 0.3087955660900000288, 0.3245875830334999934, 0.3403795999769999581, 0.3561716169204000026, 0.3719636338639000228, 0.3877556508073999875, 0.4035476677507999765, 0.4193396846942999967, 0.4351317016376999858, 0.4509237185811999504, 0.4667157355247000261, 0.4825077524681000152, 0.4982997694115999798, 0.5140917863550000799, 0.5298838032985000446, 0.5456758202420000092, 0.5614678371854000538, 0.5772598541289000185, 0.5930518710723000630, 0.6088438880158000277, 0.6246359049592999924, 0.6404279219027000369, 0.6562199388462000016, 0.6720119557896999662, 0.6878039727331000108, 0.7035959896765999755, 0.7193880066200000201, 0.7351800235634999847, 0.7509720405069999494, 0.7667640574504001050, 0.7825560743939000696, 0.7983480913373000032, 0.8141401082808000789, 0.8299321252243000435, 0.8457241421676999771, 0.8615161591112000528, 0.8773081760545999863, 0.8931001929981000620, 0.9088922099416000266, 0.9246842268849999602, 0.9404762438285000359, 0.9562682607720000005, 0.9720602777153999341, 0.9878522946589000098, 1.003644311601999961, 1.019436328545999970 ),
 .UNSPECIFIED. ) ;
#5907=VECTOR ( 'NONE', #65601, 1000.000000000000000 ) ;
#5912=CARTESIAN_POINT ( 'NONE',  ( 10.82949413291699869, -3.087070836781100169, 7.916546720849799712 ) ) ;
#5917=CARTESIAN_POINT ( 'NONE',  ( 11.80878751119029957, -5.041025164610000608, 6.955365841266999638 ) ) ;
#5996=CARTESIAN_POINT ( 'NONE',  ( 11.36301932002747961, -5.250000000000001776, 7.200148911387369566 ) ) ;
#6001=CARTESIAN_POINT ( 'NONE',  ( 10.90333997687999990, -3.786145554879500441, 8.480416814141699788 ) ) ;
#6051=CARTESIAN_POINT ( 'NONE',  ( 10.45695058442700009, -3.655872208659600275, 8.295791434820300125 ) ) ;
#6070=CARTESIAN_POINT ( 'NONE',  ( 11.54298866606777629, -4.505418116367177817, 8.213191510014491215 ) ) ;
#6073=CARTESIAN_POINT ( 'NONE',  ( 11.64595257254739913, -4.831736303435800295, 7.258104750172799768 ) ) ;
#6134=CARTESIAN_POINT ( 'NONE',  ( 11.56049777433069892, -4.851452298509800087, 7.825000000000000178 ) ) ;
#6135=CARTESIAN_POINT ( 'NONE',  ( 9.931076168958000494, -4.649151400100800302, 6.397735581984999698 ) ) ;
#6138=CARTESIAN_POINT ( 'NONE',  ( 12.10000000000000142, -3.075975407729481415, 6.664392815890119337 ) ) ;
#6215=CARTESIAN_POINT ( 'NONE',  ( 12.10477869730532774, -4.467447516829900600, 8.421761806503198500 ) ) ;
#6254=CARTESIAN_POINT ( 'NONE',  ( 11.19872335273220010, -3.650693637952500126, 6.559289673553299060 ) ) ;
#6262=CARTESIAN_POINT ( 'NONE',  ( 11.76212378248530044, -4.615095948180499619, 8.663708617168998316 ) ) ;
#6290=CARTESIAN_POINT ( 'NONE',  ( 10.30947051705162743, -3.358100414793015354, 6.905443702049931964 ) ) ;
#6328=CARTESIAN_POINT ( 'NONE',  ( 10.98791429143000009, -3.983006558652820051, 8.391963954669400039 ) ) ;
#6332=AXIS2_PLACEMENT_3D ( 'NONE', #1559, #22881, #44231 ) ;
#6340=CARTESIAN_POINT ( 'NONE',  ( 11.42028665956053501, -4.742415037725373317, 6.450604656432373574 ) ) ;
#6344=CARTESIAN_POINT ( 'NONE',  ( 10.73103300763300005, -3.307558760216100069, 6.773725604892799623 ) ) ;
#6396=CARTESIAN_POINT ( 'NONE',  ( 10.53293802597399953, -4.450760089576400347, 8.240623579255899500 ) ) ;
#6415=CARTESIAN_POINT ( 'NONE',  ( 12.16287348028854964, -4.761955701524100526, 7.088026579158399620 ) ) ;
#6425=CARTESIAN_POINT ( 'NONE',  ( 12.09999999999999964, -4.000000000000000000, 7.500000000000000000 ) ) ;
#6470=CARTESIAN_POINT ( 'NONE',  ( 11.20851354018270207, -3.836375382625528019, 8.749999999999996447 ) ) ;
#6478=CARTESIAN_POINT ( 'NONE',  ( 10.77195525820100031, -4.120672149427799802, 8.772302877803999976 ) ) ;
#6483=CARTESIAN_POINT ( 'NONE',  ( 10.96957120343300041, -4.062009413492949861, 6.222291352336999815 ) ) ;
#6524=EDGE_CURVE ( 'NONE', #64614, #21925, #42237, .T. ) ;
#6529=CARTESIAN_POINT ( 'NONE',  ( 10.11476354018332913, -2.782534154164604256, 7.827184855449092815 ) ) ;
#6531=CARTESIAN_POINT ( 'NONE',  ( 10.55862282008599884, -3.333723918618700210, 6.425317846273999933 ) ) ;
#6543=CARTESIAN_POINT ( 'NONE',  ( 12.09999999999999964, -2.820501972398000046, 7.825000000000000178 ) ) ;
#6560=DIRECTION ( 'NONE',  ( 0.000000000000000000, 1.000000000000000000, 0.000000000000000000 ) ) ;
#6565=CARTESIAN_POINT ( 'NONE',  ( 10.86325056272499978, -3.107965259299500183, 7.486779603004729111 ) ) ;
#6604=CARTESIAN_POINT ( 'NONE',  ( 11.88379707368349969, -4.566644629509899467, 8.490052513816499058 ) ) ;
#6615=CARTESIAN_POINT ( 'NONE',  ( 11.93856039236529831, -2.967715280237000375, 7.449760924956519759 ) ) ;
#6623=VERTEX_POINT ( 'NONE', #66647 ) ;
#6642=DIRECTION ( 'NONE',  ( 0.000000000000000000, 0.000000000000000000, -1.000000000000000000 ) ) ;
#6714=VECTOR ( 'NONE', #12220, 1000.000000000000114 ) ;
#6743=CARTESIAN_POINT ( 'NONE',  ( 10.30497570133299945, -3.363922674822000136, 6.910836541441499392 ) ) ;
#6762=CARTESIAN_POINT ( 'NONE',  ( 10.58521345716900086, -3.075109701058799772, 6.659120737011199331 ) ) ;
#6816=CARTESIAN_POINT ( 'NONE',  ( 11.13559687351579974, -2.907767014557175678, 8.129523725463618788 ) ) ;
#6828=CARTESIAN_POINT ( 'NONE',  ( 10.67349413291699811, -2.837298848764000514, 8.030511425625498134 ) ) ;
#6833=CARTESIAN_POINT ( 'NONE',  ( 10.00706361050499993, -3.475294527116599586, 6.333351572150998976 ) ) ;
#6836=CARTESIAN_POINT ( 'NONE',  ( 12.09999999999999964, -4.198022108741683134, 6.428664210949555979 ) ) ;
#6842=CARTESIAN_POINT ( 'NONE',  ( 11.70158531382784517, -3.727547057523674212, 8.749999999999998224 ) ) ;
#6897=CARTESIAN_POINT ( 'NONE',  ( 9.263353253171903390, -4.132446745988497483, 6.586646690369097890 ) ) ;
#6907=CARTESIAN_POINT ( 'NONE',  ( 11.54333729122640051, -5.003122373830000136, 7.526388557597149642 ) ) ;
#6949=CARTESIAN_POINT ( 'NONE',  ( 9.450772138681999834, -4.373757805842100055, 8.432280753260499750 ) ) ;
#6954=CARTESIAN_POINT ( 'NONE',  ( 11.53502897915239878, -3.672866099873000056, 6.264564938179000286 ) ) ;
#6962=CARTESIAN_POINT ( 'NONE',  ( 11.89700581613019992, -3.130347327833300053, 6.941573685175900010 ) ) ;
#6992=CARTESIAN_POINT ( 'NONE',  ( 9.929533309317628564, -3.366787958683358006, 8.103800281262431682 ) ) ;
#7014=CARTESIAN_POINT ( 'NONE',  ( 9.224822372493999723, -4.249211653873900651, 6.684745346084599582 ) ) ;
#7021=CARTESIAN_POINT ( 'NONE',  ( 9.337278925393347251, -3.116678102649798277, 8.012901425336814043 ) ) ;
#7039=CARTESIAN_POINT ( 'NONE',  ( 9.685590450029499365, -2.907727159402498707, 8.129537449122588910 ) ) ;
#7052=ORIENTED_EDGE ( 'NONE', *, *, #65670, .T. ) ;
#7059=CARTESIAN_POINT ( 'NONE',  ( 10.85226354018316108, -5.092232985442820770, 8.129523725463624118 ) ) ;
#7094=LINE ( 'NONE', #23172, #59499 ) ;
#7097=CARTESIAN_POINT ( 'NONE',  ( 9.697076168957998732, -4.439974903344300117, 6.752918994396699404 ) ) ;
#7098=FACE_OUTER_BOUND ( 'NONE', #9322, .T. ) ;
#7118=CARTESIAN_POINT ( 'NONE',  ( 11.86749010443640096, -3.136214309321499805, 7.435402237490909449 ) ) ;
#7143=CARTESIAN_POINT ( 'NONE',  ( 10.27934687351566545, -4.163624617374463988, 8.750000000000001776 ) ) ;
#7184=CARTESIAN_POINT ( 'NONE',  ( 11.06244474310100045, -2.862064370975999861, 6.947770206896899836 ) ) ;
#7217=VERTEX_POINT ( 'NONE', #52100 ) ;
#7226=CARTESIAN_POINT ( 'NONE',  ( 10.23976354018333268, -4.327184855449098144, 8.717465845835395299 ) ) ;
#7254=CYLINDRICAL_SURFACE ( 'NONE', #25509, 1.250000000000000222 ) ;
#7258=CARTESIAN_POINT ( 'NONE',  ( 12.10948876160955479, -4.695527826393099957, 6.776679950459500112 ) ) ;
#7262=DIRECTION ( 'NONE',  ( -1.000000000000000000, 0.000000000000000000, 0.000000000000000000 ) ) ;
#7282=CARTESIAN_POINT ( 'NONE',  ( 9.191343736187999269, -4.374232398910099739, 6.690658690097199823 ) ) ;
#7297=CARTESIAN_POINT ( 'NONE',  ( 9.955342523875000182, -5.128664655368000425, 7.672773098917999413 ) ) ;
#7300=CARTESIAN_POINT ( 'NONE',  ( 12.05194988689359903, -3.419512757306400363, 6.361426117087999543 ) ) ;
#7308=CARTESIAN_POINT ( 'NONE',  ( 11.77745123989519982, -3.589787500396900199, 6.707778874960499849 ) ) ;
#7356=CARTESIAN_POINT ( 'NONE',  ( 9.906696787962999906, -3.827518619249500098, 8.489491017455099708 ) ) ;
#7369=CARTESIAN_POINT ( 'NONE',  ( 11.89975833414730033, -3.203462856645999945, 7.825000000000000178 ) ) ;
#7385=FACE_OUTER_BOUND ( 'NONE', #63555, .T. ) ;
#7402=CARTESIAN_POINT ( 'NONE',  ( 10.74809687351608289, -3.672815144550895194, 8.717465845835393523 ) ) ;
#7519=CARTESIAN_POINT ( 'NONE',  ( 10.15903849359899880, -3.074215132699300135, 8.382783533462799141 ) ) ;
#7539=MECHANICAL_DESIGN_GEOMETRIC_PRESENTATION_REPRESENTATION('',(#48873),#62246);
#7567=CARTESIAN_POINT ( 'NONE',  ( 10.64393020684899938, -2.750000000000000000, 7.500000000000000000 ) ) ;
#7604=CARTESIAN_POINT ( 'NONE',  ( 11.66641369783139837, -4.050626550392200542, 6.497808498716000081 ) ) ;
#7627=CARTESIAN_POINT ( 'NONE',  ( 9.212501735000000025, -4.358851904410700584, 6.723921629386799381 ) ) ;
#7642=CARTESIAN_POINT ( 'NONE',  ( 9.425442991499998868, -4.063228561016970275, 8.502419298200999620 ) ) ;
#7645=CARTESIAN_POINT ( 'NONE',  ( 11.55964426047339977, -3.312306505177499805, 6.422784126663999338 ) ) ;
#7656=CARTESIAN_POINT ( 'NONE',  ( 11.81410538575740077, -3.024036709177600368, 7.733337754805098996 ) ) ;
#7657=CARTESIAN_POINT ( 'NONE',  ( 11.44501463001509833, -3.527519786474400121, 8.256737112932800216 ) ) ;
#7689=CARTESIAN_POINT ( 'NONE',  ( 9.349999778958000718, -4.000000000000000000, 7.500000000000000000 ) ) ;
#7711=CARTESIAN_POINT ( 'NONE',  ( 10.59058376188600015, -4.847012523549299345, 6.960174024681499816 ) ) ;
#7716=CARTESIAN_POINT ( 'NONE',  ( 9.376902336861421716, -3.730411824524082931, 8.499844062317453819 ) ) ;
#7732=CARTESIAN_POINT ( 'NONE',  ( 9.664757945270775252, -2.782574339883951087, 7.827174490145253571 ) ) ;
#7760=EDGE_CURVE ( 'NONE', #34321, #55891, #8316, .T. ) ;
#7826=ORIENTED_EDGE ( 'NONE', *, *, #39621, .T. ) ;
#7839=CARTESIAN_POINT ( 'NONE',  ( 10.22726354018233152, -3.370476274536371442, 8.592232985442818105 ) ) ;
#7876=CARTESIAN_POINT ( 'NONE',  ( 10.10636764078099858, -3.461752753411900141, 8.506987760366000018 ) ) ;
#7921=CARTESIAN_POINT ( 'NONE',  ( 11.50000000000000000, -3.008232475376599879, 7.825000000000000178 ) ) ;
#7950=CARTESIAN_POINT ( 'NONE',  ( 10.78026357027499849, -3.014700852776899698, 7.309904858193100097 ) ) ;
#7994=CARTESIAN_POINT ( 'NONE',  ( 10.61390035061499937, -3.695660922043800145, 6.399494776650000105 ) ) ;
#7997=CARTESIAN_POINT ( 'NONE',  ( 10.99764694612700033, -5.059486515935999407, 7.077178005756699974 ) ) ;
#8006=CARTESIAN_POINT ( 'NONE',  ( 10.97718582084299932, -4.656536239972400182, 8.258888014436699621 ) ) ;
#8007=CARTESIAN_POINT ( 'NONE',  ( 11.60612378248510090, -4.482960757953799558, 8.413720204863100349 ) ) ;
#8055=CARTESIAN_POINT ( 'NONE',  ( 9.780051052052000315, -3.014287398677499841, 7.307093369932900373 ) ) ;
#8062=CARTESIAN_POINT ( 'NONE',  ( 9.469356963619999235, -5.119357025014000584, 7.500000000085178087 ) ) ;
#8218=CARTESIAN_POINT ( 'NONE',  ( 10.33432996542199866, -4.793057006135000186, 6.678540912152799436 ) ) ;
#8260=CARTESIAN_POINT ( 'NONE',  ( 10.33351354018333446, -5.249999999999999112, 7.663624617374471093 ) ) ;
#8295=CARTESIAN_POINT ( 'NONE',  ( 11.48995257254740032, -5.095356924909000718, 7.181435527216799564 ) ) ;
#8316=B_SPLINE_CURVE_WITH_KNOTS ( 'NONE', 3,
 ( #4031, #62764, #15575, #9626, #68699, #25714, #41796, #63100, #36903, #58218 ),
 .UNSPECIFIED., .F., .F.,
 ( 4, 2, 2, 2, 4 ),
 ( 0.000000000000000000, 0.2500000000000000000, 0.5000000000000000000, 0.7500000000000000000, 1.000000000000000000 ),
 .UNSPECIFIED. ) ;
#8336=CARTESIAN_POINT ( 'NONE',  ( 9.222809814040999754, -3.385590752329799891, 6.705428891605899722 ) ) ;
#8348=CARTESIAN_POINT ( 'NONE',  ( 11.59256785386839894, -4.832509746210599921, 6.939751505745099358 ) ) ;
#8381=CARTESIAN_POINT ( 'NONE',  ( 9.257986382567203520, -3.848432872973400087, 6.650284907739020035 ) ) ;
#8387=CARTESIAN_POINT ( 'NONE',  ( 12.01145123989533126, -3.394760891061399999, 6.331134574721999364 ) ) ;
#8399=CARTESIAN_POINT ( 'NONE',  ( 10.18531740696900023, -3.813190776280700245, 6.513113677132300161 ) ) ;
#8414=ORIENTED_EDGE ( 'NONE', *, *, #36053, .T. ) ;
#8422=CARTESIAN_POINT ( 'NONE',  ( 11.47364560330029981, -3.734560974198899874, 8.324524538096799375 ) ) ;
#8493=ORIENTED_EDGE ( 'NONE', *, *, #1740, .T. ) ;
#8510=CARTESIAN_POINT ( 'NONE',  ( 11.96595122972050085, -3.656201404350900130, 8.295047870239098842 ) ) ;
#8516=CARTESIAN_POINT ( 'NONE',  ( 9.984696787962999309, -3.851113559088000127, 8.354131589521699652 ) ) ;
#8527=CARTESIAN_POINT ( 'NONE',  ( 10.72934687351566652, -4.163624617374463099, 8.750000000000000000 ) ) ;
#8560=CARTESIAN_POINT ( 'NONE',  ( 10.13169678796399964, -3.803923679411099990, 8.624850445389000697 ) ) ;
#8573=( LENGTH_UNIT ( ) NAMED_UNIT ( * ) SI_UNIT ( .MILLI., .METRE. ) );
#8613=DIRECTION ( 'NONE',  ( -1.000000000000000000, 0.000000000000000000, 0.000000000000000000 ) ) ;
#8633=ORIENTED_EDGE ( 'NONE', *, *, #35876, .T. ) ;
#8634=CARTESIAN_POINT ( 'NONE',  ( 11.98225819896750011, -5.120994791668000090, 7.288668995979000087 ) ) ;
#8675=CARTESIAN_POINT ( 'NONE',  ( 9.220797255587999786, -2.859210004667000149, 7.548297453605989027 ) ) ;
#8678=CARTESIAN_POINT ( 'NONE',  ( 11.04272335273199879, -3.555125495332600138, 6.301916924546999255 ) ) ;
#8688=CARTESIAN_POINT ( 'NONE',  ( 10.97303166480599934, -5.137916160623999140, 7.419769534118209720 ) ) ;
#8711=EDGE_LOOP ( 'NONE', ( #3777, #29558, #62418, #56276 ) ) ;
#8721=CARTESIAN_POINT ( 'NONE',  ( 9.524266954400626872, -4.325581995510845879, 8.312113682386053526 ) ) ;
#8726=CARTESIAN_POINT ( 'NONE',  ( 11.47124174884019965, -4.036194082918090231, 6.184229974648999928 ) ) ;
#8740=CARTESIAN_POINT ( 'NONE',  ( 12.09999999999999787, -4.254640155007241908, 8.477868186285952845 ) ) ;
#8749=ADVANCED_FACE ( 'NONE', ( #24109 ), #47873, .T. ) ;
#8766=CARTESIAN_POINT ( 'NONE',  ( 11.78949010443639978, -2.999324937259999935, 7.425165037173959703 ) ) ;
#8793=APPLICATION_CONTEXT ( 'automotive_design' ) ;
#8795=FILL_AREA_STYLE_COLOUR ( '', #29883 ) ;
#8809=LINE ( 'NONE', #4237, #40773 ) ;
#8839=CARTESIAN_POINT ( 'NONE',  ( 11.85545123989520100, -3.524778630617700248, 6.582230774881299595 ) ) ;
#8855=CARTESIAN_POINT ( 'NONE',  ( 12.11364291764652990, -4.859654669415900408, 7.606265891492399511 ) ) ;
#8860=CARTESIAN_POINT ( 'NONE',  ( 10.51660887879199890, -4.196341783741199372, 8.344486736701099971 ) ) ;
#8861=DIRECTION ( 'NONE',  ( -1.000000000000000000, 0.000000000000000000, -1.275169027325000072E-14 ) ) ;
#8901=CARTESIAN_POINT ( 'NONE',  ( 10.28367167105700020, -5.126041103316000047, 7.310881302803900361 ) ) ;
#8913=ADVANCED_FACE ( 'NONE', ( #18100 ), #7254, .T. ) ;
#8917=CARTESIAN_POINT ( 'NONE',  ( 11.06059687351646481, -3.370476274536376771, 6.407767014557177454 ) ) ;
#8963=ORIENTED_EDGE ( 'NONE', *, *, #17925, .T. ) ;
#8974=CARTESIAN_POINT ( 'NONE',  ( 11.66225954179439839, -3.122605388210700106, 6.770980925167799036 ) ) ;
#9011=CARTESIAN_POINT ( 'NONE',  ( 10.07997570133299980, -3.061513547538400104, 6.630731591496600075 ) ) ;
#9012=EDGE_LOOP ( 'NONE', ( #60936, #37395, #23838, #20036 ) ) ;
#9014=CARTESIAN_POINT ( 'NONE',  ( 10.59964828895399869, -2.878385131502000149, 6.887384543790600056 ) ) ;
#9022=FACE_OUTER_BOUND ( 'NONE', #69110, .T. ) ;
#9024=CARTESIAN_POINT ( 'NONE',  ( 10.67764828895399987, -2.998858038575999974, 6.953185708700699408 ) ) ;
#9062=CARTESIAN_POINT ( 'NONE',  ( 12.25203632436370071, -5.109717061557999429, 7.759151359668400083 ) ) ;
#9066=CLOSED_SHELL ( 'NONE', ( #538, #16438, #8749, #22515, #69092, #43742, #37728, #33930, #8913, #5647, #67242, #29082, #27532, #40872, #58827, #47969, #11124, #50802, #4328, #54968, #31590, #64768, #59178, #59820, #56964, #50716, #14278, #12700, #21395, #67469, #37751 ) ) ;
#9100=CARTESIAN_POINT ( 'NONE',  ( 11.42441504065829960, -3.305585767322499979, 8.017771632862299214 ) ) ;
#9128=CARTESIAN_POINT ( 'NONE',  ( 9.495772571291157149, -5.001491341851799888, 6.923765800360898837 ) ) ;
#9142=CARTESIAN_POINT ( 'NONE',  ( 10.89393020684999946, -5.250000000000000000, 7.500000000000000000 ) ) ;
#9144=CARTESIAN_POINT ( 'NONE',  ( 10.93210941423800087, -3.358814833524500276, 8.082391773166900606 ) ) ;
#9145=VECTOR ( 'NONE', #45672, 1000.000000000000000 ) ;
#9169=ORIENTED_EDGE ( 'NONE', *, *, #16901, .T. ) ;
#9172=CARTESIAN_POINT ( 'NONE',  ( 11.61123293495519881, -4.891405920092699589, 7.535834283667469435 ) ) ;
#9178=CARTESIAN_POINT ( 'NONE',  ( 9.349999778958000718, -4.000000000000000000, 7.500000000000000000 ) ) ;
#9192=LINE ( 'NONE', #67232, #32383 ) ;
#9231=CARTESIAN_POINT ( 'NONE',  ( 10.46097570133300003, -3.162316589966200020, 6.724099908144899551 ) ) ;
#9245=CARTESIAN_POINT ( 'NONE',  ( 10.97726354018323214, -4.629523725463626782, 6.407767014557177454 ) ) ;
#9305=CARTESIAN_POINT ( 'NONE',  ( 9.233215486276282746, -3.972057587790281730, 6.616784466747247073 ) ) ;
#9308=CARTESIAN_POINT ( 'NONE',  ( 11.83456651104149948, -3.887457492043800311, 8.635175889530000148 ) ) ;
#9322=EDGE_LOOP ( 'NONE', ( #26176, #19142, #29261, #67001 ) ) ;
#9343=CARTESIAN_POINT ( 'NONE',  ( 9.676721904869999946, -3.004358235431599855, 6.941043897400199114 ) ) ;
#9346=CARTESIAN_POINT ( 'NONE',  ( 11.31349144726329925, -4.738947899111299655, 8.542723541016000510 ) ) ;
#9354=CARTESIAN_POINT ( 'NONE',  ( 11.13880513895979973, -2.849548954067000039, 8.139542779846600240 ) ) ;
#9356=CARTESIAN_POINT ( 'NONE',  ( 12.07656516821461068, -3.100463633631699967, 6.592171857671999646 ) ) ;
#9394=CARTESIAN_POINT ( 'NONE',  ( 11.76723293495529887, -5.173938955706000264, 7.547192037433419820 ) ) ;
#9410=CARTESIAN_POINT ( 'NONE',  ( 12.10000000000000320, -4.094072174251358831, 8.528759793293474445 ) ) ;
#9435=CARTESIAN_POINT ( 'NONE',  ( 11.96179707368349909, -4.498457171163099844, 8.370914060838998694 ) ) ;
#9481=CARTESIAN_POINT ( 'NONE',  ( 11.15364694612719809, -4.804498860841600383, 7.178938988280099132 ) ) ;
#9495=CARTESIAN_POINT ( 'NONE',  ( 9.268793171738000325, -4.404188085824999987, 6.625874414451000227 ) ) ;
#9501=AXIS2_PLACEMENT_3D ( 'NONE', #14476, #9906, #15154 ) ;
#9513=CARTESIAN_POINT ( 'NONE',  ( 11.65278751119019951, -4.790480620979200133, 7.086443476450299706 ) ) ;
#9534=CARTESIAN_POINT ( 'NONE',  ( 10.33930484851599907, -3.211495113978299898, 7.139489266142899915 ) ) ;
#9558=CARTESIAN_POINT ( 'NONE',  ( 11.77531844363629965, -3.660964894626073107, 6.691304915923902641 ) ) ;
#9559=ORIENTED_EDGE ( 'NONE', *, *, #3554, .T. ) ;
#9576=CARTESIAN_POINT ( 'NONE',  ( 9.422480666858998433, -3.619299191678599925, 6.423523106103999680 ) ) ;
#9584=CARTESIAN_POINT ( 'NONE',  ( 12.04684497800060150, -4.976842342332563618, 7.175001354288133015 ) ) ;
#9621=DIRECTION ( 'NONE',  ( -1.000000000000000000, 0.000000000000000000, 0.000000000000000000 ) ) ;
#9626=CARTESIAN_POINT ( 'NONE',  ( 9.502599499754323276, -2.949662297526366661, 7.001638755957637628 ) ) ;
#9655=CARTESIAN_POINT ( 'NONE',  ( 11.58425954179440076, -3.017023678917100327, 6.683254058608399717 ) ) ;
#9676=AXIS2_PLACEMENT_3D ( 'NONE', #40345, #19020, #18341 ) ;
#9694=CARTESIAN_POINT ( 'NONE',  ( 10.28260887879199892, -4.289688213680199702, 8.745979585038000437 ) ) ;
#9697=CARTESIAN_POINT ( 'NONE',  ( 10.67349413291699811, -2.837298848764000514, 8.030511425625498134 ) ) ;
#9705=CARTESIAN_POINT ( 'NONE',  ( 11.42968717260509948, -4.687649763627899979, 6.377637058250999580 ) ) ;
#9707=CARTESIAN_POINT ( 'NONE',  ( 10.63662282008600002, -3.405288783432600219, 6.540749699823199315 ) ) ;
#9731=( GEOMETRIC_REPRESENTATION_CONTEXT ( 3 ) GLOBAL_UNCERTAINTY_ASSIGNED_CONTEXT ( ( #60943 ) ) GLOBAL_UNIT_ASSIGNED_CONTEXT ( ( #20656, #3537, #24531 ) ) REPRESENTATION_CONTEXT ( 'NONE', 'WORKASPACE' ) );
#9743=CARTESIAN_POINT ( 'NONE',  ( 11.55946005378019947, -2.963614890480000152, 8.053412743695298914 ) ) ;
#9758=CARTESIAN_POINT ( 'NONE',  ( 12.09999999999999964, -4.640264089079229493, 8.191831084107846550 ) ) ;
#9785=CARTESIAN_POINT ( 'NONE',  ( 11.15364694612719809, -4.804498860841600383, 7.178938988280099132 ) ) ;
#9832=CARTESIAN_POINT ( 'NONE',  ( 12.13825819896753977, -4.851203879749700576, 7.339530235223699073 ) ) ;
#9836=B_SPLINE_CURVE_WITH_KNOTS ( 'NONE', 3,
 ( #42340, #52820, #68536, #58742 ),
 .UNSPECIFIED., .F., .F.,
 ( 4, 4 ),
 ( 0.000000000000000000, 1.000000000000000000 ),
 .UNSPECIFIED. ) ;
#9859=ORIENTED_EDGE ( 'NONE', *, *, #50008, .T. ) ;
#9865=CARTESIAN_POINT ( 'NONE',  ( 11.14902344389989963, -4.883530143601199747, 8.036199780531900316 ) ) ;
#9868=CARTESIAN_POINT ( 'NONE',  ( 9.640654977342496323, -2.950420301507454379, 8.197403194024859729 ) ) ;
#9882=CARTESIAN_POINT ( 'NONE',  ( 12.25718044953559982, -3.110233631466100324, 7.036033215662999218 ) ) ;
#9906=DIRECTION ( 'NONE',  ( 1.000000000000000000, 0.000000000000000000, 0.000000000000000000 ) ) ;
#9928=CARTESIAN_POINT ( 'NONE',  ( 10.78824205624999877, -4.360201998293100623, 6.562398383267799673 ) ) ;
#9946=CARTESIAN_POINT ( 'NONE',  ( 10.93559687351661580, -5.092232985442824322, 6.870476274536375882 ) ) ;
#9955=CARTESIAN_POINT ( 'NONE',  ( 12.09999999999999964, -2.750000000000000000, 7.500000000000000000 ) ) ;
#10004=CARTESIAN_POINT ( 'NONE',  ( 10.87041638348499895, -5.241705141469999774, 7.802464414828100381 ) ) ;
#10008=VECTOR ( 'NONE', #12991, 1000.000000000000000 ) ;
#10039=CARTESIAN_POINT ( 'NONE',  ( 9.651392757687000667, -3.229293331742300044, 6.657535947657399866 ) ) ;
#10054=CARTESIAN_POINT ( 'NONE',  ( 12.01656039236534923, -2.826501801118000312, 7.442888368925779652 ) ) ;
#10056=CARTESIAN_POINT ( 'NONE',  ( 11.41610672858429965, -4.911600290708499905, 8.185766014210599906 ) ) ;
#10067=LINE ( 'NONE', #4465, #40502 ) ;
#10073=EDGE_LOOP ( 'NONE', ( #54784, #316, #23502, #60287, #40505, #66136, #64191, #36110, #66770, #28147 ) ) ;
#10076=CARTESIAN_POINT ( 'NONE',  ( 11.83830977893730463, -4.976598135215292373, 8.326430086672809594 ) ) ;
#10093=CARTESIAN_POINT ( 'NONE',  ( 12.09603632436369125, -4.842640371965599932, 7.696781148700499564 ) ) ;
#10135=CARTESIAN_POINT ( 'NONE',  ( 11.59256785386839894, -4.832509746210599921, 6.939751505745099358 ) ) ;
#10144=CARTESIAN_POINT ( 'NONE',  ( 12.21922412107039868, -3.930460928605089777, 8.814426450544999625 ) ) ;
#10183=CARTESIAN_POINT ( 'NONE',  ( 11.57210672858429845, -4.692204557952299737, 8.020722037455799480 ) ) ;
#10210=CARTESIAN_POINT ( 'NONE',  ( 11.69434208742519843, -4.478858766422799675, 6.747282993577999655 ) ) ;
#10212=CARTESIAN_POINT ( 'NONE',  ( 9.711801307670127059, -3.888124047000113048, 8.755178286007271993 ) ) ;
#10214=AXIS2_PLACEMENT_3D ( 'NONE', #63274, #15404, #36729 ) ;
#10224=ORIENTED_EDGE ( 'NONE', *, *, #50008, .F. ) ;
#10226=CARTESIAN_POINT ( 'NONE',  ( 10.78441772631200024, -3.627481539113199815, 6.733203680593099705 ) ) ;
#10271=CARTESIAN_POINT ( 'NONE',  ( 9.699088727410998700, -5.000897406023000258, 7.416055476975279781 ) ) ;
#10287=CARTESIAN_POINT ( 'NONE',  ( 10.96684687351657672, -4.768183399968645375, 6.500416447002276499 ) ) ;
#10317=CYLINDRICAL_SURFACE ( 'NONE', #24164, 1.250000000000000222 ) ;
#10334=EDGE_CURVE ( 'NONE', #49203, #36697, #42867, .T. ) ;
#10349=CARTESIAN_POINT ( 'NONE',  ( 11.33810672858430024, -5.021298157087000114, 8.268288002587098617 ) ) ;
#10396=CARTESIAN_POINT ( 'NONE',  ( 12.34388784977539899, -5.255745690988000263, 7.571757098260779806 ) ) ;
#10418=CARTESIAN_POINT ( 'NONE',  ( 11.68220574173929727, -2.863826994586552210, 8.088082908809445470 ) ) ;
#10432=CARTESIAN_POINT ( 'NONE',  ( 11.19568717260499824, -4.466067913030199676, 6.739296831621899742 ) ) ;
#10452=VECTOR ( 'NONE', #14909, 1000.000000000000000 ) ;
#10472=CARTESIAN_POINT ( 'NONE',  ( 11.83456651104149948, -3.887457492043800311, 8.635175889530000148 ) ) ;
#10482=CARTESIAN_POINT ( 'NONE',  ( 11.42968717260509948, -4.687649763627899979, 6.377637058250999580 ) ) ;
#10518=CARTESIAN_POINT ( 'NONE',  ( 11.17826222744820086, -4.668580868411999596, 6.949274830123499669 ) ) ;
#10550=CARTESIAN_POINT ( 'NONE',  ( 11.15413259636999932, -4.783377755405500587, 7.073141822156699732 ) ) ;
#10556=DIRECTION ( 'NONE',  ( 1.000000000000000000, 0.000000000000000000, 0.000000000000000000 ) ) ;
#10562=CARTESIAN_POINT ( 'NONE',  ( 11.49664311227126490, -3.555960431980461411, 6.293666904468254941 ) ) ;
#10568=CARTESIAN_POINT ( 'NONE',  ( 11.71979841651039855, -4.304975143798100312, 6.689266534545799558 ) ) ;
#10603=ORIENTED_EDGE ( 'NONE', *, *, #28580, .T. ) ;
#10612=CARTESIAN_POINT ( 'NONE',  ( 10.38297570133299885, -3.263119632394200220, 6.817468224793199916 ) ) ;
#10657=CARTESIAN_POINT ( 'NONE',  ( 12.09999999999999964, -4.000000000000000000, 7.500000000000000000 ) ) ;
#10690=CARTESIAN_POINT ( 'NONE',  ( 10.84995525820099971, -4.107710726525199973, 8.635644537520001052 ) ) ;
#10741=CARTESIAN_POINT ( 'NONE',  ( 10.67349413291699811, -2.837298848764000514, 8.030511425625498134 ) ) ;
#10745=CARTESIAN_POINT ( 'NONE',  ( 9.979346873516666605, -3.836375382625532904, 6.249999999999999112 ) ) ;
#10775=CARTESIAN_POINT ( 'NONE',  ( 11.35679632507500081, -3.509334349252600127, 6.590394082213600235 ) ) ;
#10820=CARTESIAN_POINT ( 'NONE',  ( 11.46533729122639933, -5.140346530769000388, 7.529998433785960010 ) ) ;
#10826=CARTESIAN_POINT ( 'NONE',  ( 12.01656039236534923, -2.826501801118000312, 7.442888368925779652 ) ) ;
#10862=CARTESIAN_POINT ( 'NONE',  ( 11.44487616594229884, -4.303437140848100029, 8.456491899811199531 ) ) ;
#10899=CARTESIAN_POINT ( 'NONE',  ( 9.599999931441001166, -2.753634353389999845, 7.595250590283559866 ) ) ;
#10911=CARTESIAN_POINT ( 'NONE',  ( 11.03057053952199951, -4.340412141385700195, 8.296503712697200328 ) ) ;
#10963=CARTESIAN_POINT ( 'NONE',  ( 10.90644474310099810, -3.106516218291800246, 7.066400461213500073 ) ) ;
#10984=( GEOMETRIC_REPRESENTATION_CONTEXT ( 3 ) GLOBAL_UNCERTAINTY_ASSIGNED_CONTEXT ( ( #21292 ) ) GLOBAL_UNIT_ASSIGNED_CONTEXT ( ( #8573, #45978, #45304 ) ) REPRESENTATION_CONTEXT ( 'NONE', 'WORKASPACE' ) );
#11040=MECHANICAL_DESIGN_GEOMETRIC_PRESENTATION_REPRESENTATION('',(#61256),#10984);
#11043=CARTESIAN_POINT ( 'NONE',  ( 11.46118313518939935, -4.792748567750200195, 6.497569908212999401 ) ) ;
#11077=CARTESIAN_POINT ( 'NONE',  ( 9.472076168957999087, -4.649151400100800302, 6.397735581984999698 ) ) ;
#11092=CARTESIAN_POINT ( 'NONE',  ( 11.38733729122639993, -5.277570687708000641, 7.533608309972310124 ) ) ;
#11096=CARTESIAN_POINT ( 'NONE',  ( 9.989763540183332680, -3.672815144550900524, 6.282534154164604701 ) ) ;
#11113=AXIS2_PLACEMENT_3D ( 'NONE', #9178, #10556, #42037 ) ;
#11123=CARTESIAN_POINT ( 'NONE',  ( 12.09999999999999964, -2.613168764257999932, 7.825000000000000178 ) ) ;
#11124=ADVANCED_FACE ( 'NONE', ( #37001 ), #15672, .T. ) ;
#11128=CARTESIAN_POINT ( 'NONE',  ( 11.64767835872009982, -4.874341053673500568, 8.051056647135798272 ) ) ;
#11144=EDGE_CURVE ( 'NONE', #30682, #36697, #36050, .T. ) ;
#11149=ORIENTED_EDGE ( 'NONE', *, *, #11144, .T. ) ;
#11164=CARTESIAN_POINT ( 'NONE',  ( 10.70641772631199906, -3.568446272909699957, 6.611684804099500212 ) ) ;
#11170=CARTESIAN_POINT ( 'NONE',  ( 10.93614141025500075, -3.450366949021700158, 6.521048559232099251 ) ) ;
#11198=CARTESIAN_POINT ( 'NONE',  ( 10.71473687196862734, -4.313773474582136558, 6.683251291081091949 ) ) ;
#11236=CARTESIAN_POINT ( 'NONE',  ( 10.78014141025500017, -3.582647672488299850, 6.756653759087999589 ) ) ;
#11239=CARTESIAN_POINT ( 'NONE',  ( 9.610163692916376732, -2.765799910565780895, 7.754438396796453858 ) ) ;
#11242=CARTESIAN_POINT ( 'NONE',  ( 10.88528584683667688, -3.267379250638398069, 6.833918148925946845 ) ) ;
#11244=DIRECTION ( 'NONE',  ( 0.000000000000000000, -1.000000000000000000, 0.000000000000000000 ) ) ;
#11250=CARTESIAN_POINT ( 'NONE',  ( 11.74441369783139955, -4.043700988887960257, 6.634905315059499209 ) ) ;
#11254=VERTEX_POINT ( 'NONE', #64923 ) ;
#11298=CARTESIAN_POINT ( 'NONE',  ( 9.747734463322998977, -3.909687748588960066, 6.637705594503099604 ) ) ;
#11307=DIRECTION ( 'NONE',  ( 0.000000000000000000, 1.000000000000000000, 0.000000000000000000 ) ) ;
#11314=CARTESIAN_POINT ( 'NONE',  ( 10.97683719568448169, -3.813711395361371714, 8.354041075310609799 ) ) ;
#11317=CARTESIAN_POINT ( 'NONE',  ( 11.76902897915239876, -3.778278678798900447, 6.662660017635100296 ) ) ;
#11380=CARTESIAN_POINT ( 'NONE',  ( 11.07088779216199903, -2.816792857868000155, 7.073306690476799830 ) ) ;
#11384=CARTESIAN_POINT ( 'NONE',  ( 12.09999999999999964, -4.831023649631406514, 7.002620348270789385 ) ) ;
#11416=VERTEX_POINT ( 'NONE', #67338 ) ;
#11427=CARTESIAN_POINT ( 'NONE',  ( 11.28887616594230003, -4.386455737425299262, 8.718182393403999697 ) ) ;
#11461=CARTESIAN_POINT ( 'NONE',  ( 11.68923293495519999, -5.032672437899000428, 7.541513160549049744 ) ) ;
#11467=LINE ( 'NONE', #59716, #46681 ) ;
#11483=VERTEX_POINT ( 'NONE', #67679 ) ;
#11499=CARTESIAN_POINT ( 'NONE',  ( 11.00180110216400031, -4.856393875115199599, 8.023010882787499298 ) ) ;
#11506=CARTESIAN_POINT ( 'NONE',  ( 11.39324174884020024, -4.032306468273969990, 6.325557131097000685 ) ) ;
#11536=CARTESIAN_POINT ( 'NONE',  ( 10.28414136986962646, -3.576408136849907216, 6.734426879786121312 ) ) ;
#11588=CARTESIAN_POINT ( 'NONE',  ( 11.12487750876920067, -4.543557328885200697, 6.656497609330299881 ) ) ;
#11605=VERTEX_POINT ( 'NONE', #47760 ) ;
#11639=CARTESIAN_POINT ( 'NONE',  ( 9.395138961224001051, -3.167792625045000143, 6.937618199889199033 ) ) ;
#11660=CARTESIAN_POINT ( 'NONE',  ( 11.67056785386840012, -4.718624889240500053, 7.016391833292499491 ) ) ;
#11681=CARTESIAN_POINT ( 'NONE',  ( 9.349999778958000718, -4.000000000000000000, 6.500000166194499940 ) ) ;
#11723=CARTESIAN_POINT ( 'NONE',  ( 11.51053724730969918, -4.948425591258600598, 7.825000000000000178 ) ) ;
#11724=CARTESIAN_POINT ( 'NONE',  ( 10.46298825978700009, -4.167373623506299474, 6.231784538167999266 ) ) ;
#11758=CARTESIAN_POINT ( 'NONE',  ( 9.725367640781000134, -3.396982508013000501, 8.628164124510998789 ) ) ;
#11772=CARTESIAN_POINT ( 'NONE',  ( 10.74733997688000109, -3.727636250918499705, 8.748653021963999521 ) ) ;
#11777=CARTESIAN_POINT ( 'NONE',  ( 10.02101354018333446, -3.231816600031356845, 6.500416447002272946 ) ) ;
#11806=PLANE ( 'NONE',  #46984 ) ;
#11848=CARTESIAN_POINT ( 'NONE',  ( 11.68687482311540116, -2.942322404451000128, 7.072673169413499217 ) ) ;
#11856=CARTESIAN_POINT ( 'NONE',  ( 12.09966954483535773, -3.361010663344000005, 8.485927942460499196 ) ) ;
#11887=CARTESIAN_POINT ( 'NONE',  ( 9.777558426223626142, -3.641115516887601267, 6.702043737600841489 ) ) ;
#11902=VERTEX_POINT ( 'NONE', #60308 ) ;
#11905=CARTESIAN_POINT ( 'NONE',  ( 11.78192504596561996, -3.091022006579346115, 7.174999814284952926 ) ) ;
#11948=VERTEX_POINT ( 'NONE', #12764 ) ;
#11995=CARTESIAN_POINT ( 'NONE',  ( 9.344480666858999030, -3.665111009453500213, 6.553061479084200336 ) ) ;
#11997=CARTESIAN_POINT ( 'NONE',  ( 11.38351354018293904, -5.249999999999998224, 7.663624617374469317 ) ) ;
#12016=CARTESIAN_POINT ( 'NONE',  ( 12.13825819896753977, -4.851203879749700576, 7.339530235223699073 ) ) ;
#12077=CARTESIAN_POINT ( 'NONE',  ( 10.62426357027499968, -2.745128867668000350, 7.257895958275299542 ) ) ;
#12084=CARTESIAN_POINT ( 'NONE',  ( 10.26035508232799920, -4.572497688003699601, 8.643954013369999245 ) ) ;
#12155=CARTESIAN_POINT ( 'NONE',  ( 9.210288521113000115, -4.352953559891299840, 6.715449042252499723 ) ) ;
#12162=DIRECTION ( 'NONE',  ( -1.000000000000000000, 0.000000000000000000, 0.000000000000000000 ) ) ;
#12163=CARTESIAN_POINT ( 'NONE',  ( 11.10026222744819790, -4.774534945026900346, 6.861998062869400172 ) ) ;
#12166=CARTESIAN_POINT ( 'NONE',  ( 10.79399293566600093, -3.453258297007899991, 6.829299525004299376 ) ) ;
#12203=CARTESIAN_POINT ( 'NONE',  ( 10.15797570133299921, -3.162316589966200020, 6.724099908144899551 ) ) ;
#12206=CARTESIAN_POINT ( 'NONE',  ( 12.00271932425157040, -4.187398418774900044, 6.235801371442999397 ) ) ;
#12214=CARTESIAN_POINT ( 'NONE',  ( 11.98011496860029901, -3.080230834057799960, 7.971338736265699332 ) ) ;
#12220=DIRECTION ( 'NONE',  ( 0.7071067388045961799, 0.7071068235684964121, -1.176037761303994353E-10 ) ) ;
#12246=CARTESIAN_POINT ( 'NONE',  ( 10.13216648677562759, -4.862862160676565182, 7.355082228165340297 ) ) ;
#12265=CARTESIAN_POINT ( 'NONE',  ( 9.478113844317999082, -3.781046324972699768, 8.338908357746399602 ) ) ;
#12290=CARTESIAN_POINT ( 'NONE',  ( 9.696006702408610067, -3.000394487162608925, 8.268211173249310875 ) ) ;
#12308=CARTESIAN_POINT ( 'NONE',  ( 10.68559687351583420, -2.907767014557174790, 8.129523725463618788 ) ) ;
#12345=CARTESIAN_POINT ( 'NONE',  ( 9.874380199233998567, -3.139757597894699881, 7.608124715612800237 ) ) ;
#12367=CARTESIAN_POINT ( 'NONE',  ( 11.94133594839949986, -3.430493414882899827, 8.152656755002400502 ) ) ;
#12414=EDGE_CURVE ( 'NONE', #55891, #55934, #8809, .T. ) ;
#12417=CARTESIAN_POINT ( 'NONE',  ( 11.17726354018259727, -3.370476274536371442, 8.592232985442818105 ) ) ;
#12427=CARTESIAN_POINT ( 'NONE',  ( 10.55862282008599884, -3.333723918618700210, 6.425317846273999933 ) ) ;
#12432=CARTESIAN_POINT ( 'NONE',  ( 10.61496314287999887, -2.748296264808000267, 7.763860089407599752 ) ) ;
#12473=CARTESIAN_POINT ( 'NONE',  ( 10.32309687351666838, -5.217465845835395299, 7.827184855449101697 ) ) ;
#12501=CARTESIAN_POINT ( 'NONE',  ( 11.50009108335969898, -2.881106418324590468, 7.402342568044064208 ) ) ;
#12506=CARTESIAN_POINT ( 'NONE',  ( 10.92795525820100089, -4.094749303624469761, 8.498986197235801399 ) ) ;
#12547=CARTESIAN_POINT ( 'NONE',  ( 10.03132996542199962, -4.793057006135000186, 6.678540912152799436 ) ) ;
#12551=CARTESIAN_POINT ( 'NONE',  ( 10.82533997688000049, -3.756890902898200046, 8.614534918052999757 ) ) ;
#12559=CARTESIAN_POINT ( 'NONE',  ( 11.52812378248509795, -4.416893162838900544, 8.288725998710999576 ) ) ;
#12590=CARTESIAN_POINT ( 'NONE',  ( 10.53743284169262573, -4.454886069780877200, 8.247402791297171021 ) ) ;
#12610=CARTESIAN_POINT ( 'NONE',  ( 10.03334252387499959, -4.992846242613000030, 7.651982363644999730 ) ) ;
#12615=CARTESIAN_POINT ( 'NONE',  ( 9.383506238772769237, -3.863849893416519521, 8.533506295447228496 ) ) ;
#12655=CARTESIAN_POINT ( 'NONE',  ( 10.69601354018253581, -3.000416447002272058, 8.268183399968641822 ) ) ;
#12691=CARTESIAN_POINT ( 'NONE',  ( 9.319151519676999840, -3.978278301382419890, 6.495824366094999469 ) ) ;
#12693=CARTESIAN_POINT ( 'NONE',  ( 11.35226354018294792, -5.092232985442820770, 8.129523725463624118 ) ) ;
#12700=ADVANCED_FACE ( 'NONE', ( #9022 ), #5612, .F. ) ;
#12715=CARTESIAN_POINT ( 'NONE',  ( 11.49826088462129903, -3.998156935320088756, 8.366195817038299509 ) ) ;
#12741=CARTESIAN_POINT ( 'NONE',  ( 10.37309687351566723, -5.217465845835394411, 7.827184855449101697 ) ) ;
#12764=CARTESIAN_POINT ( 'NONE',  ( 12.09999999999999964, -4.883784007588900522, 7.174999999999999822 ) ) ;
#12766=CARTESIAN_POINT ( 'NONE',  ( 11.10434687351569494, -2.749999999999998224, 7.663624617374462211 ) ) ;
#12780=CARTESIAN_POINT ( 'NONE',  ( 10.43765911260399903, -4.555852086785099786, 6.347865960448999090 ) ) ;
#12791=CARTESIAN_POINT ( 'NONE',  ( 11.61486084871780022, -2.792989229543000107, 7.825000000000000178 ) ) ;
#12850=CARTESIAN_POINT ( 'NONE',  ( 11.50000000000000000, -3.008232475376599879, 7.825000000000000178 ) ) ;
#12856=CARTESIAN_POINT ( 'NONE',  ( 11.69102897915239936, -3.743141152489600110, 6.529961657816500065 ) ) ;
#12896=CARTESIAN_POINT ( 'NONE',  ( 9.778038493599000347, -3.173653894988100355, 8.287963554181398962 ) ) ;
#12899=CARTESIAN_POINT ( 'NONE',  ( 11.48579841651039857, -4.449968941611500028, 6.303820944768999901 ) ) ;
#12909=CARTESIAN_POINT ( 'NONE',  ( 11.42026088462129962, -3.997864853650589634, 8.503467136482999678 ) ) ;
#12910=CARTESIAN_POINT ( 'NONE',  ( 11.69434208742519843, -4.478858766422799675, 6.747282993577999655 ) ) ;
#12941=CARTESIAN_POINT ( 'NONE',  ( 9.600254395947626307, -4.850975458930337325, 7.703403631282998099 ) ) ;
#12947=CARTESIAN_POINT ( 'NONE',  ( 9.301820635884373800, -3.939853377893446584, 6.549596649571864937 ) ) ;
#12964=CARTESIAN_POINT ( 'NONE',  ( 9.706076168957999073, -4.439974903344300117, 6.752918994396699404 ) ) ;
#12991=DIRECTION ( 'NONE',  ( -1.000000000000000000, 0.000000000000000000, 2.886579864060000134E-14 ) ) ;
#13045=CARTESIAN_POINT ( 'NONE',  ( 9.215822372493999382, -4.249211653873900651, 6.684745346084599582 ) ) ;
#13090=ORIENTED_EDGE ( 'NONE', *, *, #17398, .F. ) ;
#13102=CARTESIAN_POINT ( 'NONE',  ( 11.89975833414730033, -3.203462856645999945, 7.825000000000000178 ) ) ;
#13132=CARTESIAN_POINT ( 'NONE',  ( 9.458265421554999719, -4.240073379563900069, 6.258138488953999712 ) ) ;
#13142=CARTESIAN_POINT ( 'NONE',  ( 11.82299956498189886, -5.207010770456999893, 7.825000000000000178 ) ) ;
#13177=VECTOR ( 'NONE', #68361, 1000.000000000000227 ) ;
#13210=CARTESIAN_POINT ( 'NONE',  ( 11.74025954179439957, -3.228187097503200320, 6.858707791728399172 ) ) ;
#13222=AXIS2_PLACEMENT_3D ( 'NONE', #32075, #4789, #58978 ) ;
#13234=CARTESIAN_POINT ( 'NONE',  ( 9.205449068729999240, -4.363978735910500006, 6.712833982956899703 ) ) ;
#13249=CARTESIAN_POINT ( 'NONE',  ( 10.51258376188599897, -4.962881317320600338, 6.886327436977599525 ) ) ;
#13252=CARTESIAN_POINT ( 'NONE',  ( 11.19456919669529960, -2.906008650422999828, 7.176777099639999768 ) ) ;
#13262=CARTESIAN_POINT ( 'NONE',  ( 11.83872066707849946, -3.141388196630700236, 8.019361746728900897 ) ) ;
#13263=CARTESIAN_POINT ( 'NONE',  ( 11.27368717260499942, -4.539928529895099985, 6.618743573831199711 ) ) ;
#13295=CARTESIAN_POINT ( 'NONE',  ( 9.372292071306626227, -3.125836066416603387, 7.537009346329285542 ) ) ;
#13316=CARTESIAN_POINT ( 'NONE',  ( 9.655417874594000693, -4.797903641662700558, 7.160798403412399260 ) ) ;
#13366=EDGE_CURVE ( 'NONE', #65484, #29598, #52278, .T. ) ;
#13439=CARTESIAN_POINT ( 'NONE',  ( 10.35226354018232975, -5.092232985442820770, 8.129523725463624118 ) ) ;
#13442=CARTESIAN_POINT ( 'NONE',  ( 10.79184687351566829, -4.999583552997724389, 8.268183399968647151 ) ) ;
#13467=VERTEX_POINT ( 'NONE', #27863 ) ;
#13477=CARTESIAN_POINT ( 'NONE',  ( 9.675772138681999479, -4.424886761933599644, 8.559813987224998755 ) ) ;
#13553=CARTESIAN_POINT ( 'NONE',  ( 11.63764426047339917, -3.386171819220400003, 6.538488127609999978 ) ) ;
#13592=CARTESIAN_POINT ( 'NONE',  ( 10.33527973160900082, -3.897539901865500145, 8.637205511891998810 ) ) ;
#13595=CARTESIAN_POINT ( 'NONE',  ( 11.46118313518939935, -4.792748567750200195, 6.497569908212999401 ) ) ;
#13604=CARTESIAN_POINT ( 'NONE',  ( 12.20379573085659963, -2.893744357957000357, 7.308581953418300081 ) ) ;
#13605=CARTESIAN_POINT ( 'NONE',  ( 11.23724174883999893, -4.024531238983009906, 6.608211443991299561 ) ) ;
#13638=CARTESIAN_POINT ( 'NONE',  ( 9.295853127542962113, -3.970210778477946345, 6.554146822010631368 ) ) ;
#13651=CARTESIAN_POINT ( 'NONE',  ( 10.26130484851599967, -3.086535948898899928, 7.082356937474298952 ) ) ;
#13720=AXIS2_PLACEMENT_3D ( 'NONE', #14022, #51415, #23470 ) ;
#13761=CARTESIAN_POINT ( 'NONE',  ( 12.35979573085659844, -3.159987984332300215, 7.354650721737899133 ) ) ;
#13768=CARTESIAN_POINT ( 'NONE',  ( 9.908709346416999963, -3.216804796119200116, 7.871904849557299855 ) ) ;
#13785=B_SPLINE_CURVE_WITH_KNOTS ( 'NONE', 3,
 ( #57448, #30551, #3963, #9558, #4311, #46976, #68280, #20400, #64063, #33311 ),
 .UNSPECIFIED., .F., .F.,
 ( 4, 2, 2, 2, 4 ),
 ( 0.000000000000000000, 0.2500000000000003331, 0.5000000000000006661, 0.7500000000000003331, 1.000000000000000000 ),
 .UNSPECIFIED. ) ;
#13812=CARTESIAN_POINT ( 'NONE',  ( 9.500480666858999612, -3.573487373903700082, 6.293984733123999753 ) ) ;
#13834=CARTESIAN_POINT ( 'NONE',  ( 12.02531641787287597, -4.339035680702311382, 8.308706962315561384 ) ) ;
#13856=CARTESIAN_POINT ( 'NONE',  ( 10.27101354018333446, -4.768183399968641822, 8.499583552997725278 ) ) ;
#13890=CARTESIAN_POINT ( 'NONE',  ( 11.02226222744799955, -4.880489021643899861, 6.774721295617600170 ) ) ;
#13928=CARTESIAN_POINT ( 'NONE',  ( 9.144809814041000351, -3.301541394817099739, 6.596733927440100231 ) ) ;
#13931=CARTESIAN_POINT ( 'NONE',  ( 11.36272200990529946, -5.206705454565000224, 7.920925559347199219 ) ) ;
#13942=CARTESIAN_POINT ( 'NONE',  ( 12.12994988689360021, -3.481863023525599843, 6.483720595741000459 ) ) ;
#13980=CARTESIAN_POINT ( 'NONE',  ( 11.47635090131019986, -3.000792947412299849, 6.881982988766500497 ) ) ;
#13994=CARTESIAN_POINT ( 'NONE',  ( 12.09999999999999964, -3.927017550833199699, 8.552611010855411422 ) ) ;
#14015=CARTESIAN_POINT ( 'NONE',  ( 10.98133997688000107, -3.815400206859000054, 8.346298710230199092 ) ) ;
#14022=CARTESIAN_POINT ( 'NONE',  ( 12.09999999999999964, -4.000000000000000000, 7.500000000000000000 ) ) ;
#14077=PLANE ( 'NONE',  #48469 ) ;
#14090=CARTESIAN_POINT ( 'NONE',  ( 11.27368717260499942, -4.539928529895099985, 6.618743573831199711 ) ) ;
#14122=CARTESIAN_POINT ( 'NONE',  ( 10.84393020684900044, -5.250000000000000000, 7.500000000000000000 ) ) ;
#14156=CARTESIAN_POINT ( 'NONE',  ( 9.751759580228998914, -5.110528875107000601, 7.765443149353999708 ) ) ;
#14169=DIRECTION ( 'NONE',  ( -1.000000000000000000, 0.000000000000000000, 1.665334536957000056E-14 ) ) ;
#14230=ORIENTED_EDGE ( 'NONE', *, *, #28580, .F. ) ;
#14231=CARTESIAN_POINT ( 'NONE',  ( 11.78533594839949927, -3.249987070165300196, 8.359517726022600570 ) ) ;
#14259=CARTESIAN_POINT ( 'NONE',  ( 11.53443712336079763, -2.942831166283299105, 7.824978679112010838 ) ) ;
#14270=CARTESIAN_POINT ( 'NONE',  ( 10.15596314287999924, -2.748296264808000267, 7.763860089407599752 ) ) ;
#14274=CARTESIAN_POINT ( 'NONE',  ( 10.55862282008599884, -3.333723918618700210, 6.425317846273999933 ) ) ;
#14278=ADVANCED_FACE ( 'NONE', ( #30115 ), #58649, .F. ) ;
#14283=CARTESIAN_POINT ( 'NONE',  ( 12.30233327354039830, -5.101536739857000846, 8.220500279733599314 ) ) ;
#14286=CARTESIAN_POINT ( 'NONE',  ( 11.02226222744799955, -4.880489021643899861, 6.774721295617600170 ) ) ;
#14323=CARTESIAN_POINT ( 'NONE',  ( 11.64256920625030034, -3.957769094421040190, 8.674127893687000324 ) ) ;
#14361=CARTESIAN_POINT ( 'NONE',  ( 11.20287750876920008, -4.469200303112399908, 6.771886227364699806 ) ) ;
#14409=CARTESIAN_POINT ( 'NONE',  ( 11.10441638348510018, -4.841589649988700117, 7.705001100909899314 ) ) ;
#14436=CARTESIAN_POINT ( 'NONE',  ( 11.43990547754509990, -2.967013601007999934, 7.467215766047949899 ) ) ;
#14452=CARTESIAN_POINT ( 'NONE',  ( 12.33518044953559922, -3.231951024059400268, 7.099502491684900107 ) ) ;
#14457=CARTESIAN_POINT ( 'NONE',  ( 10.46595058442700044, -3.655872208659600275, 8.295791434820300125 ) ) ;
#14464=PLANE ( 'NONE',  #63036 ) ;
#14467=CARTESIAN_POINT ( 'NONE',  ( 10.80226354018233259, -5.092232985442821658, 8.129523725463625894 ) ) ;
#14476=CARTESIAN_POINT ( 'NONE',  ( 9.599999931441001166, -4.000000000000000000, 7.500000000000000000 ) ) ;
#14490=ORIENTED_EDGE ( 'NONE', *, *, #60574, .T. ) ;
#14498=CARTESIAN_POINT ( 'NONE',  ( 10.71426717315700117, -4.869050473540199597, 8.240598219300300897 ) ) ;
#14527=SHAPE_DEFINITION_REPRESENTATION ( #66764, #60729 ) ;
#14549=ORIENTED_EDGE ( 'NONE', *, *, #33456, .F. ) ;
#14574=CARTESIAN_POINT ( 'NONE',  ( 11.46533729122639933, -5.140346530769000388, 7.529998433785960010 ) ) ;
#14600=AXIS2_PLACEMENT_3D ( 'NONE', #27136, #37613, #64513 ) ;
#14611=CARTESIAN_POINT ( 'NONE',  ( 9.094151519677000195, -3.975306837623020062, 6.358456126310000123 ) ) ;
#14614=CARTESIAN_POINT ( 'NONE',  ( 11.33810672858430024, -5.021298157087000114, 8.268288002587098617 ) ) ;
#14621=CARTESIAN_POINT ( 'NONE',  ( 11.97500581613029880, -3.011381429075500105, 6.865182626353099948 ) ) ;
#14623=CARTESIAN_POINT ( 'NONE',  ( 11.04687750876899877, -4.617914354660699772, 6.541108991297599928 ) ) ;
#14660=CARTESIAN_POINT ( 'NONE',  ( 11.18035971519489813, -3.321859513918399731, 8.628134814664999652 ) ) ;
#14700=CARTESIAN_POINT ( 'NONE',  ( 11.86333594839950045, -3.340240242524600056, 8.256087240512899328 ) ) ;
#14718=AXIS2_PLACEMENT_3D ( 'NONE', #49887, #8613, #28571 ) ;
#14730=CARTESIAN_POINT ( 'NONE',  ( 11.83570505509991833, -3.091015088729731186, 7.824998694764690121 ) ) ;
#14743=CARTESIAN_POINT ( 'NONE',  ( 12.11364291764652990, -4.859654669415900408, 7.606265891492399511 ) ) ;
#14776=CARTESIAN_POINT ( 'NONE',  ( 12.09603632436369125, -4.842640371965599932, 7.696781148700499564 ) ) ;
#14795=CARTESIAN_POINT ( 'NONE',  ( 10.23798825978600036, -4.113440707072600233, 6.640442468193600511 ) ) ;
#14836=CARTESIAN_POINT ( 'NONE',  ( 10.35764655415099966, -3.513729974241599940, 6.621146336197599958 ) ) ;
#14851=CARTESIAN_POINT ( 'NONE',  ( 11.14393020684970104, -2.750000000000000000, 7.500000000000000000 ) ) ;
#14864=CARTESIAN_POINT ( 'NONE',  ( 10.36476354018324741, -5.217465845835395299, 7.172815144550902744 ) ) ;
#14870=CARTESIAN_POINT ( 'NONE',  ( 11.96550210169813688, -4.058074521742473628, 6.192987292895718809 ) ) ;
#14874=EDGE_LOOP ( 'NONE', ( #27464, #57537, #68746, #57737, #20496, #23779 ) ) ;
#14909=DIRECTION ( 'NONE',  ( 0.000000000000000000, 1.000000000000000000, 0.000000000000000000 ) ) ;
#14911=CARTESIAN_POINT ( 'NONE',  ( 11.04272335273199879, -3.555125495332600138, 6.301916924546999255 ) ) ;
#14946=CARTESIAN_POINT ( 'NONE',  ( 10.13063399569800005, -2.728594541839999721, 7.358888170452400068 ) ) ;
#14958=CARTESIAN_POINT ( 'NONE',  ( 11.35168717260510007, -4.613789146762799831, 6.498190316041999814 ) ) ;
#14960=CARTESIAN_POINT ( 'NONE',  ( 11.36687616594229944, -4.344946439135400240, 8.587337146608000182 ) ) ;
#14996=CARTESIAN_POINT ( 'NONE',  ( 11.93345123989529988, -3.459769760840400110, 6.456682674800999777 ) ) ;
#15012=CARTESIAN_POINT ( 'NONE',  ( 12.10000000000000142, -4.304783012932057673, 8.455673667202290744 ) ) ;
#15023=CARTESIAN_POINT ( 'NONE',  ( 12.07299956498157023, -2.792989229543000107, 7.174999999999999822 ) ) ;
#15037=CARTESIAN_POINT ( 'NONE',  ( 11.98641235500450009, -4.739919807690899489, 8.177841818594698609 ) ) ;
#15082=CARTESIAN_POINT ( 'NONE',  ( 11.35056919669530018, -3.169300617545700138, 7.254567470917099747 ) ) ;
#15116=CARTESIAN_POINT ( 'NONE',  ( 11.22702344389999851, -5.004394439171999664, 8.109550315577399360 ) ) ;
#15119=CARTESIAN_POINT ( 'NONE',  ( 9.742292592096250203, -4.365494583328262124, 8.705986097797767442 ) ) ;
#15132=CARTESIAN_POINT ( 'NONE',  ( 11.25210807141120029, -3.959980833595939664, 6.634727177901499573 ) ) ;
#15154=DIRECTION ( 'NONE',  ( 0.000000000000000000, 0.8514543052404082157, -0.5244287998266055073 ) ) ;
#15174=CARTESIAN_POINT ( 'NONE',  ( 10.33231740696899870, -3.813190776280700245, 6.513113677132300161 ) ) ;
#15190=CARTESIAN_POINT ( 'NONE',  ( 11.10226354018308115, -2.907767014557176566, 6.870476274536374106 ) ) ;
#15257=CARTESIAN_POINT ( 'NONE',  ( 10.89503166480599994, -5.274847857784000560, 7.410114961806599787 ) ) ;
#15294=CARTESIAN_POINT ( 'NONE',  ( 9.953329965422000214, -4.888489908445900589, 6.579690231462300254 ) ) ;
#15307=CARTESIAN_POINT ( 'NONE',  ( 11.76723293495529887, -5.173938955706000264, 7.547192037433419820 ) ) ;
#15309=EDGE_CURVE ( 'NONE', #51764, #61432, #61121, .T. ) ;
#15310=CARTESIAN_POINT ( 'NONE',  ( 11.53918313518939875, -4.707599264529200411, 6.605241151424599444 ) ) ;
#15328=EDGE_CURVE ( 'NONE', #29598, #57705, #47059, .T. ) ;
#15330=DIRECTION ( 'NONE',  ( -1.000000000000000000, 0.000000000000000000, 0.000000000000000000 ) ) ;
#15345=CARTESIAN_POINT ( 'NONE',  ( 11.13880513895979973, -2.849548954067000039, 8.139542779846600240 ) ) ;
#15387=CARTESIAN_POINT ( 'NONE',  ( 11.22749279009020107, -4.225282629687599822, 6.663611138821799784 ) ) ;
#15404=DIRECTION ( 'NONE',  ( 1.000000000000000000, 0.000000000000000000, 0.000000000000000000 ) ) ;
#15432=CARTESIAN_POINT ( 'NONE',  ( 11.64595257254739913, -4.831736303435800295, 7.258104750172799768 ) ) ;
#15463=CARTESIAN_POINT ( 'NONE',  ( 10.97769598648999967, -2.990523684589000197, 6.898940957443399746 ) ) ;
#15474=EDGE_CURVE ( 'NONE', #55934, #2412, #52847, .T. ) ;
#15480=CARTESIAN_POINT ( 'NONE',  ( 10.79262282008599882, -3.548418513060800361, 6.771613406921599854 ) ) ;
#15523=CARTESIAN_POINT ( 'NONE',  ( 10.68692546752099837, -5.002009261081000524, 7.569424354486659290 ) ) ;
#15541=CARTESIAN_POINT ( 'NONE',  ( 10.83103907547008227, -3.225837863097585689, 7.100484084056944312 ) ) ;
#15575=CARTESIAN_POINT ( 'NONE',  ( 9.551300837857858994, -2.809882456706737308, 7.276433888703319752 ) ) ;
#15600=CARTESIAN_POINT ( 'NONE',  ( 11.14118447801630118, -2.722297859592000435, 7.528171279442569919 ) ) ;
#15646=CARTESIAN_POINT ( 'NONE',  ( 11.80367835872029936, -5.113555564477999305, 8.201822467543799178 ) ) ;
#15648=CARTESIAN_POINT ( 'NONE',  ( 10.94426222744800015, -4.986443098259000450, 6.687444528363699625 ) ) ;
#15672=CYLINDRICAL_SURFACE ( 'NONE', #4315, 1.250000000000000222 ) ;
#15684=CARTESIAN_POINT ( 'NONE',  ( 11.07102344389999971, -4.762665848028800220, 7.962849245488699879 ) ) ;
#15700=CARTESIAN_POINT ( 'NONE',  ( 11.50000000000000000, -2.920245322398999921, 7.174999999999999822 ) ) ;
#15728=CARTESIAN_POINT ( 'NONE',  ( 10.97718582084299932, -4.656536239972400182, 8.258888014436699621 ) ) ;
#15736=CARTESIAN_POINT ( 'NONE',  ( 11.60101463001529964, -3.377766160221900016, 8.496586578655598743 ) ) ;
#15771=CARTESIAN_POINT ( 'NONE',  ( 11.91672066707849886, -3.258843737379200078, 7.948314604624900248 ) ) ;
#15811=CARTESIAN_POINT ( 'NONE',  ( 11.39393020684959978, -5.250000000000000000, 7.500000000000000000 ) ) ;
#15814=CARTESIAN_POINT ( 'NONE',  ( 11.10441638348510018, -4.841589649988700117, 7.705001100909899314 ) ) ;
#15858=CARTESIAN_POINT ( 'NONE',  ( 10.88955864498000103, -3.209241371122599773, 6.880692865553299953 ) ) ;
#15937=CARTESIAN_POINT ( 'NONE',  ( 12.07656516821461068, -3.100463633631699967, 6.592171857671999646 ) ) ;
#15982=EDGE_LOOP ( 'NONE', ( #11149, #21650, #68673, #25770 ) ) ;
#15987=CARTESIAN_POINT ( 'NONE',  ( 11.01810807141099957, -3.940954591493389891, 6.223352037434000117 ) ) ;
#16008=CARTESIAN_POINT ( 'NONE',  ( 9.515584277044482064, -4.716917290452846245, 6.568532107505763662 ) ) ;
#16022=CARTESIAN_POINT ( 'NONE',  ( 11.48146005378009882, -3.088328798999600000, 7.986817550794899745 ) ) ;
#16062=CARTESIAN_POINT ( 'NONE',  ( 11.02641638348499953, -4.974961480482700260, 7.737488872214999702 ) ) ;
#16065=B_SPLINE_SURFACE_WITH_KNOTS ( 'NONE', 3, 3, ( 
 ( #66415, #18534, #61182, #55938, #29381, #2790, #24115, #45449, #29729, #8387, #4150, #19210, #36322, #25831, #47161, #25490, #24464, #20242, #40534, #56621, #51710, #19902, #8726, #51033, #30401, #31091, #46129, #62202, #30739, #14660, #15345, #63216, #67780, #45789, #62876 ),
 ( #3805, #9062, #61859, #68461, #41228, #41567, #25143, #19560, #46474, #14996, #46818, #36673, #20584, #9394, #41910, #3133, #14323, #35648, #9743, #67101, #13980, #62539, #35976, #40882, #57638, #57292, #56960, #30069, #52399, #35305, #68123, #51372, #4491, #3470, #24806 ),
 ( #67436, #52047, #5873, #6215, #17051, #69162, #63912, #59024, #58330, #27553, #5190, #37351, #64937, #11461, #11128, #26873, #32121, #58676, #16022, #43291, #53438, #10775, #68812, #48882, #48189, #642, #5534, #21271, #291, #21951, #53776, #43640, #989, #32460, #22300 ),
 ( #57993, #10093, #31428, #32802, #21610, #64253, #42943, #52744, #4839, #26180, #47507, #16366, #42601, #20933, #64596, #37695, #42268, #27211, #47855, #48536, #16706, #63572, #38035, #10432, #59361, #54116, #15684, #37018, #31773, #53090, #26527, #6565, #66672, #12166, #17409 ) ),
 .UNSPECIFIED., .F., .F., .F.,
 ( 4, 4 ),
 ( 4, 1, 1, 1, 1, 1, 1, 1, 1, 1, 1, 1, 1, 1, 1, 1, 1, 1, 1, 1, 1, 1, 1, 1, 1, 1, 1, 1, 1, 1, 1, 1, 4 ),
 ( -0.02000000000000000042, 1.020000000000000018 ),
 ( 0.1633025096610999927, 0.1899619885200000136, 0.2166214673788000034, 0.2432809462376999965, 0.2699404250964999585, 0.2965999039553000038, 0.3232593828141999692, 0.3499188616730000145, 0.3765783405318000043, 0.4032378193906999697, 0.4298972982494999595, 0.4565567771083000048, 0.4832162559671999702, 0.5098757348260000155, 0.5365352136848999809, 0.5631946925437000262, 0.5898541714025000715, 0.6165136502614000369, 0.6431731291201999712, 0.6698326079790000165, 0.6964920868378999819, 0.7231515656967000272, 0.7498110445554999615, 0.7764705234143999268, 0.8031300022731999722, 0.8297894811320000175, 0.8564489599908999828, 0.8831084388497000282, 0.9097679177085999935, 0.9364273965674000388, 0.9630868754261999731, 0.9897463542851000495, 1.016405833144000015 ),
 .UNSPECIFIED. ) ;
#16068=CARTESIAN_POINT ( 'NONE',  ( 10.97769598648999967, -2.990523684589000197, 6.898940957443399746 ) ) ;
#16110=CARTESIAN_POINT ( 'NONE',  ( 11.56795257254739973, -4.963546614172099858, 7.219770138693499817 ) ) ;
#16145=CARTESIAN_POINT ( 'NONE',  ( 9.681310023244000362, -3.426978632899654542, 8.622334741229296995 ) ) ;
#16156=CARTESIAN_POINT ( 'NONE',  ( 11.69518313518939934, -4.537300658085600347, 6.820583637845799352 ) ) ;
#16194=ORIENTED_EDGE ( 'NONE', *, *, #64871, .F. ) ;
#16203=CARTESIAN_POINT ( 'NONE',  ( 9.749747021775998945, -4.754947163618299832, 6.837506920432799618 ) ) ;
#16221=ORIENTED_EDGE ( 'NONE', *, *, #26372, .T. ) ;
#16231=LINE ( 'NONE', #48395, #506 ) ;
#16264=CARTESIAN_POINT ( 'NONE',  ( 9.210288521113000115, -4.352953559891299840, 6.715449042252499723 ) ) ;
#16282=CARTESIAN_POINT ( 'NONE',  ( 12.10118044953561878, -2.866798846279000390, 6.909094663619399945 ) ) ;
#16316=CARTESIAN_POINT ( 'NONE',  ( 9.142797255588000382, -2.721932483203000075, 7.554109351283189611 ) ) ;
#16323=AXIS2_PLACEMENT_3D ( 'NONE', #41890, #63196, #4819 ) ;
#16330=CARTESIAN_POINT ( 'NONE',  ( 11.60887482311539998, -2.815046254222000055, 7.021250586468399391 ) ) ;
#16336=CARTESIAN_POINT ( 'NONE',  ( 10.09393020685000053, -2.750000000000000000, 7.500000000000000000 ) ) ;
#16366=CARTESIAN_POINT ( 'NONE',  ( 11.69434208742519843, -4.478858766422799675, 6.747282993577999655 ) ) ;
#16406=CARTESIAN_POINT ( 'NONE',  ( 11.07564694612699974, -4.931992688388300294, 7.128058497017000228 ) ) ;
#16411=CARTESIAN_POINT ( 'NONE',  ( 11.02799293566599914, -3.193321847920899792, 6.510429574318199464 ) ) ;
#16417=EDGE_CURVE ( 'NONE', #35697, #13467, #42384, .T. ) ;
#16438=ADVANCED_FACE ( 'NONE', ( #58115 ), #5521, .T. ) ;
#16450=CARTESIAN_POINT ( 'NONE',  ( 11.86333594839950045, -3.340240242524600056, 8.256087240512899328 ) ) ;
#16498=CARTESIAN_POINT ( 'NONE',  ( 10.88287885159599888, -3.139900861731399928, 7.602606670248799325 ) ) ;
#16520=EDGE_CURVE ( 'NONE', #1441, #61281, #35271, .T. ) ;
#16547=CARTESIAN_POINT ( 'NONE',  ( 10.02635508232799921, -4.388021368982800041, 8.275336934318801241 ) ) ;
#16564=CARTESIAN_POINT ( 'NONE',  ( 11.22299000889467635, -4.227343628179307977, 6.655959434011009535 ) ) ;
#16579=CARTESIAN_POINT ( 'NONE',  ( 10.59393020684899867, -2.750000000000000000, 7.500000000000000000 ) ) ;
#16603=VERTEX_POINT ( 'NONE', #27332 ) ;
#16630=CARTESIAN_POINT ( 'NONE',  ( 10.13370934641699961, -2.844451673749999632, 8.048718920009699573 ) ) ;
#16660=CARTESIAN_POINT ( 'NONE',  ( 9.370759580229000463, -5.244164909883999748, 7.797385380423699885 ) ) ;
#16670=CARTESIAN_POINT ( 'NONE',  ( 9.599999931441001166, -2.935682118448999844, 6.844464000216799349 ) ) ;
#16672=CARTESIAN_POINT ( 'NONE',  ( 10.22934687351666661, -4.163624617374463099, 8.750000000000000000 ) ) ;
#16674=CARTESIAN_POINT ( 'NONE',  ( 10.79657053952199952, -4.502253688815499366, 8.675184076076000395 ) ) ;
#16678=CARTESIAN_POINT ( 'NONE',  ( 9.916846873516668381, -4.768183399968644487, 6.500416447002274722 ) ) ;
#16697=CARTESIAN_POINT ( 'NONE',  ( 11.65221028326116048, -4.908903471848705458, 7.824988602100019008 ) ) ;
#16706=CARTESIAN_POINT ( 'NONE',  ( 11.32035090130999855, -3.241273085157000189, 7.030721746772699454 ) ) ;
#16717=EDGE_CURVE ( 'NONE', #52202, #41725, #19404, .T. ) ;
#16726=FACE_OUTER_BOUND ( 'NONE', #26122, .T. ) ;
#16745=CARTESIAN_POINT ( 'NONE',  ( 11.22333863405319931, -3.380905141010200232, 6.710270673950399889 ) ) ;
#16752=CARTESIAN_POINT ( 'NONE',  ( 11.05569598648999907, -2.869047858956000230, 6.826612223887499553 ) ) ;
#16784=ORIENTED_EDGE ( 'NONE', *, *, #54718, .T. ) ;
#16839=CARTESIAN_POINT ( 'NONE',  ( 11.54333729122640051, -5.003122373830000136, 7.526388557597149642 ) ) ;
#16888=CARTESIAN_POINT ( 'NONE',  ( 9.547113844317999920, -3.746347404385800051, 8.471855267550699509 ) ) ;
#16901=EDGE_CURVE ( 'NONE', #30682, #46086, #57592, .T. ) ;
#16902=CARTESIAN_POINT ( 'NONE',  ( 11.29683585285767755, -3.460706475588385178, 6.812066793331982950 ) ) ;
#16904=CARTESIAN_POINT ( 'NONE',  ( 12.08902763632552002, -4.786505910413500153, 7.862914650060299770 ) ) ;
#16969=CARTESIAN_POINT ( 'NONE',  ( 10.18436764078099976, -3.396982508013000501, 8.628164124510998789 ) ) ;
#16991=B_SPLINE_CURVE_WITH_KNOTS ( 'NONE', 3,
 ( #12791, #39017, #65569, #18040, #6842, #1603, #48809, #61025, #23614, #13142 ),
 .UNSPECIFIED., .F., .F.,
 ( 4, 2, 2, 2, 4 ),
 ( 0.000000000000000000, 0.2500000000000001665, 0.5000000000000003331, 0.7500000000000001110, 1.000000000000000000 ),
 .UNSPECIFIED. ) ;
#17016=CARTESIAN_POINT ( 'NONE',  ( 11.26426088462129904, -3.997280690308189666, 8.778009775371000245 ) ) ;
#17021=CARTESIAN_POINT ( 'NONE',  ( 10.01059687351666661, -3.370476274536376771, 6.407767014557176566 ) ) ;
#17051=CARTESIAN_POINT ( 'NONE',  ( 12.06322412107030928, -3.945399343424460525, 8.532060764998998792 ) ) ;
#17090=CARTESIAN_POINT ( 'NONE',  ( 10.78026357027499849, -3.014700852776899698, 7.309904858193100097 ) ) ;
#17098=CARTESIAN_POINT ( 'NONE',  ( 11.18035971519489813, -3.321859513918399731, 8.628134814664999652 ) ) ;
#17130=CARTESIAN_POINT ( 'NONE',  ( 10.20815392832262702, -4.380187932396833794, 6.711971190259613529 ) ) ;
#17172=CARTESIAN_POINT ( 'NONE',  ( 9.758504216683469679, -3.836370129433865017, 8.749972943975897977 ) ) ;
#17196=CARTESIAN_POINT ( 'NONE',  ( 10.75851354018278982, -3.836375382625526687, 8.749999999999996447 ) ) ;
#17241=CARTESIAN_POINT ( 'NONE',  ( 10.15300081823900058, -4.767147064380999666, 7.096028062709999418 ) ) ;
#17325=CARTESIAN_POINT ( 'NONE',  ( 10.33634252387499863, -5.264483068122999931, 7.693563834190999984 ) ) ;
#17345=EDGE_CURVE ( 'NONE', #19919, #46460, #857, .T. ) ;
#17398=EDGE_CURVE ( 'NONE', #67539, #41699, #9192, .T. ) ;
#17402=B_SPLINE_CURVE_WITH_KNOTS ( 'NONE', 3,
 ( #635, #16697, #38375, #48180 ),
 .UNSPECIFIED., .F., .F.,
 ( 4, 4 ),
 ( 0.000000000000000000, 1.000000000000000000 ),
 .UNSPECIFIED. ) ;
#17409=CARTESIAN_POINT ( 'NONE',  ( 10.78014141025500017, -3.582647672488299850, 6.756653759087999589 ) ) ;
#17447=CARTESIAN_POINT ( 'NONE',  ( 10.46192546752100050, -5.139081147506999514, 7.578921399676699089 ) ) ;
#17450=CARTESIAN_POINT ( 'NONE',  ( 11.39149144726329865, -4.659577337894599935, 8.430724369296298093 ) ) ;
#17458=CARTESIAN_POINT ( 'NONE',  ( 10.87199293566600034, -3.366612813978900220, 6.723009541442299231 ) ) ;
#17510=CARTESIAN_POINT ( 'NONE',  ( 9.680747021775999883, -4.651672637235799712, 6.928134003122899287 ) ) ;
#17523=ORIENTED_EDGE ( 'NONE', *, *, #52867, .T. ) ;
#17556=CARTESIAN_POINT ( 'NONE',  ( 10.81059687351633336, -4.629523725463621453, 8.592232985442823434 ) ) ;
#17588=AXIS2_PLACEMENT_3D ( 'NONE', #1675, #7262, #2364 ) ;
#17595=CARTESIAN_POINT ( 'NONE',  ( 9.722405316139999698, -4.184077495686000958, 6.652755395362000002 ) ) ;
#17618=CARTESIAN_POINT ( 'NONE',  ( 12.01518179236249040, -4.180996681294200101, 8.347076615013298451 ) ) ;
#17681=CARTESIAN_POINT ( 'NONE',  ( 10.79226717315700057, -4.973628086880700572, 8.329718467866699783 ) ) ;
#17707=CARTESIAN_POINT ( 'NONE',  ( 12.08810207955109917, -4.796537143354000499, 7.825000000000000178 ) ) ;
#17761=CARTESIAN_POINT ( 'NONE',  ( 10.97718582084299932, -4.656536239972400182, 8.258888014436699621 ) ) ;
#17764=FACE_OUTER_BOUND ( 'NONE', #66585, .T. ) ;
#17782=CARTESIAN_POINT ( 'NONE',  ( 9.234200250017998712, -3.906155787512310074, 6.613277660092100163 ) ) ;
#17798=CARTESIAN_POINT ( 'NONE',  ( 10.08198825978599977, -4.149395984695000372, 6.368003848175999515 ) ) ;
#17801=CARTESIAN_POINT ( 'NONE',  ( 10.97303166480599934, -5.137916160623999140, 7.419769534118209720 ) ) ;
#17804=CARTESIAN_POINT ( 'NONE',  ( 10.12309687351566900, -2.782534154164605145, 7.172815144550900968 ) ) ;
#17812=CARTESIAN_POINT ( 'NONE',  ( 11.56456920625009843, -3.962850971080120299, 8.532838639935999225 ) ) ;
#17840=CARTESIAN_POINT ( 'NONE',  ( 10.68940772478662637, -4.553612660159668479, 6.822471183635139269 ) ) ;
#17862=CARTESIAN_POINT ( 'NONE',  ( 10.10932996542199902, -4.697624103824200148, 6.777391592843399870 ) ) ;
#17886=B_SPLINE_CURVE_WITH_KNOTS ( 'NONE', 3,
 ( #59673, #1638, #6529, #22952, #44307, #42907, #53400, #37315, #26835, #16672, #7226, #24341, #13856, #35184, #61401, #12473, #8260, #28563 ),
 .UNSPECIFIED., .F., .F.,
 ( 4, 2, 2, 2, 2, 2, 2, 2, 4 ),
 ( 0.000000000000000000, 0.1250000000000003331, 0.2500000000000006661, 0.3750000000000009992, 0.5000000000000013323, 0.6250000000000009992, 0.7500000000000006661, 0.8750000000000003331, 1.000000000000000000 ),
 .UNSPECIFIED. ) ;
#17905=CARTESIAN_POINT ( 'NONE',  ( 10.82101354018304207, -4.768183399968640934, 8.499583552997727054 ) ) ;
#17925=EDGE_CURVE ( 'NONE', #65484, #53853, #27608, .T. ) ;
#17943=CARTESIAN_POINT ( 'NONE',  ( 10.43162143724499913, -3.424116261072899903, 8.148124882831599081 ) ) ;
#17964=CARTESIAN_POINT ( 'NONE',  ( 12.11364291764652990, -4.859654669415900408, 7.606265891492399511 ) ) ;
#18024=CARTESIAN_POINT ( 'NONE',  ( 10.72272469555899832, -3.360453478306600239, 8.606479382885998675 ) ) ;
#18030=CARTESIAN_POINT ( 'NONE',  ( 10.86825461470400001, -5.239722547583999912, 7.184607557167700165 ) ) ;
#18040=CARTESIAN_POINT ( 'NONE',  ( 11.68424042080583547, -3.455907502640803486, 8.657883396625683403 ) ) ;
#18100=FACE_OUTER_BOUND ( 'NONE', #63738, .T. ) ;
#18103=CARTESIAN_POINT ( 'NONE',  ( 12.08487348028855024, -4.882707455860599843, 7.022738645480499642 ) ) ;
#18139=CARTESIAN_POINT ( 'NONE',  ( 10.20863399569799945, -2.865156490077000129, 7.374045024026299799 ) ) ;
#18140=EDGE_LOOP ( 'NONE', ( #31356, #10603, #14490, #33077, #53648 ) ) ;
#18143=CARTESIAN_POINT ( 'NONE',  ( 10.63662282008600002, -3.405288783432600219, 6.540749699823199315 ) ) ;
#18153=CARTESIAN_POINT ( 'NONE',  ( 12.00687348028854906, -5.003459210197000573, 6.957450711802899868 ) ) ;
#18154=CARTESIAN_POINT ( 'NONE',  ( 11.06591429142999949, -3.980313504646230349, 8.533318907609000803 ) ) ;
#18176=EDGE_CURVE ( 'NONE', #34355, #36450, #30706, .T. ) ;
#18182=CARTESIAN_POINT ( 'NONE',  ( 9.549596101582627838, -4.563377510236459322, 8.169431139013614285 ) ) ;
#18188=CARTESIAN_POINT ( 'NONE',  ( 9.307788144226000426, -3.909067355573210278, 6.546538158064899804 ) ) ;
#18202=CARTESIAN_POINT ( 'NONE',  ( 10.51459632033899894, -4.929952350555500296, 7.879514065647800436 ) ) ;
#18225=CARTESIAN_POINT ( 'NONE',  ( 9.893930206848999376, -5.250000000000000000, 7.500000000000000000 ) ) ;
#18287=CARTESIAN_POINT ( 'NONE',  ( 9.367797255588000027, -3.133765047594600173, 7.536673658251589636 ) ) ;
#18288=CARTESIAN_POINT ( 'NONE',  ( 11.49999975383417450, -5.062986770486452848, 7.633391978603163430 ) ) ;
#18327=CARTESIAN_POINT ( 'NONE',  ( 11.54664311227086948, -3.555960431980462300, 6.293666904468257606 ) ) ;
#18341=DIRECTION ( 'NONE',  ( 1.000000000000000000, 0.000000000000000000, 0.000000000000000000 ) ) ;
#18371=CARTESIAN_POINT ( 'NONE',  ( 10.43564655415099907, -3.447209681134600245, 6.500921769151600138 ) ) ;
#18445=CARTESIAN_POINT ( 'NONE',  ( 12.01102763632551884, -4.911148285670300595, 7.920427941950599404 ) ) ;
#18468=CARTESIAN_POINT ( 'NONE',  ( 9.234020077949999461, -4.063547279775290733, 6.621188087644399367 ) ) ;
#18484=CARTESIAN_POINT ( 'NONE',  ( 9.704063610504999104, -3.588011994494999968, 6.583971515917899531 ) ) ;
#18489=CARTESIAN_POINT ( 'NONE',  ( 10.80072469555900128, -3.429147315060100176, 8.487632181750699445 ) ) ;
#18499=CARTESIAN_POINT ( 'NONE',  ( 11.39564560330030041, -3.692495237344800341, 8.455191956516999952 ) ) ;
#18500=CARTESIAN_POINT ( 'NONE',  ( 11.19057802013490033, -5.033226574983999946, 7.524052967375959966 ) ) ;
#18534=CARTESIAN_POINT ( 'NONE',  ( 12.33003632436370012, -5.243255406354000669, 7.790336465152099876 ) ) ;
#18549=CARTESIAN_POINT ( 'NONE',  ( 9.881367640780998940, -3.526522998810799781, 8.385811396220899994 ) ) ;
#18556=LINE ( 'NONE', #61883, #22927 ) ;
#18558=ADVANCED_BREP_SHAPE_REPRESENTATION ( '', ( #53935, #9676 ), #9731 ) ;
#18601=B_SPLINE_CURVE_WITH_KNOTS ( 'NONE', 3,
 ( #18820, #51984, #14259, #35588 ),
 .UNSPECIFIED., .F., .F.,
 ( 4, 4 ),
 ( 0.000000000000000000, 1.000000000000000000 ),
 .UNSPECIFIED. ) ;
#18631=CARTESIAN_POINT ( 'NONE',  ( 9.241151519676998660, -3.981249765141819719, 6.633192605878799775 ) ) ;
#18712=CARTESIAN_POINT ( 'NONE',  ( 9.802417874594000935, -5.050800927762999493, 7.053287723251499663 ) ) ;
#18730=SURFACE_STYLE_FILL_AREA ( #50540 ) ;
#18791=CARTESIAN_POINT ( 'NONE',  ( 11.80995122972050027, -3.547233695387300045, 8.547040013405998948 ) ) ;
#18820=CARTESIAN_POINT ( 'NONE',  ( 11.61486084871780022, -2.792989229543000107, 7.825000000000000178 ) ) ;
#18831=CARTESIAN_POINT ( 'NONE',  ( 10.56324205624999912, -4.409476560233800413, 6.434137271007999814 ) ) ;
#18834=CARTESIAN_POINT ( 'NONE',  ( 11.60887482311539998, -2.815046254222000055, 7.021250586468399391 ) ) ;
#18844=CARTESIAN_POINT ( 'NONE',  ( 11.17410807141120088, -3.953638752893899877, 6.497602131078999754 ) ) ;
#18845=CARTESIAN_POINT ( 'NONE',  ( 11.02946886766499901, -4.430164648092599577, 8.281567006984099422 ) ) ;
#18894=CARTESIAN_POINT ( 'NONE',  ( 9.452784697134999803, -3.529509552262100058, 8.228249052908999772 ) ) ;
#18900=CARTESIAN_POINT ( 'NONE',  ( 9.324071121570657539, -3.025928824985222754, 7.751553442067931066 ) ) ;
#19004=CARTESIAN_POINT ( 'NONE',  ( 10.74457120343299898, -4.042028078047379402, 6.634008278083699750 ) ) ;
#19020=DIRECTION ( 'NONE',  ( 0.000000000000000000, 0.000000000000000000, 1.000000000000000000 ) ) ;
#19045=CARTESIAN_POINT ( 'NONE',  ( 9.475151519677000422, -3.972335373863620234, 6.221087886525999089 ) ) ;
#19047=CARTESIAN_POINT ( 'NONE',  ( 12.08810207955109917, -4.796537143354000499, 7.825000000000000178 ) ) ;
#19120=CARTESIAN_POINT ( 'NONE',  ( 11.85918179236250047, -4.238363971154499588, 8.615559381441000752 ) ) ;
#19135=CARTESIAN_POINT ( 'NONE',  ( 9.236413463905998711, -3.915843685459630574, 6.617590440947399344 ) ) ;
#19142=ORIENTED_EDGE ( 'NONE', *, *, #12414, .F. ) ;
#19160=CARTESIAN_POINT ( 'NONE',  ( 9.119480666858999385, -3.619299191678599925, 6.423523106103999680 ) ) ;
#19174=CARTESIAN_POINT ( 'NONE',  ( 10.87872469555899890, -3.497841151814999883, 8.368784980615899372 ) ) ;
#19177=ORIENTED_EDGE ( 'NONE', *, *, #39025, .T. ) ;
#19210=CARTESIAN_POINT ( 'NONE',  ( 11.92834208742529967, -4.706521750018099581, 6.389420067180999752 ) ) ;
#19223=CARTESIAN_POINT ( 'NONE',  ( 12.09999999999999787, -3.165084187357962264, 8.298683811023391144 ) ) ;
#19246=CARTESIAN_POINT ( 'NONE',  ( 12.27359063708300013, -3.044227915785300276, 7.231278212164300001 ) ) ;
#19322=CARTESIAN_POINT ( 'NONE',  ( 12.02677869730533011, -4.403502086956500250, 8.295667533166499297 ) ) ;
#19346=CARTESIAN_POINT ( 'NONE',  ( 10.41529229006299850, -3.250213325543700016, 7.935348007132199122 ) ) ;
#19354=FACE_OUTER_BOUND ( 'NONE', #29944, .T. ) ;
#19388=CARTESIAN_POINT ( 'NONE',  ( 9.929063610504998749, -3.531653260805799999, 6.458661544034999480 ) ) ;
#19404=B_SPLINE_CURVE_WITH_KNOTS ( 'NONE', 3,
 ( #48306, #413, #11242, #22073 ),
 .UNSPECIFIED., .F., .F.,
 ( 4, 4 ),
 ( 0.000000000000000000, 1.000000000000000000 ),
 .UNSPECIFIED. ) ;
#19462=B_SPLINE_CURVE_WITH_KNOTS ( 'NONE', 3,
 ( #39678, #12766, #2271, #6816, #28505, #60310, #12417, #44931, #6470, #49122, #23589, #65543, #65192, #27817, #54717, #23939, #34093, #28861 ),
 .UNSPECIFIED., .F., .F.,
 ( 4, 2, 2, 2, 2, 2, 2, 2, 4 ),
 ( 0.000000000000000000, 0.1250000000000003331, 0.2500000000000006661, 0.3750000000000009992, 0.5000000000000013323, 0.6250000000000009992, 0.7500000000000006661, 0.8750000000000003331, 1.000000000000000000 ),
 .UNSPECIFIED. ) ;
#19467=CARTESIAN_POINT ( 'NONE',  ( 11.07149279008999976, -4.296686446741600385, 6.398515879103999993 ) ) ;
#19509=CARTESIAN_POINT ( 'NONE',  ( 9.372772138682000431, -4.424886761933599644, 8.559813987224998755 ) ) ;
#19512=CARTESIAN_POINT ( 'NONE',  ( 10.87041638348499895, -5.241705141469999774, 7.802464414828100381 ) ) ;
#19519=CARTESIAN_POINT ( 'NONE',  ( 11.30502344389999969, -5.125258734743999511, 8.182900850620900002 ) ) ;
#19521=CARTESIAN_POINT ( 'NONE',  ( 11.48995257254740032, -5.095356924909000718, 7.181435527216799564 ) ) ;
#19523=ORIENTED_EDGE ( 'NONE', *, *, #64292, .T. ) ;
#19555=CARTESIAN_POINT ( 'NONE',  ( 9.251496707488000126, -3.918323994020610268, 6.643597378104299622 ) ) ;
#19560=CARTESIAN_POINT ( 'NONE',  ( 12.01656039236534923, -2.826501801118000312, 7.442888368925779652 ) ) ;
#19577=CARTESIAN_POINT ( 'NONE',  ( 12.10000000000000142, -3.752125624359934353, 8.548800951397312886 ) ) ;
#19596=CARTESIAN_POINT ( 'NONE',  ( 9.289886373836322875, -3.999992178805580334, 6.560153657526066162 ) ) ;
#19601=CARTESIAN_POINT ( 'NONE',  ( 11.37518447801629939, -3.134012688501500055, 7.519093628927509876 ) ) ;
#19630=CARTESIAN_POINT ( 'NONE',  ( 9.535395982797806980, -4.311073552809155274, 6.345787448237017792 ) ) ;
#19643=DIRECTION ( 'NONE',  ( 0.000000000000000000, 1.000000000000000000, 0.000000000000000000 ) ) ;
#19645=CARTESIAN_POINT ( 'NONE',  ( 12.33518044953559922, -3.231951024059400268, 7.099502491684900107 ) ) ;
#19661=CARTESIAN_POINT ( 'NONE',  ( 9.249283493600000128, -3.910012670022149806, 6.649720865199900466 ) ) ;
#19675=CARTESIAN_POINT ( 'NONE',  ( 12.17403632436368888, -4.976178716761900489, 7.727966254184200245 ) ) ;
#19686=CARTESIAN_POINT ( 'NONE',  ( 12.09999999999999964, -4.000000000000000000, 7.500000000000000000 ) ) ;
#19698=CARTESIAN_POINT ( 'NONE',  ( 9.858051052051999719, -3.149129950522900234, 7.333482423122699601 ) ) ;
#19739=CARTESIAN_POINT ( 'NONE',  ( 10.89157120343299923, -4.055348968344419269, 6.359530327585999565 ) ) ;
#19753=CARTESIAN_POINT ( 'NONE',  ( 10.90434687351665310, -5.250000000000000888, 7.336375382625536901 ) ) ;
#19813=CARTESIAN_POINT ( 'NONE',  ( 11.29303032197930001, -3.336467919271199900, 8.427909097977700270 ) ) ;
#19851=CARTESIAN_POINT ( 'NONE',  ( 10.33326717315600085, -4.973628086880700572, 8.329718467866699783 ) ) ;
#19854=CARTESIAN_POINT ( 'NONE',  ( 11.23964560330029983, -3.608363763633400279, 8.716526793355999558 ) ) ;
#19856=CARTESIAN_POINT ( 'NONE',  ( 10.07101354018233508, -3.231816600031356845, 6.500416447002274722 ) ) ;
#19861=CARTESIAN_POINT ( 'NONE',  ( 12.18277869730536977, -4.531392946702499813, 8.547856079839998955 ) ) ;
#19864=CARTESIAN_POINT ( 'NONE',  ( 10.62841772631199966, -3.509411006705700053, 6.490165927606000196 ) ) ;
#19902=CARTESIAN_POINT ( 'NONE',  ( 11.51279632507520034, -3.375091146194399983, 6.341531314375999706 ) ) ;
#19906=B_SPLINE_CURVE_WITH_KNOTS ( 'NONE', 3,
 ( #10899, #11239, #22068, #9868, #32576, #32245, #16145, #53888, #10212, #42382, #15119, #37815, #64024, #31895, #37131, #31212, #65, #53206 ),
 .UNSPECIFIED., .F., .F.,
 ( 4, 2, 2, 2, 2, 2, 2, 2, 4 ),
 ( 0.000000000000000000, 0.1250000000000000000, 0.2500000000000000000, 0.3750000000000000000, 0.5000000000000000000, 0.6250000000000000000, 0.7500000000000000000, 0.8750000000000000000, 1.000000000000000000 ),
 .UNSPECIFIED. ) ;
#19919=VERTEX_POINT ( 'NONE', #19596 ) ;
#19944=CARTESIAN_POINT ( 'NONE',  ( 12.06025819896753859, -4.986099335708799707, 7.314099615601099558 ) ) ;
#19992=CARTESIAN_POINT ( 'NONE',  ( 11.54749144726329924, -4.500836215462999945, 8.206726025856399431 ) ) ;
#20019=CARTESIAN_POINT ( 'NONE',  ( 12.10477869730532774, -4.467447516829900600, 8.421761806503198500 ) ) ;
#20032=CARTESIAN_POINT ( 'NONE',  ( 12.03979707368350027, -4.430269712815499972, 8.251775607861899786 ) ) ;
#20036=ORIENTED_EDGE ( 'NONE', *, *, #66212, .T. ) ;
#20078=CARTESIAN_POINT ( 'NONE',  ( 9.876392757686998536, -3.322036695224600322, 6.758914271013199304 ) ) ;
#20081=EDGE_LOOP ( 'NONE', ( #29233, #3202, #29176, #42654 ) ) ;
#20154=CARTESIAN_POINT ( 'NONE',  ( 10.80487885159599948, -3.003595720052600448, 7.618867373350600047 ) ) ;
#20188=CARTESIAN_POINT ( 'NONE',  ( 10.18129229006300029, -2.893743561734000380, 8.142324746736500529 ) ) ;
#20199=CARTESIAN_POINT ( 'NONE',  ( 11.93345123989529988, -3.459769760840400110, 6.456682674800999777 ) ) ;
#20201=CARTESIAN_POINT ( 'NONE',  ( 12.11759063708296047, -2.782734359457999851, 7.157757529645699890 ) ) ;
#20227=CARTESIAN_POINT ( 'NONE',  ( 11.66486084871730000, -2.792989229543000107, 7.825000000000000178 ) ) ;
#20242=CARTESIAN_POINT ( 'NONE',  ( 11.67901463001530082, -3.302889347096799710, 8.616511311517999872 ) ) ;
#20282=CARTESIAN_POINT ( 'NONE',  ( 12.23256516821459883, -3.293702443348299980, 6.787191910456499500 ) ) ;
#20324=CARTESIAN_POINT ( 'NONE',  ( 11.07980110216399972, -4.739241740354600552, 7.951464549725199227 ) ) ;
#20359=CARTESIAN_POINT ( 'NONE',  ( 11.23213259636990102, -4.907524392912299582, 7.005495010505599751 ) ) ;
#20374=CARTESIAN_POINT ( 'NONE',  ( 11.15364694612719809, -4.804498860841600383, 7.178938988280099132 ) ) ;
#20400=CARTESIAN_POINT ( 'NONE',  ( 11.68114303127866194, -4.620698129841968260, 6.880574739649333083 ) ) ;
#20418=CARTESIAN_POINT ( 'NONE',  ( 9.523797255587998833, -2.859210004667000149, 7.548297453605989027 ) ) ;
#20435=CARTESIAN_POINT ( 'NONE',  ( 11.02934687351650389, -3.836375382625533348, 6.250000000000000000 ) ) ;
#20496=ORIENTED_EDGE ( 'NONE', *, *, #216, .F. ) ;
#20498=CARTESIAN_POINT ( 'NONE',  ( 10.99349279008999858, -4.332388355267299929, 6.265968249244999733 ) ) ;
#20534=CARTESIAN_POINT ( 'NONE',  ( 9.727380199234000102, -2.867101906753999785, 7.642395078236999595 ) ) ;
#20548=CARTESIAN_POINT ( 'NONE',  ( 11.02799293566599914, -3.193321847920899792, 6.510429574318199464 ) ) ;
#20550=CARTESIAN_POINT ( 'NONE',  ( 11.63764426047339917, -3.386171819220400003, 6.538488127609999978 ) ) ;
#20551=CARTESIAN_POINT ( 'NONE',  ( 10.78014141025500017, -3.582647672488299850, 6.756653759087999589 ) ) ;
#20584=CARTESIAN_POINT ( 'NONE',  ( 11.80878751119029957, -5.041025164610000608, 6.955365841266999638 ) ) ;
#20601=CARTESIAN_POINT ( 'NONE',  ( 12.09999999999999787, -3.195619894033321806, 8.322973907256258741 ) ) ;
#20627=CARTESIAN_POINT ( 'NONE',  ( 11.88795122972049967, -3.601717549869600354, 8.421043941822800249 ) ) ;
#20656=( LENGTH_UNIT ( ) NAMED_UNIT ( * ) SI_UNIT ( .MILLI., .METRE. ) );
#20672=CARTESIAN_POINT ( 'NONE',  ( 11.74441369783139955, -4.043700988887960257, 6.634905315059499209 ) ) ;
#20703=CARTESIAN_POINT ( 'NONE',  ( 11.86056039236529891, -3.108928759355700233, 7.456633480985620288 ) ) ;
#20719=CARTESIAN_POINT ( 'NONE',  ( 12.06025819896753859, -4.986099335708799707, 7.314099615601099558 ) ) ;
#20726=CARTESIAN_POINT ( 'NONE',  ( 12.14122412107036908, -3.937930136014310190, 8.673243607771999208 ) ) ;
#20764=CARTESIAN_POINT ( 'NONE',  ( 9.927051052051998781, -3.014287398677499841, 7.307093369932900373 ) ) ;
#20814=ORIENTED_EDGE ( 'NONE', *, *, #1973, .T. ) ;
#20844=CARTESIAN_POINT ( 'NONE',  ( 12.05194988689359903, -3.419512757306400363, 6.361426117087999543 ) ) ;
#20885=CARTESIAN_POINT ( 'NONE',  ( 9.935596873515667227, -5.092232985442824322, 6.870476274536375882 ) ) ;
#20892=CARTESIAN_POINT ( 'NONE',  ( 11.68412378248529926, -4.549028353065900809, 8.538714411016998795 ) ) ;
#20894=CARTESIAN_POINT ( 'NONE',  ( 11.85918179236250047, -4.238363971154499588, 8.615559381441000752 ) ) ;
#20933=CARTESIAN_POINT ( 'NONE',  ( 11.61123293495519881, -4.891405920092699589, 7.535834283667469435 ) ) ;
#20974=CARTESIAN_POINT ( 'NONE',  ( 11.12487750876920067, -4.543557328885200697, 6.656497609330299881 ) ) ;
#20982=CARTESIAN_POINT ( 'NONE',  ( 11.72056920625029974, -3.952687217764870198, 8.815417147437999645 ) ) ;
#21011=CARTESIAN_POINT ( 'NONE',  ( 9.224507172011824352, -4.124235577930278396, 6.625492773506611144 ) ) ;
#21018=CARTESIAN_POINT ( 'NONE',  ( 11.30133863405320049, -3.465595476214000215, 6.818303296693398963 ) ) ;
#21057=DIRECTION ( 'NONE',  ( -1.000000000000000000, 0.000000000000000000, 0.000000000000000000 ) ) ;
#21059=CARTESIAN_POINT ( 'NONE',  ( 11.53482133862663694, -3.057020944820409536, 6.626386139742056258 ) ) ;
#21064=CARTESIAN_POINT ( 'NONE',  ( 10.85826357027499967, -3.149486845331399998, 7.335909308151700614 ) ) ;
#21110=CARTESIAN_POINT ( 'NONE',  ( 9.825734463322998380, -3.895375416816699854, 6.501052555474699624 ) ) ;
#21113=ORIENTED_EDGE ( 'NONE', *, *, #15328, .T. ) ;
#21127=CARTESIAN_POINT ( 'NONE',  ( 11.17375944625267792, -4.674697381537265883, 6.944236520041479288 ) ) ;
#21140=EDGE_CURVE ( 'NONE', #41725, #55934, #29102, .T. ) ;
#21143=CARTESIAN_POINT ( 'NONE',  ( 10.45851354018287616, -4.163624617374470205, 6.250000000000000000 ) ) ;
#21185=CARTESIAN_POINT ( 'NONE',  ( 11.31349144726329925, -4.738947899111299655, 8.542723541016000510 ) ) ;
#21230=VERTEX_POINT ( 'NONE', #67431 ) ;
#21234=CARTESIAN_POINT ( 'NONE',  ( 11.48579841651039857, -4.449968941611500028, 6.303820944768999901 ) ) ;
#21271=CARTESIAN_POINT ( 'NONE',  ( 11.10746886766490071, -4.498335456194499926, 8.405426684175299812 ) ) ;
#21292=UNCERTAINTY_MEASURE_WITH_UNIT (LENGTH_MEASURE( 1.000000000000000082E-05 ), #8573, 'distance_accuracy_value', 'NONE');
#21293=CARTESIAN_POINT ( 'NONE',  ( 10.14393020684900115, -2.750000000000000000, 7.500000000000000000 ) ) ;
#21312=CARTESIAN_POINT ( 'NONE',  ( 11.14949279009019989, -4.260984538213099526, 6.531063508962500208 ) ) ;
#21318=CARTESIAN_POINT ( 'NONE',  ( 11.68412378248529926, -4.549028353065900809, 8.538714411016998795 ) ) ;
#21355=CARTESIAN_POINT ( 'NONE',  ( 11.76487482311540056, -3.069598554678400149, 7.124095752359899336 ) ) ;
#21387=CARTESIAN_POINT ( 'NONE',  ( 9.643927823787143083, -2.750011555256801188, 7.500000155056757656 ) ) ;
#21395=ADVANCED_FACE ( 'NONE', ( #60056 ), #11806, .F. ) ;
#21398=CARTESIAN_POINT ( 'NONE',  ( 11.81825954179440075, -3.333768806796900019, 6.946434658287599540 ) ) ;
#21426=CONICAL_SURFACE ( 'NONE', #28134, 0.9999998338055000602, 0.7853981908209605178 ) ;
#21443=CARTESIAN_POINT ( 'NONE',  ( 10.43363399569799910, -3.001718438313799808, 7.389201877599999690 ) ) ;
#21462=CARTESIAN_POINT ( 'NONE',  ( 11.41991225946277666, -3.299232917623651229, 8.022508467459166681 ) ) ;
#21478=ORIENTED_EDGE ( 'NONE', *, *, #36053, .F. ) ;
#21490=DIRECTION ( 'NONE',  ( 0.000000000000000000, 1.000000000000000000, 0.000000000000000000 ) ) ;
#21526=CARTESIAN_POINT ( 'NONE',  ( 11.11656919669529842, -2.774362666861999838, 7.137881914002699446 ) ) ;
#21572=CARTESIAN_POINT ( 'NONE',  ( 10.59964828895399869, -2.878385131502000149, 6.887384543790600056 ) ) ;
#21610=CARTESIAN_POINT ( 'NONE',  ( 11.98522412107029922, -3.952868550833580130, 8.390877922225699947 ) ) ;
#21647=CARTESIAN_POINT ( 'NONE',  ( 11.90841235500450068, -4.841138636481000290, 8.270568563129298667 ) ) ;
#21650=ORIENTED_EDGE ( 'NONE', *, *, #48870, .T. ) ;
#21655=CARTESIAN_POINT ( 'NONE',  ( 11.72567835872029995, -4.993948309075300074, 8.126439557340900066 ) ) ;
#21692=CARTESIAN_POINT ( 'NONE',  ( 12.27359063708300013, -3.044227915785300276, 7.231278212164300001 ) ) ;
#21719=VECTOR ( 'NONE', #59871, 1000.000000000000114 ) ;
#21738=CARTESIAN_POINT ( 'NONE',  ( 12.27359063708300013, -3.044227915785300276, 7.231278212164300001 ) ) ;
#21749=CARTESIAN_POINT ( 'NONE',  ( 9.582867883171827472, -3.217326796159980518, 6.525013452213887177 ) ) ;
#21787=CARTESIAN_POINT ( 'NONE',  ( 10.81155864497999808, -3.317414799430800088, 6.965412239408199646 ) ) ;
#21796=FACE_OUTER_BOUND ( 'NONE', #53791, .T. ) ;
#21835=ORIENTED_EDGE ( 'NONE', *, *, #31210, .F. ) ;
#21849=CARTESIAN_POINT ( 'NONE',  ( 9.237760194560388882, -4.066145789045416237, 6.629534018758292291 ) ) ;
#21866=CARTESIAN_POINT ( 'NONE',  ( 11.75656651104150008, -3.873914634362100262, 8.771777834828998976 ) ) ;
#21900=CARTESIAN_POINT ( 'NONE',  ( 9.193455549952998851, -3.004437130344999929, 8.303267676773000261 ) ) ;
#21916=CARTESIAN_POINT ( 'NONE',  ( 11.51041369783139956, -4.064477673403060543, 6.223614866029000048 ) ) ;
#21925=VERTEX_POINT ( 'NONE', #3555 ) ;
#21951=CARTESIAN_POINT ( 'NONE',  ( 11.02435971519499880, -3.467537960339900138, 8.385788382729799650 ) ) ;
#21991=CARTESIAN_POINT ( 'NONE',  ( 10.73103300763300005, -3.307558760216100069, 6.773725604892799623 ) ) ;
#21999=CARTESIAN_POINT ( 'NONE',  ( 11.80367835872029936, -5.113555564477999305, 8.201822467543799178 ) ) ;
#22028=CARTESIAN_POINT ( 'NONE',  ( 10.15749563395762678, -4.774169056067385952, 7.092330352431370777 ) ) ;
#22066=CARTESIAN_POINT ( 'NONE',  ( 11.23724174883999893, -4.024531238983009906, 6.608211443991299561 ) ) ;
#22068=CARTESIAN_POINT ( 'NONE',  ( 9.620327454391748745, -2.808826379911543825, 7.911210609455967102 ) ) ;
#22073=CARTESIAN_POINT ( 'NONE',  ( 10.81021345716900051, -3.363461959113699606, 6.921280946186199934 ) ) ;
#22084=CARTESIAN_POINT ( 'NONE',  ( 11.44487616594229884, -4.303437140848100029, 8.456491899811199531 ) ) ;
#22128=FACE_OUTER_BOUND ( 'NONE', #14874, .T. ) ;
#22136=CARTESIAN_POINT ( 'NONE',  ( 10.73557120343299864, -4.042028078047379402, 6.634008278083699750 ) ) ;
#22151=CARTESIAN_POINT ( 'NONE',  ( 10.92760663304248325, -3.352948950021445995, 8.087719785218890678 ) ) ;
#22165=CARTESIAN_POINT ( 'NONE',  ( 10.55226354018249957, -2.907767014557177898, 6.870476274536374994 ) ) ;
#22221=CARTESIAN_POINT ( 'NONE',  ( 9.855088727410999283, -5.274736981944999847, 7.393088754863899936 ) ) ;
#22252=CARTESIAN_POINT ( 'NONE',  ( 9.700038493598999167, -3.074215132699300135, 8.382783533462799141 ) ) ;
#22271=CARTESIAN_POINT ( 'NONE',  ( 9.854346873516666605, -5.250000000000000000, 7.336375382625534236 ) ) ;
#22300=CARTESIAN_POINT ( 'NONE',  ( 10.85814141025499957, -3.516507310755200066, 6.638851159159999682 ) ) ;
#22340=CARTESIAN_POINT ( 'NONE',  ( 11.17410807141120088, -3.953638752893899877, 6.497602131078999754 ) ) ;
#22349=CARTESIAN_POINT ( 'NONE',  ( 11.88678751119029897, -5.166297436425000278, 6.889827023674499173 ) ) ;
#22419=CARTESIAN_POINT ( 'NONE',  ( 9.883499245234512287, -5.249996043174972371, 7.663630899194568080 ) ) ;
#22479=CARTESIAN_POINT ( 'NONE',  ( 10.27964655415099848, -3.580250267348600079, 6.741370903243699253 ) ) ;
#22481=CARTESIAN_POINT ( 'NONE',  ( 11.24809687351632448, -3.672815144550895194, 8.717465845835393523 ) ) ;
#22515=ADVANCED_FACE ( 'NONE', ( #36242 ), #27835, .T. ) ;
#22558=EDGE_CURVE ( 'NONE', #11948, #51764, #33562, .T. ) ;
#22563=CARTESIAN_POINT ( 'NONE',  ( 10.81759632033899976, -5.184381781355999586, 7.983346856269500691 ) ) ;
#22627=ORIENTED_EDGE ( 'NONE', *, *, #33224, .F. ) ;
#22663=CARTESIAN_POINT ( 'NONE',  ( 9.226787239609999247, -4.219532685969900498, 6.659501631675699862 ) ) ;
#22681=CARTESIAN_POINT ( 'NONE',  ( 10.30995058442699985, -3.546800160410199965, 8.548019252390998801 ) ) ;
#22684=CARTESIAN_POINT ( 'NONE',  ( 11.78118179236250107, -4.267047616085000605, 8.749800764654999341 ) ) ;
#22692=CARTESIAN_POINT ( 'NONE',  ( 11.27879632507499963, -3.576455950783300253, 6.714825466131699727 ) ) ;
#22720=CARTESIAN_POINT ( 'NONE',  ( 10.18282478114062606, -4.607703288839251954, 6.870532779523098377 ) ) ;
#22753=CARTESIAN_POINT ( 'NONE',  ( 11.01927318630899855, -3.243547362524661359, 6.473854711408037588 ) ) ;
#22773=ORIENTED_EDGE ( 'NONE', *, *, #47710, .T. ) ;
#22823=DIRECTION ( 'NONE',  ( -1.000000000000000000, 0.000000000000000000, 1.554312234491000161E-14 ) ) ;
#22826=CARTESIAN_POINT ( 'NONE',  ( 9.950367640780999778, -3.591293244209800228, 8.264635032075899446 ) ) ;
#22874=CARTESIAN_POINT ( 'NONE',  ( 10.18559687351566723, -2.907767014557174790, 8.129523725463618788 ) ) ;
#22881=DIRECTION ( 'NONE',  ( 1.000000000000000000, 0.000000000000000000, 0.000000000000000000 ) ) ;
#22911=CARTESIAN_POINT ( 'NONE',  ( 12.10000000000000320, -4.874497702741446226, 7.130791426018634027 ) ) ;
#22927=VECTOR ( 'NONE', #33946, 1000.000000000000000 ) ;
#22952=CARTESIAN_POINT ( 'NONE',  ( 10.13559687351666483, -2.907767014557175678, 8.129523725463618788 ) ) ;
#22988=CARTESIAN_POINT ( 'NONE',  ( 11.00180110216400031, -4.856393875115199599, 8.023010882787499298 ) ) ;
#23029=CARTESIAN_POINT ( 'NONE',  ( 10.25929229006299970, -3.012566816337000297, 8.073332500201798823 ) ) ;
#23032=CARTESIAN_POINT ( 'NONE',  ( 10.87457053952200070, -4.448306506338299826, 8.548957288282998945 ) ) ;
#23034=CARTESIAN_POINT ( 'NONE',  ( 10.13351354018233330, -2.750000000000000000, 7.336375382625529795 ) ) ;
#23040=CARTESIAN_POINT ( 'NONE',  ( 10.94125056272499918, -2.966599088466999934, 7.484684486284700178 ) ) ;
#23071=CARTESIAN_POINT ( 'NONE',  ( 9.828216720588628164, -3.237060173287368503, 7.071683423462644669 ) ) ;
#23092=CARTESIAN_POINT ( 'NONE',  ( 10.64124205625000030, -4.360201998293100623, 6.562398383267799673 ) ) ;
#23101=CARTESIAN_POINT ( 'NONE',  ( 10.97145237372900084, -3.956267952212243255, 6.225919055146349912 ) ) ;
#23137=CARTESIAN_POINT ( 'NONE',  ( 10.71684687351595855, -3.231816600031351516, 8.499583552997721725 ) ) ;
#23172=CARTESIAN_POINT ( 'NONE',  ( 11.62299956498149989, -2.792989229543000107, 7.174999999999999822 ) ) ;
#23175=CARTESIAN_POINT ( 'NONE',  ( 10.71024205624999937, -4.310927436352299580, 6.690659495528099576 ) ) ;
#23197=CARTESIAN_POINT ( 'NONE',  ( 12.18748876160954886, -4.600381688599499697, 6.875627981711399883 ) ) ;
#23264=CARTESIAN_POINT ( 'NONE',  ( 9.677784697135001224, -3.305825103746500293, 8.574479223074998657 ) ) ;
#23283=VECTOR ( 'NONE', #14169, 1000.000000000000000 ) ;
#23340=CARTESIAN_POINT ( 'NONE',  ( 12.06025819896753859, -4.986099335708799707, 7.314099615601099558 ) ) ;
#23380=CARTESIAN_POINT ( 'NONE',  ( 9.854025935145999782, -4.165792341207500193, 8.629711178834000407 ) ) ;
#23383=CARTESIAN_POINT ( 'NONE',  ( 11.65810538575740019, -2.757018958839999812, 7.797177576385699638 ) ) ;
#23392=CARTESIAN_POINT ( 'NONE',  ( 10.75564828895399927, -3.119330945648699949, 7.018986873610899124 ) ) ;
#23393=CARTESIAN_POINT ( 'NONE',  ( 10.98280513895999988, -3.096689368913399854, 8.002155910165599906 ) ) ;
#23424=CARTESIAN_POINT ( 'NONE',  ( 9.802887573405627109, -3.409423315843189251, 6.854437106819677439 ) ) ;
#23444=CARTESIAN_POINT ( 'NONE',  ( 9.957355082328000151, -4.449513475323099598, 8.398209294002699110 ) ) ;
#23457=ORIENTED_EDGE ( 'NONE', *, *, #27193, .T. ) ;
#23470=DIRECTION ( 'NONE',  ( 0.000000000000000000, 1.000000000000000000, 0.000000000000000000 ) ) ;
#23502=ORIENTED_EDGE ( 'NONE', *, *, #39621, .F. ) ;
#23589=CARTESIAN_POINT ( 'NONE',  ( 11.23976354018279977, -4.327184855449098144, 8.717465845835395299 ) ) ;
#23602=CARTESIAN_POINT ( 'NONE',  ( 11.53111947020579819, -4.908799224006100026, 7.825000000000000178 ) ) ;
#23603=CARTESIAN_POINT ( 'NONE',  ( 10.64029229006299992, -2.893743561734000380, 8.142324746736500529 ) ) ;
#23614=CARTESIAN_POINT ( 'NONE',  ( 11.80565467195988916, -5.136173005413446013, 8.088082908809447247 ) ) ;
#23621=SURFACE_STYLE_USAGE ( .BOTH. , #66951 ) ;
#23681=CARTESIAN_POINT ( 'NONE',  ( 10.85826357027499967, -3.149486845331399998, 7.335909308151700614 ) ) ;
#23720=CARTESIAN_POINT ( 'NONE',  ( 9.155265421555000671, -4.188500707411799695, 6.524915741324599949 ) ) ;
#23724=CARTESIAN_POINT ( 'NONE',  ( 11.31764560330029923, -3.650429500487800460, 8.585859374935999710 ) ) ;
#23726=CARTESIAN_POINT ( 'NONE',  ( 9.231616107288068918, -3.999997736744774546, 6.618420992905502231 ) ) ;
#23733=CARTESIAN_POINT ( 'NONE',  ( 11.66641369783139837, -4.050626550392200542, 6.497808498716000081 ) ) ;
#23734=CARTESIAN_POINT ( 'NONE',  ( 11.35679632507500081, -3.509334349252600127, 6.590394082213600235 ) ) ;
#23779=ORIENTED_EDGE ( 'NONE', *, *, #40188, .T. ) ;
#23785=CARTESIAN_POINT ( 'NONE',  ( 10.23597570133300039, -3.263119632394099856, 6.817468224793199916 ) ) ;
#23792=CARTESIAN_POINT ( 'NONE',  ( 12.09999999999999964, -2.792989229543000107, 7.174999999999999822 ) ) ;
#23838=ORIENTED_EDGE ( 'NONE', *, *, #42713, .F. ) ;
#23867=CARTESIAN_POINT ( 'NONE',  ( 9.266480666858999626, -3.710922827228400056, 6.682599852064000423 ) ) ;
#23912=CARTESIAN_POINT ( 'NONE',  ( 10.39393020684899938, -5.250000000000000000, 7.500000000000000000 ) ) ;
#23939=CARTESIAN_POINT ( 'NONE',  ( 11.32309687351640193, -5.217465845835395299, 7.827184855449101697 ) ) ;
#23953=CARTESIAN_POINT ( 'NONE',  ( 10.66360887879199915, -4.258572737033900601, 8.612148635591999835 ) ) ;
#23970=B_SPLINE_SURFACE_WITH_KNOTS ( 'NONE', 3, 3, ( 
 ( #28435, #45552, #67884, #9495 ),
 ( #2886, #29826, #61964, #56726 ),
 ( #40981, #57057, #3234, #57390 ),
 ( #19661, #24209, #62970, #41327 ) ),
 .UNSPECIFIED., .F., .F., .F.,
 ( 4, 4 ),
 ( 4, 4 ),
 ( 0.7363163806532000422, 1.013499456067999960 ),
 ( -0.0005287450254680999126, 0.02696599629895000266 ),
 .UNSPECIFIED. ) ;
#24027=CARTESIAN_POINT ( 'NONE',  ( 10.73103300763300005, -3.307558760216100069, 6.773725604892799623 ) ) ;
#24066=CARTESIAN_POINT ( 'NONE',  ( 9.501430433047000079, -4.854750075120300323, 8.027488966151301142 ) ) ;
#24069=CARTESIAN_POINT ( 'NONE',  ( 12.12579573085663043, -2.760622544769000264, 7.285547569258399747 ) ) ;
#24078=CARTESIAN_POINT ( 'NONE',  ( 11.34641504065830020, -3.195537720350400068, 8.099826052678000821 ) ) ;
#24079=CARTESIAN_POINT ( 'NONE',  ( 11.90211496860029960, -3.206052520092899982, 7.906860999147899527 ) ) ;
#24109=FACE_OUTER_BOUND ( 'NONE', #56796, .T. ) ;
#24110=CARTESIAN_POINT ( 'NONE',  ( 9.422950365671626471, -3.319061674888539315, 8.049413566043876145 ) ) ;
#24115=CARTESIAN_POINT ( 'NONE',  ( 12.13611496860034933, -2.828587461987000395, 8.100294210499798808 ) ) ;
#24129=CARTESIAN_POINT ( 'NONE',  ( 9.731405316140000039, -4.184077495686000958, 6.652755395362000002 ) ) ;
#24136=CARTESIAN_POINT ( 'NONE',  ( 9.363694533038728451, -3.488685518255361551, 8.385421723231827329 ) ) ;
#24164=AXIS2_PLACEMENT_3D ( 'NONE', #10657, #9621, #21490 ) ;
#24209=CARTESIAN_POINT ( 'NONE',  ( 9.234997988989999129, -4.062652182992059657, 6.633566614602599998 ) ) ;
#24249=CARTESIAN_POINT ( 'NONE',  ( 10.21265911260399939, -4.376739491155700712, 6.719118894894999805 ) ) ;
#24258=CARTESIAN_POINT ( 'NONE',  ( 10.76059687351566652, -4.629523725463621453, 8.592232985442825210 ) ) ;
#24287=VERTEX_POINT ( 'NONE', #61944 ) ;
#24294=CARTESIAN_POINT ( 'NONE',  ( 9.601797255588000013, -2.721932483203000075, 7.554109351283189611 ) ) ;
#24319=PLANE ( 'NONE',  #63283 ) ;
#24341=CARTESIAN_POINT ( 'NONE',  ( 10.26059687351666661, -4.629523725463621453, 8.592232985442825210 ) ) ;
#24373=CARTESIAN_POINT ( 'NONE',  ( 10.97303166480599934, -5.137916160623999140, 7.419769534118209720 ) ) ;
#24413=CARTESIAN_POINT ( 'NONE',  ( 9.752709346416999381, -2.968569381205999669, 7.989780896525600085 ) ) ;
#24417=CARTESIAN_POINT ( 'NONE',  ( 10.55041772631200026, -3.450375740502100275, 6.368647051112000135 ) ) ;
#24429=CARTESIAN_POINT ( 'NONE',  ( 11.19872335273220010, -3.650693637952500126, 6.559289673553299060 ) ) ;
#24435=VERTEX_POINT ( 'NONE', #67777 ) ;
#24464=CARTESIAN_POINT ( 'NONE',  ( 11.72056920625029974, -3.952687217764870198, 8.815417147437999645 ) ) ;
#24479=CARTESIAN_POINT ( 'NONE',  ( 9.275480666858999967, -3.710922827228400056, 6.682599852064000423 ) ) ;
#24531=( NAMED_UNIT ( * ) SI_UNIT ( $, .STERADIAN. ) SOLID_ANGLE_UNIT ( ) );
#24560=CARTESIAN_POINT ( 'NONE',  ( 9.291809814040998816, -3.469640109842400122, 6.814123855771700100 ) ) ;
#24576=CARTESIAN_POINT ( 'NONE',  ( 11.81389666366019853, -4.045876550911099656, 6.467512203247999913 ) ) ;
#24598=ORIENTED_EDGE ( 'NONE', *, *, #61441, .T. ) ;
#24599=CARTESIAN_POINT ( 'NONE',  ( 10.69391290906799874, -4.548591194283900130, 6.828616613600999585 ) ) ;
#24643=CARTESIAN_POINT ( 'NONE',  ( 10.51163399569799850, -2.865156490077000129, 7.374045024026299799 ) ) ;
#24716=CARTESIAN_POINT ( 'NONE',  ( 10.89918582084299992, -4.746348444722899629, 8.362701637490498996 ) ) ;
#24754=CARTESIAN_POINT ( 'NONE',  ( 10.23195058442700045, -3.492264136285500253, 8.674133161175999973 ) ) ;
#24757=CARTESIAN_POINT ( 'NONE',  ( 10.99349279008999858, -4.332388355267299929, 6.265968249244999733 ) ) ;
#24763=B_SPLINE_CURVE_WITH_KNOTS ( 'NONE', 3,
 ( #19047, #2625, #57136, #35485 ),
 .UNSPECIFIED., .F., .F.,
 ( 4, 4 ),
 ( 0.000000000000000000, 1.000000000000000000 ),
 .UNSPECIFIED. ) ;
#24765=CARTESIAN_POINT ( 'NONE',  ( 11.76212378248530044, -4.615095948180499619, 8.663708617168998316 ) ) ;
#24767=CARTESIAN_POINT ( 'NONE',  ( 11.78533594839949927, -3.249987070165300196, 8.359517726022600570 ) ) ;
#24806=CARTESIAN_POINT ( 'NONE',  ( 10.93614141025500075, -3.450366949021700158, 6.521048559232099251 ) ) ;
#24844=CARTESIAN_POINT ( 'NONE',  ( 12.15871932425157098, -4.147141405561299621, 6.507377093516500288 ) ) ;
#24887=CARTESIAN_POINT ( 'NONE',  ( 11.03057053952199951, -4.340412141385700195, 8.296503712697200328 ) ) ;
#24914=CARTESIAN_POINT ( 'NONE',  ( 12.18788784977535933, -4.985985832792199979, 7.556342205905759890 ) ) ;
#24936=CARTESIAN_POINT ( 'NONE',  ( 10.31397570133299979, -3.363922674822000136, 6.910836541441499392 ) ) ;
#24978=CARTESIAN_POINT ( 'NONE',  ( 10.00505105205199818, -2.879444846832000415, 7.280704316743199733 ) ) ;
#25055=CARTESIAN_POINT ( 'NONE',  ( 11.53918313518939875, -4.707599264529200411, 6.605241151424599444 ) ) ;
#25094=CARTESIAN_POINT ( 'NONE',  ( 9.246126402770999064, -2.931626221533000010, 7.902879529556599891 ) ) ;
#25097=CARTESIAN_POINT ( 'NONE',  ( 10.72272469555899832, -3.360453478306600239, 8.606479382885998675 ) ) ;
#25106=CARTESIAN_POINT ( 'NONE',  ( 11.12072335273220069, -3.602909566644000083, 6.430603299050000388 ) ) ;
#25112=DIRECTION ( 'NONE',  ( 0.7071067486699967874, -0.7071068137030968037, 9.022793105466955192E-11 ) ) ;
#25138=CARTESIAN_POINT ( 'NONE',  ( 9.296304629759626792, -3.464785522094639969, 6.807845768027799060 ) ) ;
#25143=CARTESIAN_POINT ( 'NONE',  ( 12.05811496860034993, -2.954409148022000053, 8.035816473382100256 ) ) ;
#25182=CARTESIAN_POINT ( 'NONE',  ( 12.18333460557258974, -3.837988184179999873, 6.509695444280099608 ) ) ;
#25227=CARTESIAN_POINT ( 'NONE',  ( 12.16287348028854964, -4.761955701524100526, 7.088026579158399620 ) ) ;
#25242=ORIENTED_EDGE ( 'NONE', *, *, #66522, .F. ) ;
#25258=CARTESIAN_POINT ( 'NONE',  ( 10.87199293566600034, -3.366612813978900220, 6.723009541442299231 ) ) ;
#25282=CARTESIAN_POINT ( 'NONE',  ( 10.08601337669299980, -4.772923352651200268, 7.892807122431200639 ) ) ;
#25320=CARTESIAN_POINT ( 'NONE',  ( 10.05369678796300015, -3.827518619249500098, 8.489491017455099708 ) ) ;
#25396=CARTESIAN_POINT ( 'NONE',  ( 11.44072200990529886, -5.077092948368999714, 7.875713849677398848 ) ) ;
#25431=EDGE_LOOP ( 'NONE', ( #13090, #44588, #35835, #62768, #63706 ) ) ;
#25435=CARTESIAN_POINT ( 'NONE',  ( 10.40925461470300029, -5.239722547583999912, 7.184607557167700165 ) ) ;
#25438=CARTESIAN_POINT ( 'NONE',  ( 11.06733863405299800, -3.211524470605299886, 6.494205428462000107 ) ) ;
#25446=CARTESIAN_POINT ( 'NONE',  ( 11.84523293495530005, -5.315205473512000012, 7.552870914315270134 ) ) ;
#25449=CARTESIAN_POINT ( 'NONE',  ( 11.68687482311540116, -2.942322404451000128, 7.072673169413499217 ) ) ;
#25490=CARTESIAN_POINT ( 'NONE',  ( 11.76212378248530044, -4.615095948180499619, 8.663708617168998316 ) ) ;
#25509=AXIS2_PLACEMENT_3D ( 'NONE', #49212, #2017, #6560 ) ;
#25530=CARTESIAN_POINT ( 'NONE',  ( 12.03564291764652872, -4.995889373412399692, 7.623106493640399606 ) ) ;
#25578=CARTESIAN_POINT ( 'NONE',  ( 11.81825954179440075, -3.333768806796900019, 6.946434658287599540 ) ) ;
#25607=CARTESIAN_POINT ( 'NONE',  ( 11.26857802013510046, -5.174568897094999897, 7.527343341769989316 ) ) ;
#25612=CARTESIAN_POINT ( 'NONE',  ( 11.60328610135030125, -4.878060775730400422, 7.174999999999999822 ) ) ;
#25622=CARTESIAN_POINT ( 'NONE',  ( 11.37518447801629939, -3.134012688501500055, 7.519093628927509876 ) ) ;
#25627=FACE_OUTER_BOUND ( 'NONE', #37618, .T. ) ;
#25665=CARTESIAN_POINT ( 'NONE',  ( 10.15501337669299886, -4.895413217368500547, 7.955057656228099461 ) ) ;
#25714=CARTESIAN_POINT ( 'NONE',  ( 9.429547492598359781, -3.266100554355691354, 6.695580748437408580 ) ) ;
#25746=CARTESIAN_POINT ( 'NONE',  ( 11.28887616594230003, -4.386455737425299262, 8.718182393403999697 ) ) ;
#25770=ORIENTED_EDGE ( 'NONE', *, *, #16901, .F. ) ;
#25781=CARTESIAN_POINT ( 'NONE',  ( 9.928000818239000935, -5.131870447930000800, 6.903968392969799694 ) ) ;
#25784=CARTESIAN_POINT ( 'NONE',  ( 10.96887750876899936, -4.692271380433699512, 6.425720373262999274 ) ) ;
#25794=CARTESIAN_POINT ( 'NONE',  ( 11.63746005378019888, -2.838900981960999825, 8.120007936598501175 ) ) ;
#25796=CARTESIAN_POINT ( 'NONE',  ( 11.97810404293059960, -4.563346034752700398, 6.352848032645000309 ) ) ;
#25797=CARTESIAN_POINT ( 'NONE',  ( 10.79399293566600093, -3.453258297007899991, 6.829299525004299376 ) ) ;
#25831=CARTESIAN_POINT ( 'NONE',  ( 11.84523293495530005, -5.315205473512000012, 7.552870914315270134 ) ) ;
#25869=CARTESIAN_POINT ( 'NONE',  ( 11.91256651104150066, -3.901000349726440053, 8.498573944230598087 ) ) ;
#25916=CARTESIAN_POINT ( 'NONE',  ( 12.26133460557259980, -3.860150918677800025, 6.645166161828299778 ) ) ;
#25947=CARTESIAN_POINT ( 'NONE',  ( 11.31524174883999834, -4.028418853626810403, 6.466884287543999577 ) ) ;
#25966=CARTESIAN_POINT ( 'NONE',  ( 11.20287750876920008, -4.469200303112399908, 6.771886227364699806 ) ) ;
#25986=ORIENTED_EDGE ( 'NONE', *, *, #39392, .F. ) ;
#26008=B_SPLINE_CURVE_WITH_KNOTS ( 'NONE', 3,
 ( #56983, #30425, #41937, #15023 ),
 .UNSPECIFIED., .F., .F.,
 ( 4, 4 ),
 ( 0.000000000000000000, 1.000000000000000000 ),
 .UNSPECIFIED. ) ;
#26012=CARTESIAN_POINT ( 'NONE',  ( 10.10435508232799862, -4.449513475323099598, 8.398209294002699110 ) ) ;
#26027=CARTESIAN_POINT ( 'NONE',  ( 10.91476354018331030, -5.217465845835395299, 7.172815144550902744 ) ) ;
#26028=CARTESIAN_POINT ( 'NONE',  ( 11.07529832096848210, -4.746004694577873551, 7.955594773867785463 ) ) ;
#26079=VERTEX_POINT ( 'NONE', #50466 ) ;
#26093=CARTESIAN_POINT ( 'NONE',  ( 11.68272066707849888, -2.906477115133000222, 8.161456030935699602 ) ) ;
#26122=EDGE_LOOP ( 'NONE', ( #22627, #58314, #44970, #34136 ) ) ;
#26134=CARTESIAN_POINT ( 'NONE',  ( 10.03976354018233330, -3.672815144550900524, 6.282534154164603812 ) ) ;
#26143=CARTESIAN_POINT ( 'NONE',  ( 11.39324174884020024, -4.032306468273969990, 6.325557131097000685 ) ) ;
#26145=CARTESIAN_POINT ( 'NONE',  ( 10.92380110216399913, -4.973546009874400653, 8.094557215852098864 ) ) ;
#26176=ORIENTED_EDGE ( 'NONE', *, *, #15474, .F. ) ;
#26180=CARTESIAN_POINT ( 'NONE',  ( 11.77745123989519982, -3.589787500396900199, 6.707778874960499849 ) ) ;
#26223=CARTESIAN_POINT ( 'NONE',  ( 11.71564426047340035, -3.460037133261700149, 6.654192128557399499 ) ) ;
#26230=CARTESIAN_POINT ( 'NONE',  ( 11.64256920625030034, -3.957769094421040190, 8.674127893687000324 ) ) ;
#26265=CARTESIAN_POINT ( 'NONE',  ( 11.44903032197930060, -3.496160833528699996, 8.204588308639600314 ) ) ;
#26307=CARTESIAN_POINT ( 'NONE',  ( 11.55391045180431675, -2.870950512581995628, 6.885461205208883051 ) ) ;
#26312=CARTESIAN_POINT ( 'NONE',  ( 12.08487348028855024, -4.882707455860599843, 7.022738645480499642 ) ) ;
#26361=CARTESIAN_POINT ( 'NONE',  ( 10.56027973160900046, -3.909869487835140323, 8.500359330993999762 ) ) ;
#26372=EDGE_CURVE ( 'NONE', #50813, #54112, #59128, .T. ) ;
#26377=CARTESIAN_POINT ( 'NONE',  ( 11.00851354018319483, -4.163624617374471093, 6.250000000000000888 ) ) ;
#26378=CARTESIAN_POINT ( 'NONE',  ( 11.12452888361057113, -4.871957554394390044, 7.438521339935803667 ) ) ;
#26399=CARTESIAN_POINT ( 'NONE',  ( 10.84393020684900044, -5.250000000000000000, 7.500000000000000000 ) ) ;
#26440=CARTESIAN_POINT ( 'NONE',  ( 10.75149413291699929, -2.962184842772000337, 7.973529073237199505 ) ) ;
#26475=CARTESIAN_POINT ( 'NONE',  ( 9.573392757686999488, -3.136549968260000210, 6.556157624301499176 ) ) ;
#26490=CARTESIAN_POINT ( 'NONE',  ( 11.23964560330029983, -3.608363763633400279, 8.716526793355999558 ) ) ;
#26527=CARTESIAN_POINT ( 'NONE',  ( 10.90480513896000048, -3.220259576336399920, 7.933462475324499330 ) ) ;
#26569=CARTESIAN_POINT ( 'NONE',  ( 11.93302763632549990, -5.035790660926999784, 7.977941233841399971 ) ) ;
#26579=CARTESIAN_POINT ( 'NONE',  ( 12.26588784977539959, -5.120865761890000201, 7.564049652083489228 ) ) ;
#26598=ORIENTED_EDGE ( 'NONE', *, *, #58310, .T. ) ;
#26615=CARTESIAN_POINT ( 'NONE',  ( 12.20794988689359961, -3.544213289744700290, 6.606015074393400077 ) ) ;
#26663=CARTESIAN_POINT ( 'NONE',  ( 10.95672469555900008, -3.566534988568399900, 8.249937779480299938 ) ) ;
#26709=CARTESIAN_POINT ( 'NONE',  ( 10.66159632033899918, -4.929952350555500296, 7.879514065647800436 ) ) ;
#26726=CARTESIAN_POINT ( 'NONE',  ( 11.34606641549977724, -3.161700962939955506, 7.252322131039115050 ) ) ;
#26740=CARTESIAN_POINT ( 'NONE',  ( 10.39601354018312662, -4.999583552997726166, 6.731816600031358178 ) ) ;
#26790=CARTESIAN_POINT ( 'NONE',  ( 11.73195122972050086, -3.492749840905900349, 8.673036084990000560 ) ) ;
#26823=CARTESIAN_POINT ( 'NONE',  ( 8.990822372493999737, -4.367693913457399546, 6.297150255604999636 ) ) ;
#26835=CARTESIAN_POINT ( 'NONE',  ( 10.20851354018333623, -3.836375382625528019, 8.749999999999996447 ) ) ;
#26838=CARTESIAN_POINT ( 'NONE',  ( 10.77195525820100031, -4.120672149427799802, 8.772302877803999976 ) ) ;
#26845=CARTESIAN_POINT ( 'NONE',  ( 10.07309687351667016, -2.782534154164605589, 7.172815144550900968 ) ) ;
#26873=CARTESIAN_POINT ( 'NONE',  ( 11.60612378248510090, -4.482960757953799558, 8.413720204863100349 ) ) ;
#26892=UNCERTAINTY_MEASURE_WITH_UNIT (LENGTH_MEASURE( 1.000000000000000082E-05 ), #36045, 'distance_accuracy_value', 'NONE');
#26912=CARTESIAN_POINT ( 'NONE',  ( 10.71462282008599942, -3.476853648246800432, 6.656181553372300108 ) ) ;
#26918=CARTESIAN_POINT ( 'NONE',  ( 11.22191429142990060, -3.974927396630719922, 8.816028813488999916 ) ) ;
#26956=CARTESIAN_POINT ( 'NONE',  ( 11.27256919669530077, -3.037654633983899899, 7.215672285280100517 ) ) ;
#26982=CARTESIAN_POINT ( 'NONE',  ( 10.89393020684999946, -5.250000000000000000, 7.500000000000000000 ) ) ;
#26985=CARTESIAN_POINT ( 'NONE',  ( 10.82169598649000086, -3.233475335853099875, 7.043598424555200133 ) ) ;
#27000=CARTESIAN_POINT ( 'NONE',  ( 11.32595391537419971, -3.283439621430300104, 7.013338090450799811 ) ) ;
#27019=VECTOR ( 'NONE', #36801, 1000.000000000000000 ) ;
#27036=VECTOR ( 'NONE', #19643, 1000.000000000000000 ) ;
#27050=CARTESIAN_POINT ( 'NONE',  ( 10.40629229006299816, -3.250213325543700016, 7.935348007132199122 ) ) ;
#27129=CARTESIAN_POINT ( 'NONE',  ( 11.95348876160960039, -4.885820101980599794, 6.578783887955899523 ) ) ;
#27136=CARTESIAN_POINT ( 'NONE',  ( 9.099999999999999645, -4.000000000000000000, 7.500000000000000000 ) ) ;
#27163=CARTESIAN_POINT ( 'NONE',  ( 8.999265421555000088, -4.240073379563900069, 6.258138488953999712 ) ) ;
#27177=CARTESIAN_POINT ( 'NONE',  ( 11.80579707368350029, -4.634832087857400751, 8.609190966793999422 ) ) ;
#27180=ORIENTED_EDGE ( 'NONE', *, *, #31210, .T. ) ;
#27193=EDGE_CURVE ( 'NONE', #67955, #41017, #44435, .T. ) ;
#27201=CARTESIAN_POINT ( 'NONE',  ( 12.09999999999999964, -2.935681553670999921, 6.844464917182299324 ) ) ;
#27211=CARTESIAN_POINT ( 'NONE',  ( 11.44501463001509833, -3.527519786474400121, 8.256737112932800216 ) ) ;
#27253=CARTESIAN_POINT ( 'NONE',  ( 12.08071932425156980, -4.167269912168199753, 6.371589232479998977 ) ) ;
#27259=CARTESIAN_POINT ( 'NONE',  ( 11.34657802013509986, -5.315911219205999849, 7.530633716161349689 ) ) ;
#27260=ORIENTED_EDGE ( 'NONE', *, *, #39025, .F. ) ;
#27291=CARTESIAN_POINT ( 'NONE',  ( 9.701570984676626708, -4.444002162597382011, 6.746080675052237297 ) ) ;
#27297=CARTESIAN_POINT ( 'NONE',  ( 9.236413463905998711, -3.915843685459630574, 6.617590440947399344 ) ) ;
#27332=CARTESIAN_POINT ( 'NONE',  ( 11.62299956498149989, -2.792989229543000107, 7.174999999999999822 ) ) ;
#27342=CARTESIAN_POINT ( 'NONE',  ( 11.02641638348499953, -4.974961480482700260, 7.737488872214999702 ) ) ;
#27353=CARTESIAN_POINT ( 'NONE',  ( 9.548601287889788125, -3.999999532294070459, 6.301404677806389465 ) ) ;
#27390=CARTESIAN_POINT ( 'NONE',  ( 9.849051052051999378, -3.149129950522900234, 7.333482423122699601 ) ) ;
#27407=CARTESIAN_POINT ( 'NONE',  ( 11.27222057153667656, -3.695719232113590547, 6.680547245655227506 ) ) ;
#27410=CARTESIAN_POINT ( 'NONE',  ( 12.31056516821460001, -3.390321848206700128, 6.884701936848800052 ) ) ;
#27420=CARTESIAN_POINT ( 'NONE',  ( 10.41684687351637528, -4.768183399968644487, 6.500416447002274722 ) ) ;
#27464=ORIENTED_EDGE ( 'NONE', *, *, #17345, .F. ) ;
#27474=CARTESIAN_POINT ( 'NONE',  ( 11.04555864497999984, -2.992894514506000192, 6.711254117843599154 ) ) ;
#27532=ADVANCED_FACE ( 'NONE', ( #37569 ), #10317, .T. ) ;
#27540=CARTESIAN_POINT ( 'NONE',  ( 9.469356963619999235, -5.119357025014000584, 7.500000000085178087 ) ) ;
#27553=CARTESIAN_POINT ( 'NONE',  ( 11.85545123989520100, -3.524778630617700248, 6.582230774881299595 ) ) ;
#27594=CARTESIAN_POINT ( 'NONE',  ( 12.03148876160955005, -4.790673964186999534, 6.677731919207799294 ) ) ;
#27600=CARTESIAN_POINT ( 'NONE',  ( 11.67901463001530082, -3.302889347096799710, 8.616511311517999872 ) ) ;
#27608=LINE ( 'NONE', #59075, #6714 ) ;
#27637=CARTESIAN_POINT ( 'NONE',  ( 9.954862456499625978, -3.587552194319129750, 8.271634030165902374 ) ) ;
#27681=CARTESIAN_POINT ( 'NONE',  ( 9.821001730958839104, -4.768205771526717207, 8.499596153627864581 ) ) ;
#27693=CARTESIAN_POINT ( 'NONE',  ( 12.19559063708295987, -2.913481137622000006, 7.194517870904999945 ) ) ;
#27745=CARTESIAN_POINT ( 'NONE',  ( 10.60892546752099896, -4.864937374655599278, 7.559927309296559983 ) ) ;
#27765=CARTESIAN_POINT ( 'NONE',  ( 12.35979573085659844, -3.159987984332300215, 7.354650721737899133 ) ) ;
#27817=CARTESIAN_POINT ( 'NONE',  ( 11.29184687351630423, -4.999583552997724389, 8.268183399968647151 ) ) ;
#27832=CARTESIAN_POINT ( 'NONE',  ( 9.728442991499999692, -4.080527519162810535, 8.776675254768999679 ) ) ;
#27835=PLANE ( 'NONE',  #14600 ) ;
#27862=ORIENTED_EDGE ( 'NONE', *, *, #3554, .F. ) ;
#27863=CARTESIAN_POINT ( 'NONE',  ( 10.34393020685000053, -5.250000000000000000, 7.500000000000000000 ) ) ;
#27880=CARTESIAN_POINT ( 'NONE',  ( 9.958513540183334456, -4.163624617374470205, 6.250000000000000000 ) ) ;
#27905=DIRECTION ( 'NONE',  ( 0.000000000000000000, 0.000000000000000000, 1.000000000000000000 ) ) ;
#27926=CARTESIAN_POINT ( 'NONE',  ( 9.255358248830999557, -3.910012670022149806, 6.649720865199900466 ) ) ;
#27946=CARTESIAN_POINT ( 'NONE',  ( 10.67764828895399987, -2.998858038575999974, 6.953185708700699408 ) ) ;
#27953=CARTESIAN_POINT ( 'NONE',  ( 12.10988784977536525, -4.851105903694400645, 7.548634759728509280 ) ) ;
#27959=ORIENTED_EDGE ( 'NONE', *, *, #15309, .T. ) ;
#27984=CARTESIAN_POINT ( 'NONE',  ( 10.66407857760462541, -4.737836169116369511, 7.029755324101339298 ) ) ;
#28083=CARTESIAN_POINT ( 'NONE',  ( 9.369809814040999996, -3.385590752329799891, 6.705428891605899722 ) ) ;
#28101=CARTESIAN_POINT ( 'NONE',  ( 10.42581074856899725, -5.172583146916751140, 6.999756549658379789 ) ) ;
#28134=AXIS2_PLACEMENT_3D ( 'NONE', #63740, #64417, #53259 ) ;
#28137=VERTEX_POINT ( 'NONE', #42576 ) ;
#28147=ORIENTED_EDGE ( 'NONE', *, *, #49221, .F. ) ;
#28160=CARTESIAN_POINT ( 'NONE',  ( 10.74733997688000109, -3.727636250918499705, 8.748653021963999521 ) ) ;
#28165=CARTESIAN_POINT ( 'NONE',  ( 9.880417874594000338, -5.177249570814000279, 6.999532383170999239 ) ) ;
#28169=CARTESIAN_POINT ( 'NONE',  ( 12.09999999999999964, -3.890364666909557734, 6.362414725044391872 ) ) ;
#28179=EDGE_CURVE ( 'NONE', #11948, #61432, #10067, .T. ) ;
#28242=CARTESIAN_POINT ( 'NONE',  ( 11.07564694612699974, -4.931992688388300294, 7.128058497017000228 ) ) ;
#28266=CARTESIAN_POINT ( 'NONE',  ( 9.219914745407999490, -4.065337473341759988, 6.596431033727998994 ) ) ;
#28282=CARTESIAN_POINT ( 'NONE',  ( 9.729392757687000071, -3.322036695224600322, 6.758914271013199304 ) ) ;
#28285=CARTESIAN_POINT ( 'NONE',  ( 11.21918447801630059, -2.859536135895000442, 7.525145395936648995 ) ) ;
#28286=ORIENTED_EDGE ( 'NONE', *, *, #2360, .F. ) ;
#28293=CARTESIAN_POINT ( 'NONE',  ( 11.73078751119019891, -4.915752892793999962, 7.020904658857499925 ) ) ;
#28324=CARTESIAN_POINT ( 'NONE',  ( 10.33479966423462670, -3.204277625948437347, 7.136189372949617749 ) ) ;
#28348=CARTESIAN_POINT ( 'NONE',  ( 9.630088727410999638, -4.863977618062000019, 7.427538838030949719 ) ) ;
#28356=CARTESIAN_POINT ( 'NONE',  ( 11.03521345716899837, -3.075109701058799772, 6.659120737011199331 ) ) ;
#28434=CARTESIAN_POINT ( 'NONE',  ( 9.445797255587999430, -2.996487526130999779, 7.542485555928779561 ) ) ;
#28435=CARTESIAN_POINT ( 'NONE',  ( 9.311649685568999857, -3.898643963693099845, 6.542299367266399379 ) ) ;
#28454=CARTESIAN_POINT ( 'NONE',  ( 10.52145237372899800, -3.956267952212241479, 6.225919055146348136 ) ) ;
#28456=CARTESIAN_POINT ( 'NONE',  ( 11.74441369783139955, -4.043700988887960257, 6.634905315059499209 ) ) ;
#28505=CARTESIAN_POINT ( 'NONE',  ( 11.14601354018249779, -3.000416447002271170, 8.268183399968638270 ) ) ;
#28510=ORIENTED_EDGE ( 'NONE', *, *, #52867, .F. ) ;
#28521=CARTESIAN_POINT ( 'NONE',  ( 10.66562143724499911, -3.150324864944999970, 8.456261759323901117 ) ) ;
#28563=CARTESIAN_POINT ( 'NONE',  ( 10.34393020685000053, -5.250000000000000000, 7.500000000000000000 ) ) ;
#28571=DIRECTION ( 'NONE',  ( 0.000000000000000000, 1.000000000000000000, 0.000000000000000000 ) ) ;
#28580=EDGE_CURVE ( 'NONE', #41017, #28137, #42805, .T. ) ;
#28584=CARTESIAN_POINT ( 'NONE',  ( 9.475960865537832234, -5.125960927305071024, 7.353476508004328061 ) ) ;
#28598=CARTESIAN_POINT ( 'NONE',  ( 11.39564560330030041, -3.692495237344800341, 8.455191956516999952 ) ) ;
#28621=CARTESIAN_POINT ( 'NONE',  ( 9.241252916288999586, -3.907441415015589836, 6.625425395127999550 ) ) ;
#28638=CARTESIAN_POINT ( 'NONE',  ( 9.930013376692999216, -5.017903082085999777, 8.017308190024898806 ) ) ;
#28642=CARTESIAN_POINT ( 'NONE',  ( 11.90425819896749893, -5.255890247626999745, 7.263238376356399684 ) ) ;
#28650=CARTESIAN_POINT ( 'NONE',  ( 11.40346005378009941, -3.213042707518099839, 7.920222357891399945 ) ) ;
#28679=CARTESIAN_POINT ( 'NONE',  ( 10.74006601915162662, -4.042412777185713679, 6.626081523287773223 ) ) ;
#28701=CARTESIAN_POINT ( 'NONE',  ( 10.56525461470299909, -4.973404788313100511, 7.252360304610999897 ) ) ;
#28706=CARTESIAN_POINT ( 'NONE',  ( 11.07435795695566583, -2.750000000000000000, 7.192559817601734906 ) ) ;
#28843=AXIS2_PLACEMENT_3D ( 'NONE', #41089, #35842, #30946 ) ;
#28861=CARTESIAN_POINT ( 'NONE',  ( 11.34393020684979980, -5.250000000000000000, 7.500000000000000000 ) ) ;
#28874=FACE_OUTER_BOUND ( 'NONE', #10073, .T. ) ;
#28913=EDGE_LOOP ( 'NONE', ( #63039, #2145, #45503, #44233 ) ) ;
#28926=APPLICATION_CONTEXT ( 'automotive_design' ) ;
#28935=B_SPLINE_CURVE_WITH_KNOTS ( 'NONE', 3,
 ( #12155, #34176, #6897, #65281 ),
 .UNSPECIFIED., .F., .F.,
 ( 4, 4 ),
 ( 0.000000000000000000, 0.8163836489557148024 ),
 .UNSPECIFIED. ) ;
#28953=CARTESIAN_POINT ( 'NONE',  ( 11.37103032197929942, -3.416314376401300201, 8.316248703309600643 ) ) ;
#28973=CARTESIAN_POINT ( 'NONE',  ( 9.248305582559998683, -3.908727042518870043, 6.637573130164000190 ) ) ;
#28990=CARTESIAN_POINT ( 'NONE',  ( 9.476101285863999024, -4.646739515667500875, 8.268485718282699182 ) ) ;
#28993=CARTESIAN_POINT ( 'NONE',  ( 11.43656785386840014, -5.060279460151999587, 6.786470850652599474 ) ) ;
#29002=CARTESIAN_POINT ( 'NONE',  ( 10.92795525820100089, -4.094749303624469761, 8.498986197235801399 ) ) ;
#29003=CARTESIAN_POINT ( 'NONE',  ( 11.19568717260499824, -4.466067913030199676, 6.739296831621899742 ) ) ;
#29050=CARTESIAN_POINT ( 'NONE',  ( 9.376797255588000368, -3.133765047594600173, 7.536673658251589636 ) ) ;
#29082=ADVANCED_FACE ( 'NONE', ( #7385 ), #61906, .T. ) ;
#29096=CARTESIAN_POINT ( 'NONE',  ( 10.65434687351570631, -2.749999999999998668, 7.663624617374463988 ) ) ;
#29102=B_SPLINE_CURVE_WITH_KNOTS ( 'NONE', 3,
 ( #66063, #1750, #49293, #54892, #28679, #11198, #17840, #27984, #48957, #59436, #64675, #43375, #12590, #43718, #38110, #716, #1405, #38814, #39159, #60138, #28324, #6290, #11536, #32879, #48612, #17130, #22720, #22028, #12246, #55239, #33919, #60482, #59784, #2107, #44068, #27637, #6992, #49643, #33226, #32536, #23071, #23424, #11887, #1066, #65369, #27291, #54546, #2784, #61518, #12941, #30394, #18182, #8721, #29724, #66409, #67095, #24110, #34266, #13295, #34619, #51367, #25138, #40875, #8381, #19555 ),
 .UNSPECIFIED., .F., .F.,
 ( 4, 1, 1, 1, 1, 1, 1, 1, 1, 1, 1, 1, 1, 1, 1, 1, 1, 1, 1, 1, 1, 1, 1, 1, 1, 1, 1, 1, 1, 1, 1, 1, 1, 1, 1, 1, 1, 1, 1, 1, 1, 1, 1, 1, 1, 1, 1, 1, 1, 1, 1, 1, 1, 1, 1, 1, 1, 1, 1, 1, 1, 1, 4 ),
 ( 0.000000000000000000, 0.01249986222369731809, 0.02874986775682975698, 0.04499987328996219588, 0.06124987882309463477, 0.07749988435622708061, 0.09374988988935951950, 0.1099998954224919584, 0.1262499009556244112, 0.1424999064887568501, 0.1587499120218892890, 0.1749999175550217279, 0.1912499230881541668, 0.2074999286212866056, 0.2237499341544190445, 0.2399999396875514834, 0.2562499452206838946, 0.2724999507538163890, 0.2887499562869488279, 0.3049999618200812668, 0.3212499673532136502, 0.3374999728863461446, 0.3537499784194785835, 0.3699999839526110224, 0.3862499894857434612, 0.4024999950188759001, 0.4187500005520083390, 0.4350000060851407779, 0.4512500116182732168, 0.4675000171514057112, 0.4837500226845380946, 0.5000000282176705335, 0.5162500337508029169, 0.5325000392839353003, 0.5487500448170677947, 0.5650000503502001781, 0.5812500558833327835, 0.5975000614164651669, 0.6137500669495975503, 0.6300000724827300447, 0.6462500780158624281, 0.6625000835489948114, 0.6787500890821273059, 0.6950000946152596892, 0.7112501001483922947, 0.7275001056815246780, 0.7437501112146570614, 0.7600001167477895558, 0.7762501222809219392, 0.7925001278140544336, 0.8087501333471868170, 0.8250001388803192004, 0.8412501444134518058, 0.8575001499465841892, 0.8737501554797166836, 0.8900001610128490670, 0.9062501665459814504, 0.9225001720791139448, 0.9387501776122463282, 0.9550001831453788226, 0.9712501886785112060, 0.9875001942116437004, 1.000000000000000000 ),
 .UNSPECIFIED. ) ;
#29130=CARTESIAN_POINT ( 'NONE',  ( 9.595759580228998331, -4.843256805554699618, 7.701558687214699717 ) ) ;
#29176=ORIENTED_EDGE ( 'NONE', *, *, #11144, .F. ) ;
#29211=CARTESIAN_POINT ( 'NONE',  ( 10.79025461470400060, -5.106563667948999630, 7.218483930889299849 ) ) ;
#29233=ORIENTED_EDGE ( 'NONE', *, *, #42713, .T. ) ;
#29261=ORIENTED_EDGE ( 'NONE', *, *, #50603, .F. ) ;
#29289=CARTESIAN_POINT ( 'NONE',  ( 11.95764291764649911, -5.132124077409000229, 7.639947095788999221 ) ) ;
#29327=CARTESIAN_POINT ( 'NONE',  ( 10.43659632033899953, -5.057167065956000407, 7.931430460958599049 ) ) ;
#29331=CARTESIAN_POINT ( 'NONE',  ( 10.62841772631199966, -3.509411006705700053, 6.490165927606000196 ) ) ;
#29342=CARTESIAN_POINT ( 'NONE',  ( 11.88379707368349969, -4.566644629509899467, 8.490052513816499058 ) ) ;
#29343=CARTESIAN_POINT ( 'NONE',  ( 11.43990547754509990, -2.967013601007999934, 7.467215766047949899 ) ) ;
#29381=CARTESIAN_POINT ( 'NONE',  ( 12.21922412107039868, -3.930460928605089777, 8.814426450544999625 ) ) ;
#29397=CARTESIAN_POINT ( 'NONE',  ( 10.53992546752099990, -5.002009261081000524, 7.569424354486659290 ) ) ;
#29404=CARTESIAN_POINT ( 'NONE',  ( 9.403317944506802917, -4.274905112035348509, 8.526233764311365704 ) ) ;
#29406=B_SPLINE_CURVE_WITH_KNOTS ( 'NONE', 3,
 ( #38174, #47651, #21749, #58136, #68963, #27353 ),
 .UNSPECIFIED., .F., .F.,
 ( 4, 2, 4 ),
 ( 0.000000000000000000, 0.1967045975185045814, 0.3934091950370091628 ),
 .UNSPECIFIED. ) ;
#29468=CARTESIAN_POINT ( 'NONE',  ( 12.09999999999999964, -4.817420948848700313, 7.825000000000000178 ) ) ;
#29517=CARTESIAN_POINT ( 'NONE',  ( 12.35159063708299954, -3.174974693948799942, 7.268038553423699533 ) ) ;
#29558=ORIENTED_EDGE ( 'NONE', *, *, #46755, .F. ) ;
#29566=CARTESIAN_POINT ( 'NONE',  ( 10.73959632033899858, -5.057167065956000407, 7.931430460958599049 ) ) ;
#29598=VERTEX_POINT ( 'NONE', #50909 ) ;
#29641=CARTESIAN_POINT ( 'NONE',  ( 11.34226088462130022, -3.997572771977982775, 8.640738455926999961 ) ) ;
#29652=CARTESIAN_POINT ( 'NONE',  ( 11.62299956498149989, -2.792989229543000107, 7.174999999999999822 ) ) ;
#29664=CARTESIAN_POINT ( 'NONE',  ( 9.219734573340000239, -4.222669097051499953, 6.647493632115700102 ) ) ;
#29680=CARTESIAN_POINT ( 'NONE',  ( 9.172151519676999598, -3.978278301382419890, 6.495824366094999469 ) ) ;
#29688=EDGE_CURVE ( 'NONE', #48587, #57524, #49523, .T. ) ;
#29694=CARTESIAN_POINT ( 'NONE',  ( 10.85410941423799791, -3.257202320419700037, 8.174686939644999484 ) ) ;
#29724=CARTESIAN_POINT ( 'NONE',  ( 9.498937807218625906, -4.055078665241000024, 8.373211663664079651 ) ) ;
#29729=CARTESIAN_POINT ( 'NONE',  ( 12.05300581613033906, -2.892415530317000272, 6.788791567531699656 ) ) ;
#29744=CARTESIAN_POINT ( 'NONE',  ( 10.00801337669299862, -4.895413217368500547, 7.955057656228099461 ) ) ;
#29750=CARTESIAN_POINT ( 'NONE',  ( 9.357090631127384484, -3.380484464318182170, 8.304725771527003531 ) ) ;
#29755=CARTESIAN_POINT ( 'NONE',  ( 9.251496707488000126, -3.918323994020610268, 6.643597378104299622 ) ) ;
#29765=CARTESIAN_POINT ( 'NONE',  ( 11.44903032197930060, -3.496160833528699996, 8.204588308639600314 ) ) ;
#29779=EDGE_LOOP ( 'NONE', ( #38249, #48399, #17523, #10224, #16194, #2797, #25242, #47678, #54927, #8493, #38533, #32271 ) ) ;
#29826=CARTESIAN_POINT ( 'NONE',  ( 9.276575450301999481, -4.067929031554969654, 6.560591699025100532 ) ) ;
#29859=CARTESIAN_POINT ( 'NONE',  ( 11.94133594839949986, -3.430493414882899827, 8.152656755002400502 ) ) ;
#29864=CARTESIAN_POINT ( 'NONE',  ( 9.959367640781000119, -3.591293244209800228, 8.264635032075899446 ) ) ;
#29883=COLOUR_RGB ( '', 0.31764706, 0.68627451, 0.89019608) ;
#29907=CARTESIAN_POINT ( 'NONE',  ( 10.68893802597400011, -4.593629475532499562, 8.475365825607600101 ) ) ;
#29944=EDGE_LOOP ( 'NONE', ( #19177, #21835, #5428, #9559, #49557, #53899, #50056, #42939, #5235, #30552, #34229 ) ) ;
#29962=PRODUCT ( 'Terminal Screw', 'Terminal Screw', '', ( #4009 ) ) ;
#29983=CARTESIAN_POINT ( 'NONE',  ( 11.21918447801630059, -2.859536135895000442, 7.525145395936648995 ) ) ;
#30022=CARTESIAN_POINT ( 'NONE',  ( 10.60344474310099905, -2.862064370975999861, 6.947770206896899836 ) ) ;
#30025=CARTESIAN_POINT ( 'NONE',  ( 10.64887885159599890, -2.730985436695000157, 7.651388779553199626 ) ) ;
#30035=CARTESIAN_POINT ( 'NONE',  ( 10.72687885159599830, -2.867290578374000365, 7.635128076451499268 ) ) ;
#30069=CARTESIAN_POINT ( 'NONE',  ( 11.18546886766499959, -4.566506264294200257, 8.529286361367999447 ) ) ;
#30085=CARTESIAN_POINT ( 'NONE',  ( 12.10000000000000320, -4.400439255161259666, 8.403338258880266309 ) ) ;
#30108=CARTESIAN_POINT ( 'NONE',  ( 12.13410404293056999, -4.442327784369100030, 6.599279737936000423 ) ) ;
#30115=FACE_OUTER_BOUND ( 'NONE', #9012, .T. ) ;
#30116=B_SPLINE_CURVE_WITH_KNOTS ( 'NONE', 3,
 ( #28356, #44447, #28706, #2130 ),
 .UNSPECIFIED., .F., .F.,
 ( 4, 4 ),
 ( 0.000000000000000000, 1.000000000000000000 ),
 .UNSPECIFIED. ) ;
#30136=CARTESIAN_POINT ( 'NONE',  ( 9.548601287889788125, -3.999999532294070459, 6.301404677806389465 ) ) ;
#30164=CARTESIAN_POINT ( 'NONE',  ( 9.342468108405999061, -3.165798890946399879, 7.263744984161399465 ) ) ;
#30178=CARTESIAN_POINT ( 'NONE',  ( 11.19057802013490033, -5.033226574983999946, 7.524052967375959966 ) ) ;
#30186=FACE_OUTER_BOUND ( 'NONE', #61105, .T. ) ;
#30197=CARTESIAN_POINT ( 'NONE',  ( 10.44062143724499947, -3.424116261072899903, 8.148124882831599081 ) ) ;
#30241=CARTESIAN_POINT ( 'NONE',  ( 9.625113844317999323, -3.711648483798899889, 8.604802177355001191 ) ) ;
#30276=CARTESIAN_POINT ( 'NONE',  ( 12.07299956498157023, -2.792989229543000107, 7.174999999999999822 ) ) ;
#30313=CARTESIAN_POINT ( 'NONE',  ( 11.58841369783139896, -4.057552111898620417, 6.360711682373000109 ) ) ;
#30325=B_SPLINE_CURVE_WITH_KNOTS ( 'NONE', 3,
 ( #60626, #55384, #66205, #18327, #39651, #60973, #55733, #41369, #62004, #62678 ),
 .UNSPECIFIED., .F., .F.,
 ( 4, 2, 2, 2, 4 ),
 ( 0.000000000000000000, 0.2499999999999997780, 0.4999999999999995559, 0.7499999999999997780, 1.000000000000000000 ),
 .UNSPECIFIED. ) ;
#30352=CARTESIAN_POINT ( 'NONE',  ( 10.48524205624999972, -4.458751122174599679, 6.305876158747000026 ) ) ;
#30357=CARTESIAN_POINT ( 'NONE',  ( 10.02934687351566723, -3.836375382625533348, 6.250000000000000000 ) ) ;
#30362=CARTESIAN_POINT ( 'NONE',  ( 12.17766954483535891, -3.284117569315500251, 8.604570063127999546 ) ) ;
#30364=CARTESIAN_POINT ( 'NONE',  ( 10.65303300763299887, -3.212834858289399964, 6.674373427955200277 ) ) ;
#30394=CARTESIAN_POINT ( 'NONE',  ( 9.574925248765625341, -4.744576382809566617, 7.959497855362744012 ) ) ;
#30401=CARTESIAN_POINT ( 'NONE',  ( 11.38813259637009878, -5.155817667926999803, 6.870201387206400057 ) ) ;
#30425=CARTESIAN_POINT ( 'NONE',  ( 11.90221299665285848, -3.091095606691090847, 7.175011619880304004 ) ) ;
#30439=CARTESIAN_POINT ( 'NONE',  ( 11.39979975933730039, -3.180925410802600162, 7.781807394638899922 ) ) ;
#30481=FACE_OUTER_BOUND ( 'NONE', #20081, .T. ) ;
#30511=CARTESIAN_POINT ( 'NONE',  ( 11.02435971519499880, -3.467537960339900138, 8.385788382729799650 ) ) ;
#30531=ORIENTED_EDGE ( 'NONE', *, *, #31322, .T. ) ;
#30532=CARTESIAN_POINT ( 'NONE',  ( 10.59259632033900012, -4.802737635155300389, 7.827597670336898794 ) ) ;
#30551=CARTESIAN_POINT ( 'NONE',  ( 11.82240614981508742, -3.267563509902000174, 7.017906081141797259 ) ) ;
#30552=ORIENTED_EDGE ( 'NONE', *, *, #4248, .F. ) ;
#30570=CARTESIAN_POINT ( 'NONE',  ( 9.954392757686999715, -3.229293331742300044, 6.657535947657399866 ) ) ;
#30649=CARTESIAN_POINT ( 'NONE',  ( 11.16995391537419913, -3.056324258617099776, 6.859089544950699668 ) ) ;
#30665=CARTESIAN_POINT ( 'NONE',  ( 9.310863317747999801, -3.039136629551499880, 7.499999999926881600 ) ) ;
#30682=VERTEX_POINT ( 'NONE', #5765 ) ;
#30687=CARTESIAN_POINT ( 'NONE',  ( 9.423430433046998900, -4.971677342931100085, 8.099647887697699389 ) ) ;
#30692=CARTESIAN_POINT ( 'NONE',  ( 9.914763540182331525, -5.217465845835395299, 7.172815144550902744 ) ) ;
#30697=CARTESIAN_POINT ( 'NONE',  ( 12.09456039236534330, -2.685288321999000249, 7.436015812896529020 ) ) ;
#30700=CARTESIAN_POINT ( 'NONE',  ( 11.39149144726329865, -4.659577337894599935, 8.430724369296298093 ) ) ;
#30706=LINE ( 'NONE', #58300, #1134 ) ;
#30724=CARTESIAN_POINT ( 'NONE',  ( 12.09999999999999964, -4.000000000000000000, 7.500000000000000000 ) ) ;
#30739=CARTESIAN_POINT ( 'NONE',  ( 11.22191429142990060, -3.974927396630719922, 8.816028813488999916 ) ) ;
#30754=CARTESIAN_POINT ( 'NONE',  ( 12.09999999999999964, -4.817420948848700313, 7.825000000000000178 ) ) ;
#30777=CARTESIAN_POINT ( 'NONE',  ( 12.28179573085659904, -3.026866171144600326, 7.331616337578100051 ) ) ;
#30824=CARTESIAN_POINT ( 'NONE',  ( 12.28594988689359901, -3.606563555963900214, 6.728309553046099012 ) ) ;
#30855=CARTESIAN_POINT ( 'NONE',  ( 11.10235971519489873, -3.394698737128500010, 8.506961598696999971 ) ) ;
#30879=CARTESIAN_POINT ( 'NONE',  ( 10.54193802597399987, -4.450760089576400347, 8.240623579255899500 ) ) ;
#30918=CARTESIAN_POINT ( 'NONE',  ( 9.397151519676999243, -3.975306837623020062, 6.358456126310000123 ) ) ;
#30935=CARTESIAN_POINT ( 'NONE',  ( 11.07101354018312378, -3.231816600031356845, 6.500416447002274722 ) ) ;
#30946=DIRECTION ( 'NONE',  ( 0.000000000000000000, 1.000000000000000000, 0.000000000000000000 ) ) ;
#30986=AXIS2_PLACEMENT_3D ( 'NONE', #41467, #51943, #45687 ) ;
#30997=CARTESIAN_POINT ( 'NONE',  ( 9.236413463905998711, -3.915843685459630574, 6.617590440947399344 ) ) ;
#31001=CARTESIAN_POINT ( 'NONE',  ( 10.65303300763299887, -3.212834858289399964, 6.674373427955200277 ) ) ;
#31019=ORIENTED_EDGE ( 'NONE', *, *, #17345, .T. ) ;
#31040=CARTESIAN_POINT ( 'NONE',  ( 10.00398825978600037, -4.167373623506299474, 6.231784538167999266 ) ) ;
#31043=CARTESIAN_POINT ( 'NONE',  ( 11.28887616594230003, -4.386455737425299262, 8.718182393403999697 ) ) ;
#31051=CARTESIAN_POINT ( 'NONE',  ( 11.60101463001529964, -3.377766160221900016, 8.496586578655598743 ) ) ;
#31053=CARTESIAN_POINT ( 'NONE',  ( 11.29303032197930001, -3.336467919271199900, 8.427909097977700270 ) ) ;
#31091=CARTESIAN_POINT ( 'NONE',  ( 11.34657802013509986, -5.315911219205999849, 7.530633716161349689 ) ) ;
#31108=CARTESIAN_POINT ( 'NONE',  ( 12.10000000000000142, -3.409519984105202184, 8.459313701734298974 ) ) ;
#31135=CARTESIAN_POINT ( 'NONE',  ( 11.61718313518939993, -4.622449961306399402, 6.712912394634500401 ) ) ;
#31180=CARTESIAN_POINT ( 'NONE',  ( 12.31056516821460001, -3.390321848206700128, 6.884701936848800052 ) ) ;
#31209=CARTESIAN_POINT ( 'NONE',  ( 11.98522412107029922, -3.952868550833580130, 8.390877922225699947 ) ) ;
#31210=EDGE_CURVE ( 'NONE', #11416, #68324, #26008, .T. ) ;
#31212=CARTESIAN_POINT ( 'NONE',  ( 9.823602683899249399, -5.219044746006709978, 7.819247029363189050 ) ) ;
#31219=CARTESIAN_POINT ( 'NONE',  ( 11.34393020684979980, -5.250000000000000000, 7.500000000000000000 ) ) ;
#31224=CARTESIAN_POINT ( 'NONE',  ( 11.59672200990539892, -4.817867935977999672, 7.785290430335599865 ) ) ;
#31266=CARTESIAN_POINT ( 'NONE',  ( 10.25632996542199926, -4.697624103824200148, 6.777391592843399870 ) ) ;
#31303=CARTESIAN_POINT ( 'NONE',  ( 12.06493925477931661, -2.826469659297512482, 7.051164236119339179 ) ) ;
#31322=EDGE_CURVE ( 'NONE', #7217, #11254, #18601, .T. ) ;
#31341=CARTESIAN_POINT ( 'NONE',  ( 12.02733460557258915, -3.793662715184400014, 6.238754009183999472 ) ) ;
#31356=ORIENTED_EDGE ( 'NONE', *, *, #44680, .F. ) ;
#31378=CARTESIAN_POINT ( 'NONE',  ( 9.978659112603999404, -4.555852086785099786, 6.347865960448999090 ) ) ;
#31390=CARTESIAN_POINT ( 'NONE',  ( 11.88678751119029897, -5.166297436425000278, 6.889827023674499173 ) ) ;
#31392=CARTESIAN_POINT ( 'NONE',  ( 10.75149413291699929, -2.962184842772000337, 7.973529073237199505 ) ) ;
#31413=CARTESIAN_POINT ( 'NONE',  ( 11.80361999289329944, -4.544092497359196514, 8.657883396625690509 ) ) ;
#31428=CARTESIAN_POINT ( 'NONE',  ( 12.06833327354034857, -4.746587807672299597, 7.988332985010599963 ) ) ;
#31442=CARTESIAN_POINT ( 'NONE',  ( 12.09999999999999964, -3.186139913033901205, 8.315594847681079926 ) ) ;
#31467=CARTESIAN_POINT ( 'NONE',  ( 11.83872066707849946, -3.141388196630700236, 8.019361746728900897 ) ) ;
#31511=CARTESIAN_POINT ( 'NONE',  ( 11.49826088462129903, -3.998156935320088756, 8.366195817038299509 ) ) ;
#31526=ORIENTED_EDGE ( 'NONE', *, *, #35876, .F. ) ;
#31543=CARTESIAN_POINT ( 'NONE',  ( 11.27879632507499963, -3.576455950783300253, 6.714825466131699727 ) ) ;
#31560=CARTESIAN_POINT ( 'NONE',  ( 10.98133997688000107, -3.815400206859000054, 8.346298710230199092 ) ) ;
#31590=ADVANCED_FACE ( 'NONE', ( #44547 ), #3893, .F. ) ;
#31604=CARTESIAN_POINT ( 'NONE',  ( 10.83890035061499901, -3.732283713685800031, 6.531924610394499453 ) ) ;
#31621=CARTESIAN_POINT ( 'NONE',  ( 10.94601354018327122, -4.999583552997726166, 6.731816600031359066 ) ) ;
#31622=CARTESIAN_POINT ( 'NONE',  ( 10.81652245563454784, -3.317579219585634842, 6.971781362826274808 ) ) ;
#31685=CARTESIAN_POINT ( 'NONE',  ( 11.06733863405299800, -3.211524470605299886, 6.494205428462000107 ) ) ;
#31735=CARTESIAN_POINT ( 'NONE',  ( 12.26077869730539938, -4.595338376575799799, 8.673950353177000139 ) ) ;
#31737=CARTESIAN_POINT ( 'NONE',  ( 11.21503032197930061, -3.256621462143499901, 8.539569492647999027 ) ) ;
#31761=CARTESIAN_POINT ( 'NONE',  ( 11.94571737393083133, -5.011200127299592744, 6.726238946114239781 ) ) ;
#31773=CARTESIAN_POINT ( 'NONE',  ( 10.98791429143000009, -3.983006558652820051, 8.391963954669400039 ) ) ;
#31813=CARTESIAN_POINT ( 'NONE',  ( 11.78533594839949927, -3.249987070165300196, 8.359517726022600570 ) ) ;
#31820=CARTESIAN_POINT ( 'NONE',  ( 11.38813259637009878, -5.155817667926999803, 6.870201387206400057 ) ) ;
#31858=CARTESIAN_POINT ( 'NONE',  ( 12.23671932425159881, -4.127012898954600217, 6.643164954553199664 ) ) ;
#31895=CARTESIAN_POINT ( 'NONE',  ( 9.793111399473126255, -5.011294126480321687, 8.251846359484561688 ) ) ;
#31906=CARTESIAN_POINT ( 'NONE',  ( 12.23256516821459883, -3.293702443348299980, 6.787191910456499500 ) ) ;
#31952=CARTESIAN_POINT ( 'NONE',  ( 10.12968422950999958, -4.708027397558999461, 8.212418068717900255 ) ) ;
#31975=CARTESIAN_POINT ( 'NONE',  ( 11.37068169682077645, -3.126090202221432079, 7.519268307021759412 ) ) ;
#32037=CARTESIAN_POINT ( 'NONE',  ( 11.63349010443640097, -2.725546193138000284, 7.404690636538299842 ) ) ;
#32075=CARTESIAN_POINT ( 'NONE',  ( 9.099999952505998024, -4.000000000000000000, 7.500000000000000000 ) ) ;
#32087=CARTESIAN_POINT ( 'NONE',  ( 11.46118313518939935, -4.792748567750200195, 6.497569908212999401 ) ) ;
#32107=CARTESIAN_POINT ( 'NONE',  ( 11.69955063476129453, -3.023401864784706294, 8.326430086672804265 ) ) ;
#32110=B_SPLINE_CURVE_WITH_KNOTS ( 'NONE', 3,
 ( #48262, #21011, #42348, #63647 ),
 .UNSPECIFIED., .F., .F.,
 ( 4, 4 ),
 ( 0.1836163425310833319, 1.000000000000000000 ),
 .UNSPECIFIED. ) ;
#32121=CARTESIAN_POINT ( 'NONE',  ( 11.56456920625009843, -3.962850971080120299, 8.532838639935999225 ) ) ;
#32159=ORIENTED_EDGE ( 'NONE', *, *, #10334, .F. ) ;
#32162=CARTESIAN_POINT ( 'NONE',  ( 11.63764426047339917, -3.386171819220400003, 6.538488127609999978 ) ) ;
#32170=CARTESIAN_POINT ( 'NONE',  ( 11.47635090131019986, -3.000792947412299849, 6.881982988766500497 ) ) ;
#32208=CARTESIAN_POINT ( 'NONE',  ( 11.59256785386839894, -4.832509746210599921, 6.939751505745099358 ) ) ;
#32245=CARTESIAN_POINT ( 'NONE',  ( 9.671146261768624797, -3.287258916643901241, 8.539225147222756718 ) ) ;
#32255=CARTESIAN_POINT ( 'NONE',  ( 10.83364828895399867, -3.239803852721999888, 7.084788038520800413 ) ) ;
#32271=ORIENTED_EDGE ( 'NONE', *, *, #37644, .T. ) ;
#32303=CARTESIAN_POINT ( 'NONE',  ( 10.86422949779699998, -3.442773960835399993, 6.664331202173499946 ) ) ;
#32378=CARTESIAN_POINT ( 'NONE',  ( 11.41195257254739914, -5.227167235646000165, 7.143100915737699452 ) ) ;
#32383=VECTOR ( 'NONE', #8861, 1000.000000000000000 ) ;
#32412=CARTESIAN_POINT ( 'NONE',  ( 9.244113844317999096, -3.676949563211899807, 8.737749087159000894 ) ) ;
#32426=CARTESIAN_POINT ( 'NONE',  ( 10.55041772631200026, -3.450375740502100275, 6.368647051112000135 ) ) ;
#32460=CARTESIAN_POINT ( 'NONE',  ( 10.87199293566600034, -3.366612813978900220, 6.723009541442299231 ) ) ;
#32499=CARTESIAN_POINT ( 'NONE',  ( 11.27256919669530077, -3.037654633983899899, 7.215672285280100517 ) ) ;
#32505=CARTESIAN_POINT ( 'NONE',  ( 12.18788784977535933, -4.985985832792199979, 7.556342205905759890 ) ) ;
#32536=CARTESIAN_POINT ( 'NONE',  ( 9.853545867770625577, -3.141341610201948686, 7.331958223794097229 ) ) ;
#32576=CARTESIAN_POINT ( 'NONE',  ( 9.650818738817875442, -3.048937241343601112, 8.326721469190600189 ) ) ;
#32579=EDGE_CURVE ( 'NONE', #57524, #58532, #64250, .T. ) ;
#32588=CARTESIAN_POINT ( 'NONE',  ( 12.20794988689359961, -3.544213289744700290, 6.606015074393400077 ) ) ;
#32638=CARTESIAN_POINT ( 'NONE',  ( 9.671747021775999542, -4.651672637235799712, 6.928134003122899287 ) ) ;
#32653=CARTESIAN_POINT ( 'NONE',  ( 11.24760529021567734, -3.959614718189205185, 6.626811228128840270 ) ) ;
#32658=CARTESIAN_POINT ( 'NONE',  ( 11.81825954179440075, -3.333768806796900019, 6.946434658287599540 ) ) ;
#32721=CARTESIAN_POINT ( 'NONE',  ( 10.53897570133299944, -3.061513547538400104, 6.630731591496600075 ) ) ;
#32725=CARTESIAN_POINT ( 'NONE',  ( 12.09999999999999964, -2.935681553670999921, 6.844464917182299324 ) ) ;
#32753=CARTESIAN_POINT ( 'NONE',  ( 9.548063610505000298, -3.475294527116599586, 6.333351572150998976 ) ) ;
#32772=CARTESIAN_POINT ( 'NONE',  ( 10.05226354018333446, -2.907767014557177898, 6.870476274536374994 ) ) ;
#32802=CARTESIAN_POINT ( 'NONE',  ( 12.02677869730533011, -4.403502086956500250, 8.295667533166499297 ) ) ;
#32835=B_SPLINE_CURVE_WITH_KNOTS ( 'NONE', 3,
 ( #23912, #65167, #12741, #13439, #61321, #65864, #43863, #60977, #7143, #38613, #44572, #7839, #34071, #59933, #22874, #45249, #50482, #1905 ),
 .UNSPECIFIED., .F., .F.,
 ( 4, 2, 2, 2, 2, 2, 2, 2, 4 ),
 ( 0.000000000000000000, 0.1250000000000000000, 0.2500000000000000000, 0.3750000000000000000, 0.5000000000000000000, 0.6250000000000000000, 0.7500000000000000000, 0.8750000000000000000, 1.000000000000000000 ),
 .UNSPECIFIED. ) ;
#32843=CARTESIAN_POINT ( 'NONE',  ( 12.15456516821461008, -3.197083038490000195, 6.689681884064299311 ) ) ;
#32850=CARTESIAN_POINT ( 'NONE',  ( 11.59590547754519996, -2.684394667508000154, 7.458246194669389872 ) ) ;
#32879=CARTESIAN_POINT ( 'NONE',  ( 10.25881222268762549, -3.837269700090108593, 6.640319176431033199 ) ) ;
#32932=CARTESIAN_POINT ( 'NONE',  ( 11.05103166480599874, -5.000984463463999496, 7.429424106427209296 ) ) ;
#32954=PRODUCT_DEFINITION_FORMATION_WITH_SPECIFIED_SOURCE ( 'ANY', '', #29962, .NOT_KNOWN. ) ;
#32980=CARTESIAN_POINT ( 'NONE',  ( 10.76090035061499961, -3.768906505327899836, 6.664354444139199529 ) ) ;
#33001=CARTESIAN_POINT ( 'NONE',  ( 12.28594988689359901, -3.606563555963900214, 6.728309553046099012 ) ) ;
#33066=CARTESIAN_POINT ( 'NONE',  ( 10.84292546752099895, -5.276153033933000280, 7.588418444866789514 ) ) ;
#33077=ORIENTED_EDGE ( 'NONE', *, *, #44565, .T. ) ;
#33115=CARTESIAN_POINT ( 'NONE',  ( 11.43656785386840014, -5.060279460151999587, 6.786470850652599474 ) ) ;
#33186=CARTESIAN_POINT ( 'NONE',  ( 11.66225954179439839, -3.122605388210700106, 6.770980925167799036 ) ) ;
#33195=CARTESIAN_POINT ( 'NONE',  ( 11.97500581613029880, -3.011381429075500105, 6.865182626353099948 ) ) ;
#33224=EDGE_CURVE ( 'NONE', #55934, #50471, #49041, .T. ) ;
#33226=CARTESIAN_POINT ( 'NONE',  ( 9.878875014952626543, -3.131883468830893857, 7.609114422657746069 ) ) ;
#33272=CARTESIAN_POINT ( 'NONE',  ( 9.852250488097013204, -5.092274670905198697, 8.129544561320937390 ) ) ;
#33277=EDGE_CURVE ( 'NONE', #40612, #58532, #61262, .T. ) ;
#33281=ORIENTED_EDGE ( 'NONE', *, *, #57711, .F. ) ;
#33297=ORIENTED_EDGE ( 'NONE', *, *, #63905, .F. ) ;
#33311=CARTESIAN_POINT ( 'NONE',  ( 11.64975833414749928, -4.796537143354000499, 7.174999999999999822 ) ) ;
#33332=CARTESIAN_POINT ( 'NONE',  ( 10.82844474310100047, -3.228742141949900279, 7.125715588371799747 ) ) ;
#33334=CARTESIAN_POINT ( 'NONE',  ( 11.31059687351629961, -4.629523725463621453, 8.592232985442823434 ) ) ;
#33343=LINE ( 'NONE', #59554, #41948 ) ;
#33349=CARTESIAN_POINT ( 'NONE',  ( 10.56927318630899926, -3.243547362524661359, 6.473854711408034923 ) ) ;
#33352=CARTESIAN_POINT ( 'NONE',  ( 12.06441235500451015, -4.638700978900200056, 8.085115074060599483 ) ) ;
#33410=CARTESIAN_POINT ( 'NONE',  ( 10.79657053952199952, -4.502253688815499366, 8.675184076076000395 ) ) ;
#33415=CARTESIAN_POINT ( 'NONE',  ( 10.05772190487000017, -2.884547197234000215, 6.873781641694999500 ) ) ;
#33435=ORIENTED_EDGE ( 'NONE', *, *, #64292, .F. ) ;
#33456=EDGE_CURVE ( 'NONE', #11483, #24435, #51454, .T. ) ;
#33461=CARTESIAN_POINT ( 'NONE',  ( 9.643927823787143083, -2.750011555256801188, 7.500000155056757656 ) ) ;
#33466=CARTESIAN_POINT ( 'NONE',  ( 9.885596873516664829, -5.092232985442824322, 6.870476274536375882 ) ) ;
#33494=CARTESIAN_POINT ( 'NONE',  ( 12.25718044953559982, -3.110233631466100324, 7.036033215662999218 ) ) ;
#33531=CARTESIAN_POINT ( 'NONE',  ( 10.13264655415100002, -3.447209681134600245, 6.500921769151600138 ) ) ;
#33534=CARTESIAN_POINT ( 'NONE',  ( 11.85502763632550050, -5.160433036184000066, 8.035454525731699604 ) ) ;
#33544=CARTESIAN_POINT ( 'NONE',  ( 11.31524174883999834, -4.028418853626810403, 6.466884287543999577 ) ) ;
#33562=B_SPLINE_CURVE_WITH_KNOTS ( 'NONE', 3,
 ( #49141, #22911, #43909, #11384, #43561, #55082, #64175, #911, #64861, #42866, #6836, #28169, #49485, #1596, #6138, #32725 ),
 .UNSPECIFIED., .F., .F.,
 ( 4, 2, 2, 2, 2, 2, 2, 4 ),
 ( 0.000000000000000000, 0.06250000000000043021, 0.1250000000000008604, 0.2500000000000007216, 0.3750000000000006106, 0.5000000000000005551, 0.7500000000000002220, 1.000000000000000000 ),
 .UNSPECIFIED. ) ;
#33594=CARTESIAN_POINT ( 'NONE',  ( 9.528772138681999238, -4.322628849750500102, 8.304747519296199698 ) ) ;
#33600=CARTESIAN_POINT ( 'NONE',  ( 9.462753061708918167, -5.112753122729035482, 7.646523492023318269 ) ) ;
#33678=CARTESIAN_POINT ( 'NONE',  ( 9.823721904869998411, -3.243980311826100138, 7.075568408810499754 ) ) ;
#33680=CARTESIAN_POINT ( 'NONE',  ( 11.32101354018296568, -4.768183399968640934, 8.499583552997727054 ) ) ;
#33697=CARTESIAN_POINT ( 'NONE',  ( 12.21210404293059959, -4.381818659177399766, 6.722495590581700320 ) ) ;
#33763=CARTESIAN_POINT ( 'NONE',  ( 9.829759580229000093, -5.244164909883999748, 7.797385380423699885 ) ) ;
#33781=LINE ( 'NONE', #61032, #40995 ) ;
#33839=CARTESIAN_POINT ( 'NONE',  ( 12.15871932425157098, -4.147141405561299621, 6.507377093516500288 ) ) ;
#33878=CARTESIAN_POINT ( 'NONE',  ( 10.00600081823899856, -5.010295986746999830, 6.967988282883199602 ) ) ;
#33882=CARTESIAN_POINT ( 'NONE',  ( 10.72687885159599830, -2.867290578374000365, 7.635128076451499268 ) ) ;
#33891=CARTESIAN_POINT ( 'NONE',  ( 11.48656920625009903, -3.967932847735990531, 8.391549386185598536 ) ) ;
#33919=CARTESIAN_POINT ( 'NONE',  ( 10.08150819241162566, -4.779998216922380472, 7.896402636871828307 ) ) ;
#33930=ADVANCED_FACE ( 'NONE', ( #22128 ), #21426, .T. ) ;
#33941=CARTESIAN_POINT ( 'NONE',  ( 10.21064655415099942, -3.513729974241599940, 6.621146336197599958 ) ) ;
#33946=DIRECTION ( 'NONE',  ( -1.000000000000000000, 0.000000000000000000, 0.000000000000000000 ) ) ;
#34000=B_SPLINE_SURFACE_WITH_KNOTS ( 'NONE', 3, 3, ( 
 ( #27926, #49236, #22663, #7627 ),
 ( #28973, #18468, #29664, #13234 ),
 ( #28621, #34560, #39794, #50281 ),
 ( #17782, #28266, #44705, #7282 ) ),
 .UNSPECIFIED., .F., .F., .F.,
 ( 4, 4 ),
 ( 4, 4 ),
 ( -0.01349945606786999951, 0.08053609420915000539 ),
 ( -0.0005287450254680999126, 0.02696599629895000266 ),
 .UNSPECIFIED. ) ;
#34028=CARTESIAN_POINT ( 'NONE',  ( 10.38096314287999888, -3.151633609938700342, 7.678836273503299559 ) ) ;
#34030=CARTESIAN_POINT ( 'NONE',  ( 11.22726354018300121, -3.370476274536371442, 8.592232985442818105 ) ) ;
#34046=CARTESIAN_POINT ( 'NONE',  ( 10.55333291544900121, -3.468906853242414989, 6.341063066638221279 ) ) ;
#34071=CARTESIAN_POINT ( 'NONE',  ( 10.21684687351566723, -3.231816600031351516, 8.499583552997721725 ) ) ;
#34093=CARTESIAN_POINT ( 'NONE',  ( 11.33351354018309998, -5.249999999999999112, 7.663624617374471093 ) ) ;
#34108=CYLINDRICAL_SURFACE ( 'NONE', #49411, 1.250000000000000222 ) ;
#34109=CARTESIAN_POINT ( 'NONE',  ( 10.94424205625099944, -4.458751122174599679, 6.305876158747000026 ) ) ;
#34136=ORIENTED_EDGE ( 'NONE', *, *, #36263, .F. ) ;
#34153=CARTESIAN_POINT ( 'NONE',  ( 9.629282595918656540, -2.750056606219161370, 7.269976573734650671 ) ) ;
#34176=CARTESIAN_POINT ( 'NONE',  ( 9.236820887142258130, -4.253281749927232624, 6.641515014115457305 ) ) ;
#34186=CARTESIAN_POINT ( 'NONE',  ( 12.28179573085659904, -3.026866171144600326, 7.331616337578100051 ) ) ;
#34225=CARTESIAN_POINT ( 'NONE',  ( 9.602747021775998704, -4.754947163618299832, 6.837506920432799618 ) ) ;
#34228=CARTESIAN_POINT ( 'NONE',  ( 12.10118044953561878, -2.866798846279000390, 6.909094663619399945 ) ) ;
#34229=ORIENTED_EDGE ( 'NONE', *, *, #28179, .T. ) ;
#34237=CARTESIAN_POINT ( 'NONE',  ( 10.95257053952200010, -4.394359323863099576, 8.422730500489899796 ) ) ;
#34238=CARTESIAN_POINT ( 'NONE',  ( 11.61123293495519881, -4.891405920092699589, 7.535834283667469435 ) ) ;
#34266=CARTESIAN_POINT ( 'NONE',  ( 9.397621218489627282, -3.181327125463422334, 7.808718305523518310 ) ) ;
#34288=CARTESIAN_POINT ( 'NONE',  ( 10.66657120343299958, -4.048688523195909994, 6.496769302834999316 ) ) ;
#34294=CARTESIAN_POINT ( 'NONE',  ( 9.423129650240840149, -4.658877085170328058, 8.358757503607595396 ) ) ;
#34321=VERTEX_POINT ( 'NONE', #4241 ) ;
#34337=CARTESIAN_POINT ( 'NONE',  ( 10.89393020684999946, -5.250000000000000000, 7.500000000000000000 ) ) ;
#34355=VERTEX_POINT ( 'NONE', #57047 ) ;
#34374=CARTESIAN_POINT ( 'NONE',  ( 9.570430433046999141, -4.737822807309499673, 7.955330044604899342 ) ) ;
#34460=CARTESIAN_POINT ( 'NONE',  ( 10.98444474310100105, -2.984290294633999974, 7.007085334055199510 ) ) ;
#34463=ORIENTED_EDGE ( 'NONE', *, *, #33456, .T. ) ;
#34536=CARTESIAN_POINT ( 'NONE',  ( 12.10533460557258323, -3.815825449682300086, 6.374224726731999802 ) ) ;
#34560=CARTESIAN_POINT ( 'NONE',  ( 9.226967411678998587, -4.064442376558529801, 6.608809560686199625 ) ) ;
#34574=CARTESIAN_POINT ( 'NONE',  ( 9.146822372494000319, -4.288705740401799638, 6.555546982591299532 ) ) ;
#34577=CARTESIAN_POINT ( 'NONE',  ( 11.87964291764649971, -5.268358781405000357, 7.656787697937099679 ) ) ;
#34579=CARTESIAN_POINT ( 'NONE',  ( 10.14393020684900115, -2.750000000000000000, 7.500000000000000000 ) ) ;
#34587=CARTESIAN_POINT ( 'NONE',  ( 11.64179841651039915, -4.353306409735099969, 6.560784671286499226 ) ) ;
#34588=CARTESIAN_POINT ( 'NONE',  ( 11.10746886766490071, -4.498335456194499926, 8.405426684175299812 ) ) ;
#34593=ORIENTED_EDGE ( 'NONE', *, *, #13366, .F. ) ;
#34619=CARTESIAN_POINT ( 'NONE',  ( 9.346962924124627037, -3.158163127838481188, 7.261582451272839300 ) ) ;
#34632=ORIENTED_EDGE ( 'NONE', *, *, #39622, .F. ) ;
#34638=CARTESIAN_POINT ( 'NONE',  ( 10.41327973160900022, -3.909869487835140323, 8.500359330993999762 ) ) ;
#34796=CARTESIAN_POINT ( 'NONE',  ( 10.18235508232799980, -4.511005581663400044, 8.521081653687000212 ) ) ;
#34806=CARTESIAN_POINT ( 'NONE',  ( 12.09999999999999964, -2.935681553670999921, 6.844464917182299324 ) ) ;
#34814=PRESENTATION_STYLE_ASSIGNMENT (( #23621 ) ) ;
#34819=CARTESIAN_POINT ( 'NONE',  ( 11.96253286130404980, -3.661005694687299528, 8.308656198582323071 ) ) ;
#34870=CARTESIAN_POINT ( 'NONE',  ( 11.36687616594229944, -4.344946439135400240, 8.587337146608000182 ) ) ;
#34912=CARTESIAN_POINT ( 'NONE',  ( 10.68988779216199880, -2.943881405003000218, 7.119137915499500480 ) ) ;
#34916=CARTESIAN_POINT ( 'NONE',  ( 11.07149279008999976, -4.296686446741600385, 6.398515879103999993 ) ) ;
#34925=CARTESIAN_POINT ( 'NONE',  ( 11.37103032197929942, -3.416314376401300201, 8.316248703309600643 ) ) ;
#34979=CARTESIAN_POINT ( 'NONE',  ( 9.233265421555000074, -4.162714371335800578, 6.658304367510099908 ) ) ;
#35101=CARTESIAN_POINT ( 'NONE',  ( 9.883380199233998908, -3.139757597894699881, 7.608124715612800237 ) ) ;
#35107=CARTESIAN_POINT ( 'NONE',  ( 12.09999999999999964, -5.499854772664000357, 7.174999999999999822 ) ) ;
#35134=ORIENTED_EDGE ( 'NONE', *, *, #63072, .F. ) ;
#35143=CARTESIAN_POINT ( 'NONE',  ( 10.53696314287999947, -2.882742046518000034, 7.735518817439499983 ) ) ;
#35184=CARTESIAN_POINT ( 'NONE',  ( 10.29184687351666838, -4.999583552997724389, 8.268183399968647151 ) ) ;
#35217=CARTESIAN_POINT ( 'NONE',  ( 11.26841504065830080, -3.085489673376300424, 8.181880472491098288 ) ) ;
#35255=CARTESIAN_POINT ( 'NONE',  ( 9.499417874594000111, -5.050800927762999493, 7.053287723251499663 ) ) ;
#35258=CARTESIAN_POINT ( 'NONE',  ( 11.19041504065829962, -2.975441626403999784, 8.263934892306599167 ) ) ;
#35268=CARTESIAN_POINT ( 'NONE',  ( 10.94841638348500013, -5.108333310975999630, 7.769976643522699788 ) ) ;
#35271=B_SPLINE_CURVE_WITH_KNOTS ( 'NONE', 3,
 ( #62327, #68941, #25612, #51831, #35762, #41688 ),
 .UNSPECIFIED., .F., .F.,
 ( 4, 1, 1, 4 ),
 ( 0.000000000000000000, 0.3333333333333000081, 0.6666666666667000474, 1.000000000000000000 ),
 .UNSPECIFIED. ) ;
#35295=B_SPLINE_CURVE_WITH_KNOTS ( 'NONE', 3,
 ( #1411, #13638, #12947, #18188 ),
 .UNSPECIFIED., .F., .F.,
 ( 4, 4 ),
 ( 0.8163836489557148024, 1.000000000000000000 ),
 .UNSPECIFIED. ) ;
#35305=CARTESIAN_POINT ( 'NONE',  ( 11.10235971519489873, -3.394698737128500010, 8.506961598696999971 ) ) ;
#35319=CARTESIAN_POINT ( 'NONE',  ( 12.09999999999999787, -3.983295036746753670, 8.547709597963841333 ) ) ;
#35344=CARTESIAN_POINT ( 'NONE',  ( 11.49410672858429905, -4.801902424331299990, 8.103244025831999764 ) ) ;
#35417=CARTESIAN_POINT ( 'NONE',  ( 12.06322412107030928, -3.945399343424460525, 8.532060764998998792 ) ) ;
#35432=CARTESIAN_POINT ( 'NONE',  ( 12.31056516821460001, -3.390321848206700128, 6.884701936848800052 ) ) ;
#35437=CARTESIAN_POINT ( 'NONE',  ( 10.61792546752099931, -4.864937374655599278, 7.559927309296559983 ) ) ;
#35447=CARTESIAN_POINT ( 'NONE',  ( 10.73976354018233437, -4.327184855449098144, 8.717465845835395299 ) ) ;
#35483=CARTESIAN_POINT ( 'NONE',  ( 9.726430433046999724, -4.971677342931100085, 8.099647887697699389 ) ) ;
#35485=CARTESIAN_POINT ( 'NONE',  ( 12.09999999999999964, -4.817420948848700313, 7.825000000000000178 ) ) ;
#35513=CIRCLE ( 'NONE', #28843, 0.7499999936418002555 ) ;
#35555=CARTESIAN_POINT ( 'NONE',  ( 9.469356963619999235, -5.119357025014000584, 7.500000000085178087 ) ) ;
#35559=CARTESIAN_POINT ( 'NONE',  ( 12.12994988689360021, -3.481863023525599843, 6.483720595741000459 ) ) ;
#35588=CARTESIAN_POINT ( 'NONE',  ( 11.50000000000000000, -3.008232475376599879, 7.825000000000000178 ) ) ;
#35598=CARTESIAN_POINT ( 'NONE',  ( 10.45991290906800053, -4.809406943772300380, 6.509421987543800192 ) ) ;
#35610=CARTESIAN_POINT ( 'NONE',  ( 11.18035971519489813, -3.321859513918399731, 8.628134814664999652 ) ) ;
#35612=CARTESIAN_POINT ( 'NONE',  ( 10.99764694612700033, -5.059486515935999407, 7.077178005756699974 ) ) ;
#35613=CARTESIAN_POINT ( 'NONE',  ( 10.82169598649000086, -3.233475335853099875, 7.043598424555200133 ) ) ;
#35639=CARTESIAN_POINT ( 'NONE',  ( 10.64393020684899938, -2.750000000000000000, 7.500000000000000000 ) ) ;
#35648=CARTESIAN_POINT ( 'NONE',  ( 11.60101463001529964, -3.377766160221900016, 8.496586578655598743 ) ) ;
#35660=CARTESIAN_POINT ( 'NONE',  ( 12.09999999999999787, -3.636382150325344842, 8.530211724564091824 ) ) ;
#35674=ORIENTED_EDGE ( 'NONE', *, *, #33224, .T. ) ;
#35685=CARTESIAN_POINT ( 'NONE',  ( 10.80903300763299946, -3.402282662142699809, 6.873077781830399857 ) ) ;
#35697=VERTEX_POINT ( 'NONE', #50074 ) ;
#35711=CARTESIAN_POINT ( 'NONE',  ( 9.522188178962254668, -4.591134893453497234, 6.476088678109181984 ) ) ;
#35726=CARTESIAN_POINT ( 'NONE',  ( 11.32595391537419971, -3.283439621430300104, 7.013338090450799811 ) ) ;
#35739=DIRECTION ( 'NONE',  ( -1.000000000000000000, 0.000000000000000000, 0.000000000000000000 ) ) ;
#35756=CARTESIAN_POINT ( 'NONE',  ( 11.81900581613029999, -3.249313226592100534, 7.017964743997199939 ) ) ;
#35762=CARTESIAN_POINT ( 'NONE',  ( 11.51811411617009817, -5.026960591456000493, 7.174999999999999822 ) ) ;
#35764=CARTESIAN_POINT ( 'NONE',  ( 9.548601287889788125, -3.999999532294070459, 6.301404677806389465 ) ) ;
#35772=CARTESIAN_POINT ( 'NONE',  ( 12.26133460557259980, -3.860150918677800025, 6.645166161828299778 ) ) ;
#35777=CARTESIAN_POINT ( 'NONE',  ( 9.782063610505000284, -3.644370728184199937, 6.709281487801199262 ) ) ;
#35783=DIRECTION ( 'NONE',  ( 0.000000000000000000, 0.000000000000000000, -1.000000000000000000 ) ) ;
#35817=CARTESIAN_POINT ( 'NONE',  ( 10.38498825978699891, -4.149395984695000372, 6.368003848175999515 ) ) ;
#35835=ORIENTED_EDGE ( 'NONE', *, *, #33277, .T. ) ;
#35842=DIRECTION ( 'NONE',  ( -1.000000000000000000, 0.000000000000000000, 0.000000000000000000 ) ) ;
#35875=CARTESIAN_POINT ( 'NONE',  ( 9.349999778958000718, -4.000000000000000000, 6.500000166194499940 ) ) ;
#35876=EDGE_CURVE ( 'NONE', #6623, #46086, #17402, .T. ) ;
#35890=CARTESIAN_POINT ( 'NONE',  ( 11.12072335273220069, -3.602909566644000083, 6.430603299050000388 ) ) ;
#35929=CARTESIAN_POINT ( 'NONE',  ( 10.38392546752099932, -5.276153033933000280, 7.588418444866789514 ) ) ;
#35935=CARTESIAN_POINT ( 'NONE',  ( 9.904346873515667227, -5.250000000000000888, 7.336375382625536901 ) ) ;
#35940=CARTESIAN_POINT ( 'NONE',  ( 11.55435090131019926, -2.880552878538999995, 6.807613609764599616 ) ) ;
#35942=CARTESIAN_POINT ( 'NONE',  ( 11.61302897915239818, -3.708003626182200030, 6.397263297997000109 ) ) ;
#35976=CARTESIAN_POINT ( 'NONE',  ( 11.39324174884020024, -4.032306468273969990, 6.325557131097000685 ) ) ;
#35984=ORIENTED_EDGE ( 'NONE', *, *, #68496, .T. ) ;
#35992=CARTESIAN_POINT ( 'NONE',  ( 12.10000000000000142, -2.912667852269568147, 8.017651347927678529 ) ) ;
#36017=CARTESIAN_POINT ( 'NONE',  ( 11.07980110216399972, -4.739241740354600552, 7.951464549725199227 ) ) ;
#36045=( LENGTH_UNIT ( ) NAMED_UNIT ( * ) SI_UNIT ( .MILLI., .METRE. ) );
#36050=B_SPLINE_CURVE_WITH_KNOTS ( 'NONE', 3,
 ( #57979, #47491, #10076, #31413, #47146, #52729, #4824, #32107, #10418, #20227 ),
 .UNSPECIFIED., .F., .F.,
 ( 4, 2, 2, 2, 4 ),
 ( 0.000000000000000000, 0.2499999999999997780, 0.4999999999999995559, 0.7499999999999997780, 1.000000000000000000 ),
 .UNSPECIFIED. ) ;
#36053=EDGE_CURVE ( 'NONE', #11254, #41424, #40674, .T. ) ;
#36062=CARTESIAN_POINT ( 'NONE',  ( 11.20287750876920008, -4.469200303112399908, 6.771886227364699806 ) ) ;
#36076=DIRECTION ( 'NONE',  ( 0.000000000000000000, -1.000000000000000000, 0.000000000000000000 ) ) ;
#36094=CARTESIAN_POINT ( 'NONE',  ( 11.73589666366019912, -4.039600775206940497, 6.608753462694600067 ) ) ;
#36110=ORIENTED_EDGE ( 'NONE', *, *, #21140, .F. ) ;
#36156=CARTESIAN_POINT ( 'NONE',  ( 9.599784697134998268, -3.380386586585000241, 8.459069166353199165 ) ) ;
#36165=CARTESIAN_POINT ( 'NONE',  ( 12.09999999999999964, -4.883784007588900522, 7.174999999999999822 ) ) ;
#36172=CARTESIAN_POINT ( 'NONE',  ( 11.03976354018315753, -3.672815144550900524, 6.282534154164603812 ) ) ;
#36192=ORIENTED_EDGE ( 'NONE', *, *, #46755, .T. ) ;
#36233=CARTESIAN_POINT ( 'NONE',  ( 11.01810807141099957, -3.940954591493389891, 6.223352037434000117 ) ) ;
#36242=FACE_OUTER_BOUND ( 'NONE', #68777, .T. ) ;
#36263=EDGE_CURVE ( 'NONE', #50471, #57705, #38189, .T. ) ;
#36271=CARTESIAN_POINT ( 'NONE',  ( 10.02931740696899965, -3.762080884004200154, 6.243107450209000042 ) ) ;
#36282=CARTESIAN_POINT ( 'NONE',  ( 12.26588784977539959, -5.120865761890000201, 7.564049652083489228 ) ) ;
#36284=CARTESIAN_POINT ( 'NONE',  ( 11.16995391537419913, -3.056324258617099776, 6.859089544950699668 ) ) ;
#36298=FACE_OUTER_BOUND ( 'NONE', #28913, .T. ) ;
#36322=CARTESIAN_POINT ( 'NONE',  ( 11.88678751119029897, -5.166297436425000278, 6.889827023674499173 ) ) ;
#36363=CARTESIAN_POINT ( 'NONE',  ( 11.69102897915239936, -3.743141152489600110, 6.529961657816500065 ) ) ;
#36407=CARTESIAN_POINT ( 'NONE',  ( 12.35159063708299954, -3.174974693948799942, 7.268038553423699533 ) ) ;
#36436=CARTESIAN_POINT ( 'NONE',  ( 11.01925056272500036, -2.825232917634000085, 7.482589369563879877 ) ) ;
#36450=VERTEX_POINT ( 'NONE', #35555 ) ;
#36452=CARTESIAN_POINT ( 'NONE',  ( 11.05518582084300050, -4.566724035220099509, 8.155074391384399490 ) ) ;
#36498=CARTESIAN_POINT ( 'NONE',  ( 10.28165911260399845, -4.436443689698799986, 6.595367916746299741 ) ) ;
#36514=CARTESIAN_POINT ( 'NONE',  ( 11.13351354018304740, -2.750000000000000000, 7.336375382625529795 ) ) ;
#36523=DIRECTION ( 'NONE',  ( 1.000000000000000000, 0.000000000000000000, -0.000000000000000000 ) ) ;
#36580=CARTESIAN_POINT ( 'NONE',  ( 10.80072469555900128, -3.429147315060100176, 8.487632181750699445 ) ) ;
#36619=CARTESIAN_POINT ( 'NONE',  ( 9.852013376692999813, -5.140392946802999852, 8.079558723821699928 ) ) ;
#36623=CARTESIAN_POINT ( 'NONE',  ( 10.77195525820100031, -4.120672149427799802, 8.772302877803999976 ) ) ;
#36632=CARTESIAN_POINT ( 'NONE',  ( 11.51790547754520055, -2.825704134258000266, 7.462730980357120458 ) ) ;
#36634=CARTESIAN_POINT ( 'NONE',  ( 11.26841504065830080, -3.085489673376300424, 8.181880472491098288 ) ) ;
#36658=DIRECTION ( 'NONE',  ( 0.000000000000000000, 1.000000000000000000, 0.000000000000000000 ) ) ;
#36673=CARTESIAN_POINT ( 'NONE',  ( 11.85034208742530026, -4.630634088820300143, 6.508707709313799050 ) ) ;
#36697=VERTEX_POINT ( 'NONE', #46475 ) ;
#36715=CARTESIAN_POINT ( 'NONE',  ( 11.93718179236249988, -4.209680326224799707, 8.481317998227099864 ) ) ;
#36729=DIRECTION ( 'NONE',  ( 0.000000000000000000, 0.8514543052404082157, -0.5244287998266055073 ) ) ;
#36759=CARTESIAN_POINT ( 'NONE',  ( 11.89210538575740017, -3.157545584346100220, 7.701417844014099678 ) ) ;
#36788=CARTESIAN_POINT ( 'NONE',  ( 10.94125056272499918, -2.966599088466999934, 7.484684486284700178 ) ) ;
#36801=DIRECTION ( 'NONE',  ( -1.000000000000000000, 0.000000000000000000, -3.164702532202999971E-14 ) ) ;
#36805=CARTESIAN_POINT ( 'NONE',  ( 11.96179707368349909, -4.498457171163099844, 8.370914060838998694 ) ) ;
#36850=CARTESIAN_POINT ( 'NONE',  ( 9.800405316139999101, -4.213249376011100722, 6.518487389810699639 ) ) ;
#36889=B_SPLINE_CURVE_WITH_KNOTS ( 'NONE', 3,
 ( #30665, #68390, #41836, #57219, #45716, #19135 ),
 .UNSPECIFIED., .F., .F.,
 ( 4, 2, 4 ),
 ( 0.000000000000000000, 0.5000000000000000000, 1.000000000000000000 ),
 .UNSPECIFIED. ) ;
#36903=CARTESIAN_POINT ( 'NONE',  ( 9.332144816391007680, -3.783447583457012264, 6.534094574943864586 ) ) ;
#36932=CARTESIAN_POINT ( 'NONE',  ( 11.90425819896749893, -5.255890247626999745, 7.263238376356399684 ) ) ;
#36980=CARTESIAN_POINT ( 'NONE',  ( 11.22191429142990060, -3.974927396630719922, 8.816028813488999916 ) ) ;
#36982=CARTESIAN_POINT ( 'NONE',  ( 10.72272469555899832, -3.360453478306600239, 8.606479382885998675 ) ) ;
#36989=ORIENTED_EDGE ( 'NONE', *, *, #1401, .T. ) ;
#37001=FACE_OUTER_BOUND ( 'NONE', #39506, .T. ) ;
#37018=CARTESIAN_POINT ( 'NONE',  ( 11.02946886766499901, -4.430164648092599577, 8.281567006984099422 ) ) ;
#37055=CARTESIAN_POINT ( 'NONE',  ( 12.12994988689360021, -3.481863023525599843, 6.483720595741000459 ) ) ;
#37064=CARTESIAN_POINT ( 'NONE',  ( 11.30502344389999969, -5.125258734743999511, 8.182900850620900002 ) ) ;
#37100=CARTESIAN_POINT ( 'NONE',  ( 11.37518447801629939, -3.134012688501500055, 7.519093628927509876 ) ) ;
#37131=CARTESIAN_POINT ( 'NONE',  ( 9.803275160948500044, -5.099670516381894281, 8.115397037630309285 ) ) ;
#37144=CARTESIAN_POINT ( 'NONE',  ( 11.86749010443640096, -3.136214309321499805, 7.435402237490909449 ) ) ;
#37188=CARTESIAN_POINT ( 'NONE',  ( 10.81357120343299982, -4.048688523195909994, 6.496769302834999316 ) ) ;
#37268=CARTESIAN_POINT ( 'NONE',  ( 11.97810404293059960, -4.563346034752700398, 6.352848032645000309 ) ) ;
#37279=B_SPLINE_SURFACE_WITH_KNOTS ( 'NONE', 3, 3, ( 
 ( #11380, #7184, #27474, #43558, #38651, #6483, #34109, #1249, #43905, #18030, #33066, #22563, #17681, #1593, #2285, #50182, #54733, #28521, #23603, #12432, #49832, #44262, #32721, #54033, #65208, #11724, #12780, #39344, #59974, #65558, #17325, #48799, #60324, #12084, #55428, #49481, #16969, #7519, #16630, #64510, #60665, #33415, #39006, #6833, #37958, #59278, #6135, #908, #28165, #22221, #33763, #38300, #59630, #54382, #27832, #55078, #23264, #44608, #65902, #24294, #51885, #67612, #45963, #13812, #19045, #13132, #51212 ),
 ( #61014, #34460, #50868, #61356, #62381, #19739, #40373, #3308, #66935, #29211, #40713, #29566, #14498, #29907, #23953, #57134, #66249, #3980, #41061, #35143, #24643, #2965, #9231, #18371, #44945, #35817, #45631, #8218, #55773, #8901, #56455, #39693, #61694, #34796, #67273, #8560, #7876, #51545, #66593, #3641, #24978, #56107, #30570, #19388, #62040, #50522, #2622, #45287, #18712, #40045, #14156, #35483, #46312, #13477, #56804, #30241, #36156, #57469, #126, #20418, #63746, #68299, #57819, #9576, #30918, #41746, #52231 ),
 ( #42435, #10963, #15858, #32303, #31604, #37188, #9928, #63048, #53611, #48023, #15523, #26709, #47687, #58507, #63402, #26361, #4670, #68646, #46658, #58853, #21443, #5371, #10612, #14836, #15174, #46997, #36498, #31266, #52576, #42778, #4331, #25665, #31952, #26012, #41407, #25320, #53269, #47341, #67963, #37527, #20764, #42094, #20078, #62713, #21110, #36850, #64085, #16203, #58170, #10271, #52926, #5022, #68998, #53948, #49058, #16888, #44524, #59544, #54294, #28434, #43477, #11639, #28083, #11995, #12691, #60586, #65118 ),
 ( #38922, #33332, #21787, #64425, #32980, #22136, #23175, #49748, #1164, #54649, #27745, #59196, #1508, #6396, #65819, #59886, #6051, #17943, #27050, #34028, #1857, #43821, #6743, #22479, #39263, #48363, #5709, #470, #17241, #38215, #43121, #60243, #38563, #16547, #49397, #64774, #22826, #44174, #37877, #12345, #27390, #33678, #54996, #65470, #11298, #17595, #7097, #32638, #48717, #819, #29130, #34374, #56378, #50790, #56725, #60933, #2885, #50438, #66168, #18287, #30164, #2540, #24560, #23867, #18631, #39606, #13045 ) ),
 .UNSPECIFIED., .F., .F., .F.,
 ( 4, 4 ),
 ( 4, 1, 1, 1, 1, 1, 1, 1, 1, 1, 1, 1, 1, 1, 1, 1, 1, 1, 1, 1, 1, 1, 1, 1, 1, 1, 1, 1, 1, 1, 1, 1, 1, 1, 1, 1, 1, 1, 1, 1, 1, 1, 1, 1, 1, 1, 1, 1, 1, 1, 1, 1, 1, 1, 1, 1, 1, 1, 1, 1, 1, 1, 1, 1, 4 ),
 ( -0.02000000000000000042, 1.020000000000000018 ),
 ( -0.02000000000000000042, -0.003749999999999999861, 0.01250000000000000069, 0.02875000000000000125, 0.04499999999999999833, 0.06124999999999999889, 0.07749999999999999944, 0.09375000000000000000, 0.1100000000000000006, 0.1262500000000000011, 0.1424999999999999878, 0.1587500000000000022, 0.1749999999999999889, 0.1912500000000000033, 0.2074999999999999900, 0.2237500000000000044, 0.2399999999999999911, 0.2562499999999999778, 0.2725000000000000200, 0.2887500000000000067, 0.3049999999999999933, 0.3212499999999999800, 0.3375000000000000222, 0.3537500000000000089, 0.3699999999999999956, 0.3862499999999999822, 0.4025000000000000244, 0.4187500000000000111, 0.4349999999999999978, 0.4512499999999999845, 0.4675000000000000266, 0.4837500000000000133, 0.5000000000000000000, 0.5162499999999999867, 0.5324999999999999734, 0.5487499999999999600, 0.5649999999999999467, 0.5812500000000000444, 0.5975000000000000311, 0.6137500000000000178, 0.6300000000000000044, 0.6462499999999999911, 0.6624999999999999778, 0.6787499999999999645, 0.6949999999999999512, 0.7112500000000000488, 0.7275000000000000355, 0.7437500000000000222, 0.7600000000000000089, 0.7762499999999999956, 0.7924999999999999822, 0.8087499999999999689, 0.8249999999999999556, 0.8412500000000000533, 0.8575000000000000400, 0.8737500000000000266, 0.8900000000000000133, 0.9062500000000000000, 0.9224999999999999867, 0.9387499999999999734, 0.9549999999999999600, 0.9712499999999999467, 0.9875000000000000444, 1.003749999999999920, 1.020000000000000018 ),
 .UNSPECIFIED. ) ;
#37302=CARTESIAN_POINT ( 'NONE',  ( 9.497405316140000053, -4.271593136661399726, 6.249951378708000327 ) ) ;
#37315=CARTESIAN_POINT ( 'NONE',  ( 10.19809687351667016, -3.672815144550895639, 8.717465845835397076 ) ) ;
#37318=CARTESIAN_POINT ( 'NONE',  ( 11.85502763632550050, -5.160433036184000066, 8.035454525731699604 ) ) ;
#37351=CARTESIAN_POINT ( 'NONE',  ( 11.77234208742519961, -4.554746427620499638, 6.627995351445298944 ) ) ;
#37392=CARTESIAN_POINT ( 'NONE',  ( 12.20379573085659963, -2.893744357957000357, 7.308581953418300081 ) ) ;
#37395=ORIENTED_EDGE ( 'NONE', *, *, #63072, .T. ) ;
#37401=CARTESIAN_POINT ( 'NONE',  ( 12.18277869730536977, -4.531392946702499813, 8.547856079839998955 ) ) ;
#37434=CARTESIAN_POINT ( 'NONE',  ( 11.51872200990539952, -4.947480442174099657, 7.830502140005199507 ) ) ;
#37480=CARTESIAN_POINT ( 'NONE',  ( 11.27672335273219950, -3.698477709264200275, 6.687976048055599421 ) ) ;
#37527=CARTESIAN_POINT ( 'NONE',  ( 9.952380199233999747, -3.003429752324399793, 7.625259896924899472 ) ) ;
#37533=CARTESIAN_POINT ( 'NONE',  ( 9.893930206848999376, -5.250000000000000000, 7.500000000000000000 ) ) ;
#37555=DIRECTION ( 'NONE',  ( -1.000000000000000000, 0.000000000000000000, -1.233561263588000078E-14 ) ) ;
#37569=FACE_OUTER_BOUND ( 'NONE', #15982, .T. ) ;
#37603=CARTESIAN_POINT ( 'NONE',  ( 11.50000000000000000, -5.058572498595999889, 7.174999999999999822 ) ) ;
#37607=CARTESIAN_POINT ( 'NONE',  ( 11.92887348028849992, -5.124210964533999935, 6.892162778124999889 ) ) ;
#37613=DIRECTION ( 'NONE',  ( -1.000000000000000000, 0.000000000000000000, 0.000000000000000000 ) ) ;
#37618=EDGE_LOOP ( 'NONE', ( #47951, #43353, #28510, #65952, #35674, #4088, #708, #65857, #4565, #23457, #60789, #33281 ) ) ;
#37644=EDGE_CURVE ( 'NONE', #61281, #11902, #55529, .T. ) ;
#37659=CARTESIAN_POINT ( 'NONE',  ( 11.33810672858430024, -5.021298157087000114, 8.268288002587098617 ) ) ;
#37695=CARTESIAN_POINT ( 'NONE',  ( 11.52812378248509795, -4.416893162838900544, 8.288725998710999576 ) ) ;
#37728=ADVANCED_FACE ( 'NONE', ( #7098 ), #23970, .F. ) ;
#37737=CARTESIAN_POINT ( 'NONE',  ( 11.32179975933729921, -3.051121678931899783, 7.826467126457498757 ) ) ;
#37742=CARTESIAN_POINT ( 'NONE',  ( 11.55435090131019926, -2.880552878538999995, 6.807613609764599616 ) ) ;
#37751=ADVANCED_FACE ( 'NONE', ( #66857 ), #14077, .F. ) ;
#37779=CARTESIAN_POINT ( 'NONE',  ( 11.14949279009019989, -4.260984538213099526, 6.531063508962500208 ) ) ;
#37803=B_SPLINE_CURVE_WITH_KNOTS ( 'NONE', 3,
 ( #35639, #57280, #46120, #56610 ),
 .UNSPECIFIED., .F., .F.,
 ( 4, 4 ),
 ( 0.000000000000000000, 1.000000000000000000 ),
 .UNSPECIFIED. ) ;
#37805=CARTESIAN_POINT ( 'NONE',  ( 10.87581074856900010, -5.172583146916752028, 6.999756549658378901 ) ) ;
#37815=CARTESIAN_POINT ( 'NONE',  ( 9.762620115047001335, -4.656877754660387225, 8.575407073603340535 ) ) ;
#37825=CARTESIAN_POINT ( 'NONE',  ( 11.35056919669530018, -3.169300617545700138, 7.254567470917099747 ) ) ;
#37877=CARTESIAN_POINT ( 'NONE',  ( 9.899709346416999622, -3.216804796119200116, 7.871904849557299855 ) ) ;
#37891=CARTESIAN_POINT ( 'NONE',  ( 10.85376078907948028, -3.141705924399422312, 7.334408124199476298 ) ) ;
#37904=CARTESIAN_POINT ( 'NONE',  ( 10.48976354018275003, -3.672815144550900524, 6.282534154164604701 ) ) ;
#37958=CARTESIAN_POINT ( 'NONE',  ( 9.981734463323000739, -3.866750753272200303, 6.227746477418000026 ) ) ;
#38000=CARTESIAN_POINT ( 'NONE',  ( 10.69810941423799910, -3.053977294209000437, 8.359277272599898723 ) ) ;
#38035=CARTESIAN_POINT ( 'NONE',  ( 11.23724174883999893, -4.024531238983009906, 6.608211443991299561 ) ) ;
#38073=CARTESIAN_POINT ( 'NONE',  ( 11.76072066707849828, -3.023932655881500065, 8.090408888831799317 ) ) ;
#38080=CARTESIAN_POINT ( 'NONE',  ( 12.25203632436370071, -5.109717061557999429, 7.759151359668400083 ) ) ;
#38110=CARTESIAN_POINT ( 'NONE',  ( 10.48677454732762726, -3.921486932049647489, 8.371417217572535208 ) ) ;
#38141=CARTESIAN_POINT ( 'NONE',  ( 10.92363156114900136, -4.684311564990209398, 6.424401362931539516 ) ) ;
#38161=CARTESIAN_POINT ( 'NONE',  ( 11.78949010443639978, -2.999324937259999935, 7.425165037173959703 ) ) ;
#38174=CARTESIAN_POINT ( 'NONE',  ( 9.599999931441001166, -2.935682118448999844, 6.844464000216799349 ) ) ;
#38189=B_SPLINE_CURVE_WITH_KNOTS ( 'NONE', 3,
 ( #30997, #57202, #9305, #40784 ),
 .UNSPECIFIED., .F., .F.,
 ( 4, 4 ),
 ( 0.000000000000000000, 0.1836163425310833319 ),
 .UNSPECIFIED. ) ;
#38215=CARTESIAN_POINT ( 'NONE',  ( 10.12767167105699961, -4.855035690642299784, 7.356396684460199786 ) ) ;
#38234=CARTESIAN_POINT ( 'NONE',  ( 12.03979707368350027, -4.430269712815499972, 8.251775607861899786 ) ) ;
#38245=CARTESIAN_POINT ( 'NONE',  ( 10.47934687351612659, -3.836375382625532904, 6.249999999999999112 ) ) ;
#38246=DIRECTION ( 'NONE',  ( 0.000000000000000000, 1.000000000000000000, 0.000000000000000000 ) ) ;
#38249=ORIENTED_EDGE ( 'NONE', *, *, #40725, .T. ) ;
#38300=CARTESIAN_POINT ( 'NONE',  ( 9.804430433047000903, -5.088604610742000212, 8.171806809244198888 ) ) ;
#38347=CARTESIAN_POINT ( 'NONE',  ( 11.09195391537400077, -2.942766577210000012, 6.781965272201699868 ) ) ;
#38353=CARTESIAN_POINT ( 'NONE',  ( 10.08351354018333446, -2.750000000000000000, 7.336375382625531572 ) ) ;
#38362=CARTESIAN_POINT ( 'NONE',  ( 11.95284386393252873, -3.097320422761385750, 7.824986766837089824 ) ) ;
#38375=CARTESIAN_POINT ( 'NONE',  ( 11.73052404082913469, -5.045680872279848295, 7.824990945864982450 ) ) ;
#38422=CARTESIAN_POINT ( 'NONE',  ( 11.85918179236250047, -4.238363971154499588, 8.615559381441000752 ) ) ;
#38431=CARTESIAN_POINT ( 'NONE',  ( 11.55946005378019947, -2.963614890480000152, 8.053412743695298914 ) ) ;
#38533=ORIENTED_EDGE ( 'NONE', *, *, #16520, .T. ) ;
#38563=CARTESIAN_POINT ( 'NONE',  ( 10.05168422951000018, -4.611171355610000688, 8.114961396014498618 ) ) ;
#38582=CARTESIAN_POINT ( 'NONE',  ( 10.47363156114899851, -4.684311564990208510, 6.424401362931538628 ) ) ;
#38605=DIRECTION ( 'NONE',  ( 0.7071067617951957152, 0.000000000000000000, -0.7071068005778986532 ) ) ;
#38613=CARTESIAN_POINT ( 'NONE',  ( 10.25851354018233152, -3.836375382625526687, 8.749999999999996447 ) ) ;
#38645=CARTESIAN_POINT ( 'NONE',  ( 10.84580110216399973, -5.090698144635000588, 8.166103548914600552 ) ) ;
#38651=CARTESIAN_POINT ( 'NONE',  ( 10.99490035061499960, -3.659038130401700339, 6.267064942904999825 ) ) ;
#38773=CARTESIAN_POINT ( 'NONE',  ( 10.23396314288000042, -2.882742046518000034, 7.735518817439499983 ) ) ;
#38776=CARTESIAN_POINT ( 'NONE',  ( 11.83041235500449950, -4.942357465271699724, 8.363295307663500822 ) ) ;
#38783=CARTESIAN_POINT ( 'NONE',  ( 12.17403632436368888, -4.976178716761900489, 7.727966254184200245 ) ) ;
#38814=CARTESIAN_POINT ( 'NONE',  ( 10.41078710578162791, -3.243350240173176413, 7.939332914627393656 ) ) ;
#38836=CARTESIAN_POINT ( 'NONE',  ( 9.326138961223998436, -3.281636118526699786, 7.014550357332099750 ) ) ;
#38882=CARTESIAN_POINT ( 'NONE',  ( 10.78976354018291239, -4.327184855449096368, 8.717465845835395299 ) ) ;
#38922=CARTESIAN_POINT ( 'NONE',  ( 10.83688779216199904, -3.198058499272899979, 7.210800365544999480 ) ) ;
#38924=CARTESIAN_POINT ( 'NONE',  ( 11.27934687351631382, -4.163624617374463988, 8.750000000000001776 ) ) ;
#39006=CARTESIAN_POINT ( 'NONE',  ( 10.03239275768699912, -3.136549968260000210, 6.556157624301499176 ) ) ;
#39017=CARTESIAN_POINT ( 'NONE',  ( 11.63220574173980992, -2.863826994586552654, 8.088082908809447247 ) ) ;
#39025=EDGE_CURVE ( 'NONE', #61432, #68324, #16231, .T. ) ;
#39030=CARTESIAN_POINT ( 'NONE',  ( 12.07240408529959907, -4.732472998177641443, 7.982112976485220557 ) ) ;
#39079=CARTESIAN_POINT ( 'NONE',  ( 10.95257053952200010, -4.394359323863099576, 8.422730500489899796 ) ) ;
#39082=CYLINDRICAL_SURFACE ( 'NONE', #17588, 1.250000000000000222 ) ;
#39117=CARTESIAN_POINT ( 'NONE',  ( 10.68144474310099845, -2.984290294633999974, 7.007085334055199510 ) ) ;
#39120=CARTESIAN_POINT ( 'NONE',  ( 11.04687750876899877, -4.617914354660699772, 6.541108991297599928 ) ) ;
#39128=CARTESIAN_POINT ( 'NONE',  ( 11.98522412107029922, -3.952868550833580130, 8.390877922225699947 ) ) ;
#39159=CARTESIAN_POINT ( 'NONE',  ( 10.38545795859862686, -3.143868186573851364, 7.680473230592850697 ) ) ;
#39178=CARTESIAN_POINT ( 'NONE',  ( 10.08400081823899974, -4.888721525563999748, 7.032008172796599510 ) ) ;
#39184=CARTESIAN_POINT ( 'NONE',  ( 9.456149159797570647, -5.077028306801780744, 7.790330864865199878 ) ) ;
#39263=CARTESIAN_POINT ( 'NONE',  ( 10.25431740696899929, -3.838745722419000028, 6.648116790593900483 ) ) ;
#39283=CARTESIAN_POINT ( 'NONE',  ( 11.62133729122639991, -4.865898216891100247, 7.522778681411049995 ) ) ;
#39343=CARTESIAN_POINT ( 'NONE',  ( 11.50000000000000000, -4.968589424331200100, 7.825000000000000178 ) ) ;
#39344=CARTESIAN_POINT ( 'NONE',  ( 10.41232996542199984, -4.888489908445900589, 6.579690231462300254 ) ) ;
#39392=EDGE_CURVE ( 'NONE', #24287, #50813, #63696, .T. ) ;
#39423=CARTESIAN_POINT ( 'NONE',  ( 11.96179707368349909, -4.498457171163099844, 8.370914060838998694 ) ) ;
#39455=EDGE_LOOP ( 'NONE', ( #26598, #65537, #58643, #27180 ) ) ;
#39462=CARTESIAN_POINT ( 'NONE',  ( 9.828696787963000503, -3.803923679411099990, 8.624850445389000697 ) ) ;
#39465=CARTESIAN_POINT ( 'NONE',  ( 12.02733460557258915, -3.793662715184400014, 6.238754009183999472 ) ) ;
#39474=CARTESIAN_POINT ( 'NONE',  ( 11.98225819896750011, -5.120994791668000090, 7.288668995979000087 ) ) ;
#39475=CARTESIAN_POINT ( 'NONE',  ( 11.94366954483529852, -3.514796851401900124, 8.248643701125299543 ) ) ;
#39506=EDGE_LOOP ( 'NONE', ( #35984, #62504, #16221, #27862 ) ) ;
#39525=CARTESIAN_POINT ( 'NONE',  ( 9.300809814040999157, -3.469640109842400122, 6.814123855771700100 ) ) ;
#39531=CARTESIAN_POINT ( 'NONE',  ( 9.442941355974877382, -4.954666522228584391, 8.051224688103600258 ) ) ;
#39606=CARTESIAN_POINT ( 'NONE',  ( 9.224265421554999733, -4.162714371335800578, 6.658304367510099908 ) ) ;
#39621=EDGE_CURVE ( 'NONE', #21925, #13467, #17886, .T. ) ;
#39622=EDGE_CURVE ( 'NONE', #11254, #11902, #39740, .T. ) ;
#39651=CARTESIAN_POINT ( 'NONE',  ( 11.52755399909320921, -3.866653594937912608, 6.221473734489903151 ) ) ;
#39678=CARTESIAN_POINT ( 'NONE',  ( 11.09393020684900044, -2.750000000000000000, 7.500000000000000000 ) ) ;
#39693=CARTESIAN_POINT ( 'NONE',  ( 10.23301337669299826, -5.017903082085999777, 8.017308190024898806 ) ) ;
#39740=LINE ( 'NONE', #7921, #9145 ) ;
#39747=FACE_OUTER_BOUND ( 'NONE', #18140, .T. ) ;
#39771=CARTESIAN_POINT ( 'NONE',  ( 11.93718179236249988, -4.209680326224799707, 8.481317998227099864 ) ) ;
#39794=CARTESIAN_POINT ( 'NONE',  ( 9.212681907068999365, -4.225805508133200661, 6.635485632555699453 ) ) ;
#39810=CARTESIAN_POINT ( 'NONE',  ( 9.248138961223999033, -3.167792625045000143, 6.937618199889199033 ) ) ;
#39813=CARTESIAN_POINT ( 'NONE',  ( 11.09610807141099897, -3.947296672195129918, 6.360477084256999980 ) ) ;
#39824=CARTESIAN_POINT ( 'NONE',  ( 11.51872200990539952, -4.947480442174099657, 7.830502140005199507 ) ) ;
#39825=CARTESIAN_POINT ( 'NONE',  ( 11.02435971519499880, -3.467537960339900138, 8.385788382729799650 ) ) ;
#39878=CARTESIAN_POINT ( 'NONE',  ( 9.805380199233999505, -3.003429752324399793, 7.625259896924899472 ) ) ;
#39993=CARTESIAN_POINT ( 'NONE',  ( 11.99056651104150006, -3.914543207408039738, 8.361971998931499783 ) ) ;
#40045=CARTESIAN_POINT ( 'NONE',  ( 9.777088727410999880, -5.137817193984000497, 7.404572115919599185 ) ) ;
#40092=CARTESIAN_POINT ( 'NONE',  ( 11.57299956498199833, -2.792989229543000107, 7.174999999999999822 ) ) ;
#40119=CARTESIAN_POINT ( 'NONE',  ( 11.88379707368349969, -4.566644629509899467, 8.490052513816499058 ) ) ;
#40157=CARTESIAN_POINT ( 'NONE',  ( 10.53791290906799993, -4.722468360609500593, 6.615820196229499572 ) ) ;
#40161=CARTESIAN_POINT ( 'NONE',  ( 11.58425954179440076, -3.017023678917100327, 6.683254058608399717 ) ) ;
#40170=CARTESIAN_POINT ( 'NONE',  ( 11.14949279009019989, -4.260984538213099526, 6.531063508962500208 ) ) ;
#40171=CARTESIAN_POINT ( 'NONE',  ( 11.65278751119019951, -4.790480620979200133, 7.086443476450299706 ) ) ;
#40188=EDGE_CURVE ( 'NONE', #67955, #46460, #29406, .T. ) ;
#40199=DIRECTION ( 'NONE',  ( 1.000000000000000000, 0.000000000000000000, 0.000000000000000000 ) ) ;
#40219=CARTESIAN_POINT ( 'NONE',  ( 10.43860887879199950, -4.227457260387500249, 8.478317686146800369 ) ) ;
#40225=CARTESIAN_POINT ( 'NONE',  ( 9.310863317747999801, -3.039136629551499880, 7.499999999926881600 ) ) ;
#40326=CARTESIAN_POINT ( 'NONE',  ( 12.13825819896753977, -4.851203879749700576, 7.339530235223699073 ) ) ;
#40331=CARTESIAN_POINT ( 'NONE',  ( 10.06068422951000052, -4.611171355610000688, 8.114961396014498618 ) ) ;
#40345=CARTESIAN_POINT ( 'NONE',  ( 0.000000000000000000, 0.000000000000000000, 0.000000000000000000 ) ) ;
#40373=CARTESIAN_POINT ( 'NONE',  ( 10.86624205625100004, -4.409476560233800413, 6.434137271007999814 ) ) ;
#40444=CARTESIAN_POINT ( 'NONE',  ( 11.41610672858429965, -4.911600290708499905, 8.185766014210599906 ) ) ;
#40484=CARTESIAN_POINT ( 'NONE',  ( 9.575405316139999456, -4.242421256336299962, 6.384219384258999597 ) ) ;
#40488=CARTESIAN_POINT ( 'NONE',  ( 11.21503032197930061, -3.256621462143499901, 8.539569492647999027 ) ) ;
#40497=CARTESIAN_POINT ( 'NONE',  ( 11.32179975933729921, -3.051121678931899783, 7.826467126457498757 ) ) ;
#40502=VECTOR ( 'NONE', #42920, 1000.000000000000000 ) ;
#40505=ORIENTED_EDGE ( 'NONE', *, *, #44565, .F. ) ;
#40534=CARTESIAN_POINT ( 'NONE',  ( 11.63746005378019888, -2.838900981960999825, 8.120007936598501175 ) ) ;
#40540=B_SPLINE_CURVE_WITH_KNOTS ( 'NONE', 3,
 ( #27201, #62864, #5861, #52383, #47843, #48521, #630, #31761, #5177, #52730 ),
 .UNSPECIFIED., .F., .F.,
 ( 4, 2, 2, 2, 4 ),
 ( 0.000000000000000000, 0.2500000000000004441, 0.5000000000000008882, 0.7500000000000004441, 1.000000000000000000 ),
 .UNSPECIFIED. ) ;
#40561=CARTESIAN_POINT ( 'NONE',  ( 11.86486084871759950, -5.207010770456999893, 7.174999999999999822 ) ) ;
#40574=CARTESIAN_POINT ( 'NONE',  ( 12.10948876160955479, -4.695527826393099957, 6.776679950459500112 ) ) ;
#40612=VERTEX_POINT ( 'NONE', #26982 ) ;
#40617=DIRECTION ( 'NONE',  ( -1.000000000000000000, 0.000000000000000000, 0.000000000000000000 ) ) ;
#40647=CARTESIAN_POINT ( 'NONE',  ( 11.90211496860029960, -3.206052520092899982, 7.906860999147899527 ) ) ;
#40674=B_SPLINE_CURVE_WITH_KNOTS ( 'NONE', 3,
 ( #12850, #55497, #12501, #50597 ),
 .UNSPECIFIED., .F., .F.,
 ( 4, 4 ),
 ( 0.000000000000000000, 1.000000000000000000 ),
 .UNSPECIFIED. ) ;
#40680=CARTESIAN_POINT ( 'NONE',  ( 10.61476354018233259, -2.782534154164604256, 7.827184855449092815 ) ) ;
#40713=CARTESIAN_POINT ( 'NONE',  ( 10.76492546752099955, -5.139081147506999514, 7.578921399676699089 ) ) ;
#40725=EDGE_CURVE ( 'NONE', #11902, #6623, #1902, .T. ) ;
#40726=LINE ( 'NONE', #68660, #23283 ) ;
#40773=VECTOR ( 'NONE', #62957, 1000.000000000000114 ) ;
#40784=CARTESIAN_POINT ( 'NONE',  ( 9.231616107288068918, -3.999997736744774546, 6.618420992905502231 ) ) ;
#40790=CARTESIAN_POINT ( 'NONE',  ( 10.71462282008599942, -3.476853648246800432, 6.656181553372300108 ) ) ;
#40827=CARTESIAN_POINT ( 'NONE',  ( 9.068822372493999140, -4.328199826929600036, 6.426348619097999482 ) ) ;
#40831=CARTESIAN_POINT ( 'NONE',  ( 11.09195391537400077, -2.942766577210000012, 6.781965272201699868 ) ) ;
#40834=CARTESIAN_POINT ( 'NONE',  ( 9.893930206848999376, -5.250000000000000000, 7.500000000000000000 ) ) ;
#40839=CARTESIAN_POINT ( 'NONE',  ( 11.05569598648999907, -2.869047858956000230, 6.826612223887499553 ) ) ;
#40841=CARTESIAN_POINT ( 'NONE',  ( 11.31764560330029923, -3.650429500487800460, 8.585859374935999710 ) ) ;
#40872=ADVANCED_FACE ( 'NONE', ( #49831 ), #34108, .T. ) ;
#40875=CARTESIAN_POINT ( 'NONE',  ( 9.272923981633081070, -3.689545703815816591, 6.685328252913995684 ) ) ;
#40882=CARTESIAN_POINT ( 'NONE',  ( 11.35168717260510007, -4.613789146762799831, 6.498190316041999814 ) ) ;
#40920=CARTESIAN_POINT ( 'NONE',  ( 10.83364828895399867, -3.239803852721999888, 7.084788038520800413 ) ) ;
#40968=CARTESIAN_POINT ( 'NONE',  ( 11.25210807141120029, -3.959980833595939664, 6.634727177901499573 ) ) ;
#40981=CARTESIAN_POINT ( 'NONE',  ( 9.270072224255999416, -3.906223101245800411, 6.613913699222099041 ) ) ;
#40995=VECTOR ( 'NONE', #44963, 1000.000000000000000 ) ;
#40997=CARTESIAN_POINT ( 'NONE',  ( 11.39835090130999973, -3.121033016283800254, 6.956352367771000189 ) ) ;
#41008=DIRECTION ( 'NONE',  ( 0.000000000000000000, -1.000000000000000000, 0.000000000000000000 ) ) ;
#41017=VERTEX_POINT ( 'NONE', #44088 ) ;
#41018=CARTESIAN_POINT ( 'NONE',  ( 9.832721904869998752, -3.243980311826100138, 7.075568408810499754 ) ) ;
#41061=CARTESIAN_POINT ( 'NONE',  ( 10.56229229006299875, -3.012566816337000297, 8.073332500201798823 ) ) ;
#41089=CARTESIAN_POINT ( 'NONE',  ( 9.099999952505998024, -4.000000000000000000, 7.500000000000000000 ) ) ;
#41144=CARTESIAN_POINT ( 'NONE',  ( 11.24379975933729980, -2.921317947059999920, 7.871126858273000515 ) ) ;
#41180=CARTESIAN_POINT ( 'NONE',  ( 9.474088727410999056, -5.137817193984000497, 7.404572115919599185 ) ) ;
#41185=CARTESIAN_POINT ( 'NONE',  ( 10.06059687351566723, -3.370476274536376771, 6.407767014557177454 ) ) ;
#41193=CARTESIAN_POINT ( 'NONE',  ( 12.05811496860034993, -2.954409148022000053, 8.035816473382100256 ) ) ;
#41195=CARTESIAN_POINT ( 'NONE',  ( 12.10118044953561878, -2.866798846279000390, 6.909094663619399945 ) ) ;
#41228=CARTESIAN_POINT ( 'NONE',  ( 12.14122412107036908, -3.937930136014310190, 8.673243607771999208 ) ) ;
#41242=CARTESIAN_POINT ( 'NONE',  ( 12.09999999999999964, -3.133991299512489892, 8.272804384030438385 ) ) ;
#41265=CARTESIAN_POINT ( 'NONE',  ( 11.32595391537419971, -3.283439621430300104, 7.013338090450799811 ) ) ;
#41298=PRESENTATION_STYLE_ASSIGNMENT (( #67167 ) ) ;
#41313=CARTESIAN_POINT ( 'NONE',  ( 11.52287616594230002, -4.261927842557799551, 8.325646653015098764 ) ) ;
#41327=CARTESIAN_POINT ( 'NONE',  ( 9.206426979769998908, -4.358851904410700584, 6.723921629386799381 ) ) ;
#41343=CARTESIAN_POINT ( 'NONE',  ( 11.10746886766490071, -4.498335456194499926, 8.405426684175299812 ) ) ;
#41366=CARTESIAN_POINT ( 'NONE',  ( 10.84588779216199939, -3.198058499272899979, 7.210800365544999480 ) ) ;
#41369=CARTESIAN_POINT ( 'NONE',  ( 11.43210843320491499, -5.137688304401064165, 6.901605483505058203 ) ) ;
#41407=CARTESIAN_POINT ( 'NONE',  ( 10.07902593514599943, -4.145841638824199649, 8.493766832166899761 ) ) ;
#41424=VERTEX_POINT ( 'NONE', #15700 ) ;
#41437=CARTESIAN_POINT ( 'NONE',  ( 10.34393020685000053, -5.250000000000000000, 7.500000000000000000 ) ) ;
#41467=CARTESIAN_POINT ( 'NONE',  ( 12.09999999999999964, -4.000000000000000000, 7.500000000000000000 ) ) ;
#41481=CARTESIAN_POINT ( 'NONE',  ( 10.70641772631199906, -3.568446272909699957, 6.611684804099500212 ) ) ;
#41516=CARTESIAN_POINT ( 'NONE',  ( 10.10530484851599908, -2.836617618740000069, 6.968092280137199168 ) ) ;
#41519=CARTESIAN_POINT ( 'NONE',  ( 10.79657053952199952, -4.502253688815499366, 8.675184076076000395 ) ) ;
#41526=CARTESIAN_POINT ( 'NONE',  ( 11.55946005378019947, -2.963614890480000152, 8.053412743695298914 ) ) ;
#41528=CARTESIAN_POINT ( 'NONE',  ( 11.76072066707849828, -3.023932655881500065, 8.090408888831799317 ) ) ;
#41529=CARTESIAN_POINT ( 'NONE',  ( 10.86325056272499978, -3.107965259299500183, 7.486779603004729111 ) ) ;
#41567=CARTESIAN_POINT ( 'NONE',  ( 12.09966954483535773, -3.361010663344000005, 8.485927942460499196 ) ) ;
#41610=CARTESIAN_POINT ( 'NONE',  ( 10.78441772631200024, -3.627481539113199815, 6.733203680593099705 ) ) ;
#41651=CARTESIAN_POINT ( 'NONE',  ( 10.90749413291699987, -3.211956830789300277, 7.859564368461399830 ) ) ;
#41683=CARTESIAN_POINT ( 'NONE',  ( 10.85814141025499957, -3.516507310755200066, 6.638851159159999682 ) ) ;
#41688=CARTESIAN_POINT ( 'NONE',  ( 11.50000000000000000, -5.058572498595999889, 7.174999999999999822 ) ) ;
#41697=CARTESIAN_POINT ( 'NONE',  ( 11.12903166480609940, -4.864052766304100217, 7.439078678739090122 ) ) ;
#41699=VERTEX_POINT ( 'NONE', #47788 ) ;
#41725=VERTEX_POINT ( 'NONE', #64870 ) ;
#41746=CARTESIAN_POINT ( 'NONE',  ( 9.380265421555000316, -4.214287043487900064, 6.391527115138999626 ) ) ;
#41796=CARTESIAN_POINT ( 'NONE',  ( 9.405196823546312146, -3.391797362091467427, 6.627513167511573045 ) ) ;
#41822=CARTESIAN_POINT ( 'NONE',  ( 10.96887750876899936, -4.692271380433699512, 6.425720373262999274 ) ) ;
#41836=CARTESIAN_POINT ( 'NONE',  ( 9.286046699800502680, -3.154588942369298099, 7.038404655459764570 ) ) ;
#41859=CARTESIAN_POINT ( 'NONE',  ( 9.347442991499999465, -4.071878040089889517, 8.639547276484998761 ) ) ;
#41874=CARTESIAN_POINT ( 'NONE',  ( 12.05194988689359903, -3.419512757306400363, 6.361426117087999543 ) ) ;
#41890=CARTESIAN_POINT ( 'NONE',  ( 12.09999999999999964, -4.000000000000000000, 7.500000000000000000 ) ) ;
#41910=CARTESIAN_POINT ( 'NONE',  ( 11.72567835872029995, -4.993948309075300074, 8.126439557340900066 ) ) ;
#41913=B_SPLINE_CURVE_WITH_KNOTS ( 'NONE', 3,
 ( #49527, #44989, #60369, #40092 ),
 .UNSPECIFIED., .F., .F.,
 ( 4, 4 ),
 ( 0.000000000000000000, 1.000000000000000000 ),
 .UNSPECIFIED. ) ;
#41926=CARTESIAN_POINT ( 'NONE',  ( 12.10000000000000320, -3.812684744683585869, 8.553266857751333774 ) ) ;
#41937=CARTESIAN_POINT ( 'NONE',  ( 11.98052502238430073, -2.954316262216015065, 7.175009015034043536 ) ) ;
#41948=VECTOR ( 'NONE', #65828, 1000.000000000000000 ) ;
#41952=CARTESIAN_POINT ( 'NONE',  ( 12.20794988689359961, -3.544213289744700290, 6.606015074393400077 ) ) ;
#42000=CARTESIAN_POINT ( 'NONE',  ( 11.71979841651039855, -4.304975143798100312, 6.689266534545799558 ) ) ;
#42032=CARTESIAN_POINT ( 'NONE',  ( 11.73078751119019891, -4.915752892793999962, 7.020904658857499925 ) ) ;
#42037=DIRECTION ( 'NONE',  ( 0.000000000000000000, 0.000000000000000000, -1.000000000000000000 ) ) ;
#42046=CARTESIAN_POINT ( 'NONE',  ( 11.22749279009020107, -4.225282629687599822, 6.663611138821799784 ) ) ;
#42094=CARTESIAN_POINT ( 'NONE',  ( 9.901721904869999591, -3.124169273628900179, 7.008306153105300140 ) ) ;
#42112=CARTESIAN_POINT ( 'NONE',  ( 11.19837472757367713, -4.473492782822720670, 6.765225077371590956 ) ) ;
#42178=CARTESIAN_POINT ( 'NONE',  ( 12.12579573085663043, -2.760622544769000264, 7.285547569258399747 ) ) ;
#42216=CARTESIAN_POINT ( 'NONE',  ( 9.421417874593998931, -5.177249570814000279, 6.999532383170999239 ) ) ;
#42221=CARTESIAN_POINT ( 'NONE',  ( 10.09184687351566723, -3.000416447002275167, 6.731816600031356401 ) ) ;
#42228=CARTESIAN_POINT ( 'NONE',  ( 11.64256920625030034, -3.957769094421040190, 8.674127893687000324 ) ) ;
#42231=CARTESIAN_POINT ( 'NONE',  ( 11.73610538575739959, -2.890527834009000152, 7.765257665594799796 ) ) ;
#42237=B_SPLINE_CURVE_WITH_KNOTS ( 'NONE', 3,
 ( #53407, #22271, #48852, #33466, #65264, #16678, #1645, #60026, #27880, #10745, #11096, #17021, #11777, #5505, #32772, #26845, #38353, #16336 ),
 .UNSPECIFIED., .F., .F.,
 ( 4, 2, 2, 2, 2, 2, 2, 2, 4 ),
 ( 0.000000000000000000, 0.1250000000000000000, 0.2500000000000000000, 0.3750000000000000000, 0.5000000000000000000, 0.6250000000000000000, 0.7500000000000000000, 0.8750000000000000000, 1.000000000000000000 ),
 .UNSPECIFIED. ) ;
#42268=CARTESIAN_POINT ( 'NONE',  ( 11.48656920625009903, -3.967932847735990531, 8.391549386185598536 ) ) ;
#42310=CARTESIAN_POINT ( 'NONE',  ( 10.90333997687999990, -3.786145554879500441, 8.480416814141699788 ) ) ;
#42318=CARTESIAN_POINT ( 'NONE',  ( 11.84523293495530005, -5.315205473512000012, 7.552870914315270134 ) ) ;
#42340=CARTESIAN_POINT ( 'NONE',  ( 11.87299956498129916, -5.207010770456999893, 7.825000000000000178 ) ) ;
#42348=CARTESIAN_POINT ( 'NONE',  ( 9.217397846562217723, -4.245312990446880264, 6.659228100213050006 ) ) ;
#42354=CARTESIAN_POINT ( 'NONE',  ( 12.21210404293059959, -4.381818659177399766, 6.722495590581700320 ) ) ;
#42382=CARTESIAN_POINT ( 'NONE',  ( 9.732128830620874638, -4.207195853723359136, 8.743003876391233220 ) ) ;
#42384=LINE ( 'NONE', #5311, #47996 ) ;
#42395=CARTESIAN_POINT ( 'NONE',  ( 11.47364560330029981, -3.734560974198899874, 8.324524538096799375 ) ) ;
#42435=CARTESIAN_POINT ( 'NONE',  ( 10.91488779216199845, -3.070969952137800441, 7.164969140522200242 ) ) ;
#42469=CARTESIAN_POINT ( 'NONE',  ( 10.52101354018262391, -3.231816600031356845, 6.500416447002272946 ) ) ;
#42516=CARTESIAN_POINT ( 'NONE',  ( 12.00271932425157040, -4.187398418774900044, 6.235801371442999397 ) ) ;
#42551=CARTESIAN_POINT ( 'NONE',  ( 9.041480666858999982, -3.573487373903700082, 6.293984733123999753 ) ) ;
#42558=CIRCLE ( 'NONE', #10214, 1.249999999999999778 ) ;
#42565=CARTESIAN_POINT ( 'NONE',  ( 11.31349144726329925, -4.738947899111299655, 8.542723541016000510 ) ) ;
#42576=CARTESIAN_POINT ( 'NONE',  ( 9.599999931441001166, -2.750000000000000000, 7.500000000000000000 ) ) ;
#42581=CYLINDRICAL_SURFACE ( 'NONE', #16323, 1.250000000000000222 ) ;
#42601=CARTESIAN_POINT ( 'NONE',  ( 11.65278751119019951, -4.790480620979200133, 7.086443476450299706 ) ) ;
#42642=CARTESIAN_POINT ( 'NONE',  ( 11.48995257254740032, -5.095356924909000718, 7.181435527216799564 ) ) ;
#42647=CARTESIAN_POINT ( 'NONE',  ( 11.26857802013510046, -5.174568897094999897, 7.527343341769989316 ) ) ;
#42654=ORIENTED_EDGE ( 'NONE', *, *, #63905, .T. ) ;
#42683=CARTESIAN_POINT ( 'NONE',  ( 11.71564426047340035, -3.460037133261700149, 6.654192128557399499 ) ) ;
#42713=EDGE_CURVE ( 'NONE', #11605, #49203, #55874, .T. ) ;
#42720=CARTESIAN_POINT ( 'NONE',  ( 9.654341692891298621, -2.749999283195044164, 7.663628708442520754 ) ) ;
#42731=CARTESIAN_POINT ( 'NONE',  ( 11.76902897915239876, -3.778278678798900447, 6.662660017635100296 ) ) ;
#42778=CARTESIAN_POINT ( 'NONE',  ( 10.20567167105699902, -4.990538396979200542, 7.333638993632098924 ) ) ;
#42797=CARTESIAN_POINT ( 'NONE',  ( 11.51837338474677708, -4.264324089837040255, 8.333200082717626245 ) ) ;
#42805=LINE ( 'NONE', #9955, #48287 ) ;
#42810=CARTESIAN_POINT ( 'NONE',  ( 10.42726354018300050, -4.629523725463626782, 6.407767014557179230 ) ) ;
#42857=CARTESIAN_POINT ( 'NONE',  ( 10.82533997688000049, -3.756890902898200046, 8.614534918052999757 ) ) ;
#42866=CARTESIAN_POINT ( 'NONE',  ( 12.09999999999999609, -4.292035002842707669, 6.463642954493290738 ) ) ;
#42867=B_SPLINE_CURVE_WITH_KNOTS ( 'NONE', 3,
 ( #13102, #14730, #44918, #66222 ),
 .UNSPECIFIED., .F., .F.,
 ( 4, 4 ),
 ( 0.000000000000000000, 1.000000000000000000 ),
 .UNSPECIFIED. ) ;
#42907=CARTESIAN_POINT ( 'NONE',  ( 10.16684687351666661, -3.231816600031351516, 8.499583552997723501 ) ) ;
#42910=CARTESIAN_POINT ( 'NONE',  ( 10.89503166480599994, -5.274847857784000560, 7.410114961806599787 ) ) ;
#42920=DIRECTION ( 'NONE',  ( 0.000000000000000000, 1.000000000000000000, 0.000000000000000000 ) ) ;
#42939=ORIENTED_EDGE ( 'NONE', *, *, #49559, .F. ) ;
#42943=CARTESIAN_POINT ( 'NONE',  ( 11.90211496860029960, -3.206052520092899982, 7.906860999147899527 ) ) ;
#42945=VECTOR ( 'NONE', #40617, 1000.000000000000000 ) ;
#42982=CARTESIAN_POINT ( 'NONE',  ( 10.95257053952200010, -4.394359323863099576, 8.422730500489899796 ) ) ;
#42988=CARTESIAN_POINT ( 'NONE',  ( 11.26346886766499900, -4.634677072395899877, 8.653146038559000885 ) ) ;
#43027=CARTESIAN_POINT ( 'NONE',  ( 11.17410807141120088, -3.953638752893899877, 6.497602131078999754 ) ) ;
#43057=CARTESIAN_POINT ( 'NONE',  ( 11.19568717260499824, -4.466067913030199676, 6.739296831621899742 ) ) ;
#43069=CARTESIAN_POINT ( 'NONE',  ( 11.67056785386840012, -4.718624889240500053, 7.016391833292499491 ) ) ;
#43121=CARTESIAN_POINT ( 'NONE',  ( 10.10234252387499865, -4.857027829858100887, 7.631191628371899682 ) ) ;
#43203=CARTESIAN_POINT ( 'NONE',  ( 11.19041504065829962, -2.975441626403999784, 8.263934892306599167 ) ) ;
#43239=CARTESIAN_POINT ( 'NONE',  ( 9.294772138681999252, -4.476015718025199597, 8.687347221188998603 ) ) ;
#43253=CARTESIAN_POINT ( 'NONE',  ( 11.36272200990529946, -5.206705454565000224, 7.920925559347199219 ) ) ;
#43291=CARTESIAN_POINT ( 'NONE',  ( 11.43990547754509990, -2.967013601007999934, 7.467215766047949899 ) ) ;
#43307=ORIENTED_EDGE ( 'NONE', *, *, #15328, .F. ) ;
#43334=CARTESIAN_POINT ( 'NONE',  ( 12.05610404293055993, -4.502836909561000134, 6.476063885290000322 ) ) ;
#43342=CARTESIAN_POINT ( 'NONE',  ( 11.13880513895979973, -2.849548954067000039, 8.139542779846600240 ) ) ;
#43353=ORIENTED_EDGE ( 'NONE', *, *, #44290, .F. ) ;
#43375=CARTESIAN_POINT ( 'NONE',  ( 10.56276198887462847, -4.665935521472182934, 8.067505198359821605 ) ) ;
#43384=AXIS2_PLACEMENT_3D ( 'NONE', #7689, #40199, #6642 ) ;
#43429=CARTESIAN_POINT ( 'NONE',  ( 11.07564694612699974, -4.931992688388300294, 7.128058497017000228 ) ) ;
#43477=CARTESIAN_POINT ( 'NONE',  ( 9.420468108405998464, -3.033597967472499768, 7.226304214866999587 ) ) ;
#43484=CARTESIAN_POINT ( 'NONE',  ( 11.98513281071060632, -5.084573083995119980, 7.175000865651856685 ) ) ;
#43552=CARTESIAN_POINT ( 'NONE',  ( 10.64887885159599890, -2.730985436695000157, 7.651388779553199626 ) ) ;
#43558=CARTESIAN_POINT ( 'NONE',  ( 11.02022949779800065, -3.290320231472799950, 6.435697190503999465 ) ) ;
#43561=CARTESIAN_POINT ( 'NONE',  ( 12.09999999999999787, -4.813068503488582728, 6.962391415777370973 ) ) ;
#43590=CARTESIAN_POINT ( 'NONE',  ( 9.522734463322999332, -3.866750753272200303, 6.227746477418000026 ) ) ;
#43605=CARTESIAN_POINT ( 'NONE',  ( 10.57503300763299947, -3.118110956362800223, 6.575021251017499679 ) ) ;
#43640=CARTESIAN_POINT ( 'NONE',  ( 10.94125056272499918, -2.966599088466999934, 7.484684486284700178 ) ) ;
#43678=CARTESIAN_POINT ( 'NONE',  ( 10.80487885159599948, -3.003595720052600448, 7.618867373350600047 ) ) ;
#43682=VERTEX_POINT ( 'NONE', #21293 ) ;
#43687=CARTESIAN_POINT ( 'NONE',  ( 11.89189666366029918, -4.052152326617509459, 6.326270943800999191 ) ) ;
#43718=CARTESIAN_POINT ( 'NONE',  ( 10.51210369451062832, -4.198138975488563851, 8.352216648108843344 ) ) ;
#43742=ADVANCED_FACE ( 'NONE', ( #16726 ), #34000, .F. ) ;
#43750=CARTESIAN_POINT ( 'NONE',  ( 11.00333291544899872, -3.468906853242413657, 6.341063066638221279 ) ) ;
#43757=CARTESIAN_POINT ( 'NONE',  ( 11.36190547754509872, -3.108323067758099967, 7.471700551735359852 ) ) ;
#43821=CARTESIAN_POINT ( 'NONE',  ( 10.33030484851599873, -3.211495113978299898, 7.139489266142899915 ) ) ;
#43823=CARTESIAN_POINT ( 'NONE',  ( 11.18559687351634935, -2.907767014557174790, 8.129523725463618788 ) ) ;
#43837=CARTESIAN_POINT ( 'NONE',  ( 10.40987047770899920, -5.250000000000000888, 7.249610810850631637 ) ) ;
#43839=CARTESIAN_POINT ( 'NONE',  ( 11.54749144726329924, -4.500836215462999945, 8.206726025856399431 ) ) ;
#43863=CARTESIAN_POINT ( 'NONE',  ( 10.31059687351566545, -4.629523725463621453, 8.592232985442823434 ) ) ;
#43902=EDGE_CURVE ( 'NONE', #43682, #21925, #33781, .T. ) ;
#43905=CARTESIAN_POINT ( 'NONE',  ( 10.89358376188600097, -5.078750111091999919, 6.812480849273599759 ) ) ;
#43909=CARTESIAN_POINT ( 'NONE',  ( 12.09999999999999964, -4.862088370180454255, 7.087473780876516471 ) ) ;
#43925=ORIENTED_EDGE ( 'NONE', *, *, #44196, .F. ) ;
#44025=CARTESIAN_POINT ( 'NONE',  ( 10.28462143724499889, -3.241588663654300095, 8.353549467159899322 ) ) ;
#44028=CARTESIAN_POINT ( 'NONE',  ( 10.92380110216399913, -4.973546009874400653, 8.094557215852098864 ) ) ;
#44036=CARTESIAN_POINT ( 'NONE',  ( 10.94635971519499940, -3.540377183549800133, 8.264615166761799969 ) ) ;
#44068=CARTESIAN_POINT ( 'NONE',  ( 9.980191603681628720, -3.849750744317739670, 8.361949783971203587 ) ) ;
#44088=CARTESIAN_POINT ( 'NONE',  ( 9.643927823787143083, -2.750011555256801188, 7.500000155056757656 ) ) ;
#44158=CARTESIAN_POINT ( 'NONE',  ( 9.251496707488000126, -3.918323994020610268, 6.643597378104299622 ) ) ;
#44174=CARTESIAN_POINT ( 'NONE',  ( 9.925038493598998812, -3.372531419565699906, 8.098323595618600379 ) ) ;
#44186=ORIENTED_EDGE ( 'NONE', *, *, #6524, .T. ) ;
#44196=EDGE_CURVE ( 'NONE', #6623, #41725, #4915, .T. ) ;
#44231=DIRECTION ( 'NONE',  ( 0.000000000000000000, 0.000000000000000000, -1.000000000000000000 ) ) ;
#44233=ORIENTED_EDGE ( 'NONE', *, *, #64871, .T. ) ;
#44261=CARTESIAN_POINT ( 'NONE',  ( 11.58810207955139937, -4.796537143354000499, 7.825000000000000178 ) ) ;
#44262=CARTESIAN_POINT ( 'NONE',  ( 10.56430484851600049, -2.836617618740000069, 6.968092280137199168 ) ) ;
#44290=EDGE_CURVE ( 'NONE', #26079, #35697, #4035, .T. ) ;
#44307=CARTESIAN_POINT ( 'NONE',  ( 10.14601354018333090, -3.000416447002271170, 8.268183399968638270 ) ) ;
#44337=CARTESIAN_POINT ( 'NONE',  ( 10.80903300763299946, -3.402282662142699809, 6.873077781830399857 ) ) ;
#44378=CARTESIAN_POINT ( 'NONE',  ( 9.653405316140000636, -4.213249376011100722, 6.518487389810699639 ) ) ;
#44381=CARTESIAN_POINT ( 'NONE',  ( 10.70226357027499908, -2.879914860223000250, 7.283900408233900059 ) ) ;
#44389=CARTESIAN_POINT ( 'NONE',  ( 10.89969598649000027, -3.111999510220800236, 6.971269690999399415 ) ) ;
#44435=B_SPLINE_CURVE_WITH_KNOTS ( 'NONE', 3,
 ( #49878, #60709, #34153, #33461 ),
 .UNSPECIFIED., .F., .F.,
 ( 4, 4 ),
 ( 0.000000000000000000, 0.1494581667962518179 ),
 .UNSPECIFIED. ) ;
#44441=CARTESIAN_POINT ( 'NONE',  ( 10.15998825978599918, -4.131418345883800747, 6.504223158184999853 ) ) ;
#44447=CARTESIAN_POINT ( 'NONE',  ( 11.05478570706233299, -2.868293641868291388, 6.886599490775120458 ) ) ;
#44453=CARTESIAN_POINT ( 'NONE',  ( 9.307788144226000426, -3.909067355573210278, 6.546538158064899804 ) ) ;
#44488=CARTESIAN_POINT ( 'NONE',  ( 10.66476354018241501, -2.782534154164604256, 7.827184855449094592 ) ) ;
#44524=CARTESIAN_POINT ( 'NONE',  ( 9.521784697134998865, -3.454948069423500190, 8.343659109631099469 ) ) ;
#44547=FACE_OUTER_BOUND ( 'NONE', #54900, .T. ) ;
#44565=EDGE_CURVE ( 'NONE', #34321, #64614, #19906, .T. ) ;
#44572=CARTESIAN_POINT ( 'NONE',  ( 10.24809687351566723, -3.672815144550895194, 8.717465845835393523 ) ) ;
#44588=ORIENTED_EDGE ( 'NONE', *, *, #54179, .T. ) ;
#44607=DIRECTION ( 'NONE',  ( -1.000000000000000000, 0.000000000000000000, 0.000000000000000000 ) ) ;
#44608=CARTESIAN_POINT ( 'NONE',  ( 9.652455549953000258, -3.004437130344999929, 8.303267676773000261 ) ) ;
#44680=EDGE_CURVE ( 'NONE', #41017, #4376, #65835, .T. ) ;
#44684=CARTESIAN_POINT ( 'NONE',  ( 11.34641504065830020, -3.195537720350400068, 8.099826052678000821 ) ) ;
#44705=CARTESIAN_POINT ( 'NONE',  ( 9.205629240798000268, -4.228941919214900480, 6.623477632995699693 ) ) ;
#44719=CARTESIAN_POINT ( 'NONE',  ( 9.754721904869999349, -3.124169273628900179, 7.008306153105300140 ) ) ;
#44722=CARTESIAN_POINT ( 'NONE',  ( 11.34226088462130022, -3.997572771977982775, 8.640738455926999961 ) ) ;
#44732=CARTESIAN_POINT ( 'NONE',  ( 12.10533460557258323, -3.815825449682300086, 6.374224726731999802 ) ) ;
#44733=CARTESIAN_POINT ( 'NONE',  ( 11.23213259636990102, -4.907524392912299582, 7.005495010505599751 ) ) ;
#44782=CARTESIAN_POINT ( 'NONE',  ( 10.71722949779699974, -3.442773960835399993, 6.664331202173499946 ) ) ;
#44886=ORIENTED_EDGE ( 'NONE', *, *, #58310, .F. ) ;
#44918=CARTESIAN_POINT ( 'NONE',  ( 11.75740844561608789, -2.954218652640771214, 7.824999626888802240 ) ) ;
#44931=CARTESIAN_POINT ( 'NONE',  ( 11.19809687351600047, -3.672815144550895639, 8.717465845835397076 ) ) ;
#44945=CARTESIAN_POINT ( 'NONE',  ( 10.41031740696899810, -3.787635830142400462, 6.378110563671000044 ) ) ;
#44963=DIRECTION ( 'NONE',  ( -1.000000000000000000, 0.000000000000000000, 0.000000000000000000 ) ) ;
#44970=ORIENTED_EDGE ( 'NONE', *, *, #1973, .F. ) ;
#44989=CARTESIAN_POINT ( 'NONE',  ( 11.52319144466311052, -2.880026002252477291, 7.175010281093781472 ) ) ;
#45018=CARTESIAN_POINT ( 'NONE',  ( 10.78441772631200024, -3.627481539113199815, 6.733203680593099705 ) ) ;
#45035=FACE_OUTER_BOUND ( 'NONE', #25431, .T. ) ;
#45056=CARTESIAN_POINT ( 'NONE',  ( 10.58857120343300018, -4.055348968344419269, 6.359530327585999565 ) ) ;
#45059=CARTESIAN_POINT ( 'NONE',  ( 10.84995525820099971, -4.107710726525199973, 8.635644537520001052 ) ) ;
#45064=EDGE_CURVE ( 'NONE', #13467, #57524, #57410, .T. ) ;
#45071=CARTESIAN_POINT ( 'NONE',  ( 11.00180110216400031, -4.856393875115199599, 8.023010882787499298 ) ) ;
#45072=CARTESIAN_POINT ( 'NONE',  ( 12.06833327354034857, -4.746587807672299597, 7.988332985010599963 ) ) ;
#45106=FACE_OUTER_BOUND ( 'NONE', #39455, .T. ) ;
#45121=CARTESIAN_POINT ( 'NONE',  ( 10.13465911260399999, -4.436443689698799986, 6.595367916746299741 ) ) ;
#45249=CARTESIAN_POINT ( 'NONE',  ( 10.16476354018233508, -2.782534154164604256, 7.827184855449094592 ) ) ;
#45287=CARTESIAN_POINT ( 'NONE',  ( 9.827747021775998348, -4.858221690000700477, 6.746879837742599584 ) ) ;
#45304=( NAMED_UNIT ( * ) SI_UNIT ( $, .STERADIAN. ) SOLID_ANGLE_UNIT ( ) );
#45310=CARTESIAN_POINT ( 'NONE',  ( 12.05670819615735923, -4.620649663933218854, 8.119355997108678835 ) ) ;
#45327=EDGE_LOOP ( 'NONE', ( #65097, #33297, #9169, #31526, #55132, #34632, #58195, #68794, #32159, #35134, #14549 ) ) ;
#45361=CARTESIAN_POINT ( 'NONE',  ( 12.08071932425156980, -4.167269912168199753, 6.371589232479998977 ) ) ;
#45372=CARTESIAN_POINT ( 'NONE',  ( 11.83810207955129989, -3.203462856645999945, 7.174999999999999822 ) ) ;
#45401=CARTESIAN_POINT ( 'NONE',  ( 10.38593802597399929, -4.593629475532499562, 8.475365825607600101 ) ) ;
#45406=CARTESIAN_POINT ( 'NONE',  ( 12.11759063708296047, -2.782734359457999851, 7.157757529645699890 ) ) ;
#45415=CARTESIAN_POINT ( 'NONE',  ( 11.29718447801629999, -2.996774412198000448, 7.522119512433738997 ) ) ;
#45416=CARTESIAN_POINT ( 'NONE',  ( 11.85545123989520100, -3.524778630617700248, 6.582230774881299595 ) ) ;
#45449=CARTESIAN_POINT ( 'NONE',  ( 12.09456039236534330, -2.685288321999000249, 7.436015812896529020 ) ) ;
#45464=CARTESIAN_POINT ( 'NONE',  ( 9.604759580228998672, -4.843256805554699618, 7.701558687214699717 ) ) ;
#45469=CARTESIAN_POINT ( 'NONE',  ( 9.436337454063533414, -4.868096831666449908, 8.168216413461584224 ) ) ;
#45473=CARTESIAN_POINT ( 'NONE',  ( 11.64975833414749928, -4.796537143354000499, 7.174999999999999822 ) ) ;
#45503=ORIENTED_EDGE ( 'NONE', *, *, #33277, .F. ) ;
#45552=CARTESIAN_POINT ( 'NONE',  ( 9.297364180957998769, -4.070567455836420656, 6.524104241236299728 ) ) ;
#45581=CARTESIAN_POINT ( 'NONE',  ( 12.21210404293059959, -4.381818659177399766, 6.722495590581700320 ) ) ;
#45586=CARTESIAN_POINT ( 'NONE',  ( 10.13667167105699995, -4.855035690642299784, 7.356396684460199786 ) ) ;
#45598=CARTESIAN_POINT ( 'NONE',  ( 10.83351354018233259, -5.249999999999999112, 7.663624617374471093 ) ) ;
#45631=CARTESIAN_POINT ( 'NONE',  ( 10.35965911260399963, -4.496147888241900148, 6.471616938597000157 ) ) ;
#45647=FILL_AREA_STYLE_COLOUR ( '', #60153 ) ;
#45653=DIRECTION ( 'NONE',  ( 0.000000000000000000, 0.000000000000000000, 1.000000000000000000 ) ) ;
#45672=DIRECTION ( 'NONE',  ( 0.000000000000000000, -1.000000000000000000, 0.000000000000000000 ) ) ;
#45687=DIRECTION ( 'NONE',  ( 0.000000000000000000, 0.8514547570628039352, -0.5244280662542016858 ) ) ;
#45702=CARTESIAN_POINT ( 'NONE',  ( 11.51456785386839954, -4.946394603182100447, 6.863111178199799767 ) ) ;
#45716=CARTESIAN_POINT ( 'NONE',  ( 9.248821772879615821, -3.697635112905263366, 6.625936606111492821 ) ) ;
#45741=CARTESIAN_POINT ( 'NONE',  ( 10.56122949779699915, -3.290320231472799950, 6.435697190503999465 ) ) ;
#45753=CARTESIAN_POINT ( 'NONE',  ( 11.10026222744819790, -4.774534945026900346, 6.861998062869400172 ) ) ;
#45789=CARTESIAN_POINT ( 'NONE',  ( 11.02799293566599914, -3.193321847920899792, 6.510429574318199464 ) ) ;
#45801=CARTESIAN_POINT ( 'NONE',  ( 10.38795058442699926, -3.601336184534900120, 8.421905343605699201 ) ) ;
#45824=CARTESIAN_POINT ( 'NONE',  ( 12.33518044953559922, -3.231951024059400268, 7.099502491684900107 ) ) ;
#45900=CARTESIAN_POINT ( 'NONE',  ( 11.64767835872009982, -4.874341053673500568, 8.051056647135798272 ) ) ;
#45963=CARTESIAN_POINT ( 'NONE',  ( 9.525809814041000578, -3.217492037304399588, 6.488038963273999649 ) ) ;
#45978=( NAMED_UNIT ( * ) PLANE_ANGLE_UNIT ( ) SI_UNIT ( $, .RADIAN. ) );
#46041=CARTESIAN_POINT ( 'NONE',  ( 10.87457053952200070, -4.448306506338299826, 8.548957288282998945 ) ) ;
#46079=CARTESIAN_POINT ( 'NONE',  ( 9.902671671056999969, -5.261543809652999393, 7.288123611975898974 ) ) ;
#46083=CARTESIAN_POINT ( 'NONE',  ( 11.26426088462129904, -3.997280690308189666, 8.778009775371000245 ) ) ;
#46085=CARTESIAN_POINT ( 'NONE',  ( 9.966846873515667227, -4.768183399968645375, 6.500416447002276499 ) ) ;
#46086=VERTEX_POINT ( 'NONE', #63429 ) ;
#46090=CARTESIAN_POINT ( 'NONE',  ( 11.51279632507520034, -3.375091146194399983, 6.341531314375999706 ) ) ;
#46093=CARTESIAN_POINT ( 'NONE',  ( 11.24379975933729980, -2.921317947059999920, 7.871126858273000515 ) ) ;
#46120=CARTESIAN_POINT ( 'NONE',  ( 10.60478570706233370, -2.868293641868291388, 6.886599490775120458 ) ) ;
#46129=CARTESIAN_POINT ( 'NONE',  ( 11.30502344389999969, -5.125258734743999511, 8.182900850620900002 ) ) ;
#46146=CARTESIAN_POINT ( 'NONE',  ( 12.10000000000000142, -4.149724965537171073, 8.514310854298580367 ) ) ;
#46171=CARTESIAN_POINT ( 'NONE',  ( 11.56795257254739973, -4.963546614172099858, 7.219770138693499817 ) ) ;
#46179=CARTESIAN_POINT ( 'NONE',  ( 12.17766954483535891, -3.284117569315500251, 8.604570063127999546 ) ) ;
#46199=EDGE_CURVE ( 'NONE', #29598, #34355, #35513, .T. ) ;
#46202=FILL_AREA_STYLE ('',( #8795 ) ) ;
#46218=CARTESIAN_POINT ( 'NONE',  ( 11.00595525820100029, -4.081787880721680750, 8.362327856951900173 ) ) ;
#46247=CARTESIAN_POINT ( 'NONE',  ( 11.60612378248510090, -4.482960757953799558, 8.413720204863100349 ) ) ;
#46264=FACE_OUTER_BOUND ( 'NONE', #29779, .T. ) ;
#46270=CARTESIAN_POINT ( 'NONE',  ( 10.26331740696899963, -3.838745722419000028, 6.648116790593900483 ) ) ;
#46279=CARTESIAN_POINT ( 'NONE',  ( 10.82309687351566474, -5.217465845835395299, 7.827184855449101697 ) ) ;
#46312=CARTESIAN_POINT ( 'NONE',  ( 9.701101285863998669, -4.735211557675400584, 8.373612278672599274 ) ) ;
#46386=CARTESIAN_POINT ( 'NONE',  ( 11.39149144726329865, -4.659577337894599935, 8.430724369296298093 ) ) ;
#46425=CARTESIAN_POINT ( 'NONE',  ( 10.35859632033900013, -5.184381781355999586, 7.983346856269500691 ) ) ;
#46428=CARTESIAN_POINT ( 'NONE',  ( 11.14118447801630118, -2.722297859592000435, 7.528171279442569919 ) ) ;
#46436=CARTESIAN_POINT ( 'NONE',  ( 12.05300581613033906, -2.892415530317000272, 6.788791567531699656 ) ) ;
#46438=CARTESIAN_POINT ( 'NONE',  ( 10.77610941423800028, -3.155589807313900153, 8.266982106121901097 ) ) ;
#46460=VERTEX_POINT ( 'NONE', #35764 ) ;
#46474=CARTESIAN_POINT ( 'NONE',  ( 11.97500581613029880, -3.011381429075500105, 6.865182626353099948 ) ) ;
#46475=CARTESIAN_POINT ( 'NONE',  ( 11.66486084871730000, -2.792989229543000107, 7.825000000000000178 ) ) ;
#46491=CARTESIAN_POINT ( 'NONE',  ( 12.09999999999999609, -3.064876132552082577, 8.208828950335220753 ) ) ;
#46517=CARTESIAN_POINT ( 'NONE',  ( 12.08487348028855024, -4.882707455860599843, 7.022738645480499642 ) ) ;
#46550=SURFACE_SIDE_STYLE ('',( #57029 ) ) ;
#46563=CARTESIAN_POINT ( 'NONE',  ( 12.08902763632552002, -4.786505910413500153, 7.862914650060299770 ) ) ;
#46596=CARTESIAN_POINT ( 'NONE',  ( 11.56456920625009843, -3.962850971080120299, 8.532838639935999225 ) ) ;
#46616=CARTESIAN_POINT ( 'NONE',  ( 10.01002593514599859, -4.125890936441000356, 8.357822485499299958 ) ) ;
#46658=CARTESIAN_POINT ( 'NONE',  ( 10.48429229006299934, -3.131390070940299974, 8.004340253666999416 ) ) ;
#46681=VECTOR ( 'NONE', #65300, 1000.000000000000000 ) ;
#46732=CARTESIAN_POINT ( 'NONE',  ( 11.31764560330029923, -3.650429500487800460, 8.585859374935999710 ) ) ;
#46755=EDGE_CURVE ( 'NONE', #34355, #65484, #60063, .T. ) ;
#46768=CARTESIAN_POINT ( 'NONE',  ( 10.25727973160899964, -3.885210315895800015, 8.774051692788999546 ) ) ;
#46771=CARTESIAN_POINT ( 'NONE',  ( 11.38733729122639993, -5.277570687708000641, 7.533608309972310124 ) ) ;
#46779=CARTESIAN_POINT ( 'NONE',  ( 11.67901463001530082, -3.302889347096799710, 8.616511311517999872 ) ) ;
#46781=CARTESIAN_POINT ( 'NONE',  ( 11.19456919669529960, -2.906008650422999828, 7.176777099639999768 ) ) ;
#46818=CARTESIAN_POINT ( 'NONE',  ( 11.89189666366029918, -4.052152326617509459, 6.326270943800999191 ) ) ;
#46859=CARTESIAN_POINT ( 'NONE',  ( 11.74025954179439957, -3.228187097503200320, 6.858707791728399172 ) ) ;
#46904=CARTESIAN_POINT ( 'NONE',  ( 11.27672335273219950, -3.698477709264200275, 6.687976048055599421 ) ) ;
#46935=CARTESIAN_POINT ( 'NONE',  ( 11.40346005378009941, -3.213042707518099839, 7.920222357891399945 ) ) ;
#46943=DIRECTION ( 'NONE',  ( -1.000000000000000000, 0.000000000000000000, 0.000000000000000000 ) ) ;
#46949=CARTESIAN_POINT ( 'NONE',  ( 11.49826088462129903, -3.998156935320088756, 8.366195817038299509 ) ) ;
#46955=CARTESIAN_POINT ( 'NONE',  ( 10.28864655415099882, -3.580250267348600079, 6.741370903243699253 ) ) ;
#46976=CARTESIAN_POINT ( 'NONE',  ( 11.72823073745748879, -4.169674042210387732, 6.639671036489041001 ) ) ;
#46984=AXIS2_PLACEMENT_3D ( 'NONE', #11123, #27905, #12162 ) ;
#46992=CARTESIAN_POINT ( 'NONE',  ( 11.03521345716899837, -3.075109701058799772, 6.659120737011199331 ) ) ;
#46997=CARTESIAN_POINT ( 'NONE',  ( 10.30698825978599942, -4.131418345883800747, 6.504223158184999853 ) ) ;
#47001=B_SPLINE_CURVE_WITH_KNOTS ( 'NONE', 3,
 ( #30276, #31303, #51581, #52613, #14870, #52272, #4367, #4707, #62751 ),
 .UNSPECIFIED., .F., .F.,
 ( 4, 1, 1, 1, 1, 1, 4 ),
 ( 0.000000000000000000, 0.1176715969261408201, 0.3173201826739890374, 0.5169687684225858781, 0.7166173541704341510, 0.9162659399182827569, 1.000000000000000000 ),
 .UNSPECIFIED. ) ;
#47059=LINE ( 'NONE', #35875, #13177 ) ;
#47076=CARTESIAN_POINT ( 'NONE',  ( 10.72687885159599830, -2.867290578374000365, 7.635128076451499268 ) ) ;
#47112=CARTESIAN_POINT ( 'NONE',  ( 9.322113844317998499, -3.711648483798899889, 8.604802177355001191 ) ) ;
#47124=CARTESIAN_POINT ( 'NONE',  ( 11.92834208742529967, -4.706521750018099581, 6.389420067180999752 ) ) ;
#47126=CARTESIAN_POINT ( 'NONE',  ( 11.95348876160960039, -4.885820101980599794, 6.578783887955899523 ) ) ;
#47146=CARTESIAN_POINT ( 'NONE',  ( 11.78627509987130040, -4.272452942476324900, 8.749999999999998224 ) ) ;
#47161=CARTESIAN_POINT ( 'NONE',  ( 11.80367835872029936, -5.113555564477999305, 8.201822467543799178 ) ) ;
#47175=CARTESIAN_POINT ( 'NONE',  ( 12.10000000000000320, -3.304217902137880802, 8.404145852941008243 ) ) ;
#47203=CARTESIAN_POINT ( 'NONE',  ( 11.30133863405320049, -3.465595476214000215, 6.818303296693398963 ) ) ;
#47247=CARTESIAN_POINT ( 'NONE',  ( 11.99056651104150006, -3.914543207408039738, 8.361971998931499783 ) ) ;
#47280=CARTESIAN_POINT ( 'NONE',  ( 10.98280513895999988, -3.096689368913399854, 8.002155910165599906 ) ) ;
#47295=CARTESIAN_POINT ( 'NONE',  ( 12.13410404293056999, -4.442327784369100030, 6.599279737936000423 ) ) ;
#47328=CARTESIAN_POINT ( 'NONE',  ( 9.843930206850000530, -5.250000000000000000, 7.500000000000000000 ) ) ;
#47341=CARTESIAN_POINT ( 'NONE',  ( 10.00303849359899822, -3.273092657276900130, 8.193143574899998782 ) ) ;
#47418=CARTESIAN_POINT ( 'NONE',  ( 10.62841772631199966, -3.509411006705700053, 6.490165927606000196 ) ) ;
#47468=CARTESIAN_POINT ( 'NONE',  ( 11.31013259637009938, -5.031671030421000168, 6.937848198857199833 ) ) ;
#47470=CARTESIAN_POINT ( 'NONE',  ( 11.90425819896749893, -5.255890247626999745, 7.263238376356399684 ) ) ;
#47491=CARTESIAN_POINT ( 'NONE',  ( 11.85565467195930367, -5.136173005413449566, 8.088082908809450799 ) ) ;
#47507=CARTESIAN_POINT ( 'NONE',  ( 11.73589666366019912, -4.039600775206940497, 6.608753462694600067 ) ) ;
#47551=CARTESIAN_POINT ( 'NONE',  ( 11.24795391537420031, -3.169881940022800215, 6.936213817702099327 ) ) ;
#47559=CARTESIAN_POINT ( 'NONE',  ( 11.31013259637009938, -5.031671030421000168, 6.937848198857199833 ) ) ;
#47595=CARTESIAN_POINT ( 'NONE',  ( 11.42441504065829960, -3.305585767322499979, 8.017771632862299214 ) ) ;
#47641=CARTESIAN_POINT ( 'NONE',  ( 11.39979975933730039, -3.180925410802600162, 7.781807394638899922 ) ) ;
#47651=CARTESIAN_POINT ( 'NONE',  ( 9.591433907306443629, -3.054280487670652189, 6.668243572402049679 ) ) ;
#47675=CONICAL_SURFACE ( 'NONE', #6332, 0.9346783463124002100, 0.7853981908209605178 ) ;
#47678=ORIENTED_EDGE ( 'NONE', *, *, #68496, .F. ) ;
#47687=CARTESIAN_POINT ( 'NONE',  ( 10.63626717315599990, -4.764472860199700399, 8.151477970733999712 ) ) ;
#47710=EDGE_CURVE ( 'NONE', #21230, #50475, #40726, .T. ) ;
#47760=CARTESIAN_POINT ( 'NONE',  ( 12.08810207955109917, -4.796537143354000499, 7.825000000000000178 ) ) ;
#47770=CARTESIAN_POINT ( 'NONE',  ( 10.70226357027499908, -2.879914860223000250, 7.283900408233900059 ) ) ;
#47788=CARTESIAN_POINT ( 'NONE',  ( 11.09393020684900044, -2.750000000000000000, 7.500000000000000000 ) ) ;
#47808=CARTESIAN_POINT ( 'NONE',  ( 9.117468108405999416, -2.769196120524999749, 7.151422676278199830 ) ) ;
#47820=CARTESIAN_POINT ( 'NONE',  ( 11.78118179236250107, -4.267047616085000605, 8.749800764654999341 ) ) ;
#47839=CARTESIAN_POINT ( 'NONE',  ( 9.541999884715579583, -4.156896875802718050, 6.308000049678228471 ) ) ;
#47843=CARTESIAN_POINT ( 'NONE',  ( 12.02285868696541549, -3.940189611494480992, 6.228129494253471066 ) ) ;
#47855=CARTESIAN_POINT ( 'NONE',  ( 11.40346005378009941, -3.213042707518099839, 7.920222357891399945 ) ) ;
#47873=CONICAL_SURFACE ( 'NONE', #43384, 0.9999998338055000602, 0.7853981908209605178 ) ;
#47894=CARTESIAN_POINT ( 'NONE',  ( 11.53918313518939875, -4.707599264529200411, 6.605241151424599444 ) ) ;
#47901=CARTESIAN_POINT ( 'NONE',  ( 11.63746005378019888, -2.838900981960999825, 8.120007936598501175 ) ) ;
#47934=CARTESIAN_POINT ( 'NONE',  ( 12.18333460557258974, -3.837988184179999873, 6.509695444280099608 ) ) ;
#47951=ORIENTED_EDGE ( 'NONE', *, *, #59616, .F. ) ;
#47964=CARTESIAN_POINT ( 'NONE',  ( 10.94635971519499940, -3.540377183549800133, 8.264615166761799969 ) ) ;
#47969=ADVANCED_FACE ( 'NONE', ( #28874 ), #37279, .F. ) ;
#47979=CARTESIAN_POINT ( 'NONE',  ( 11.91256651104150066, -3.901000349726440053, 8.498573944230598087 ) ) ;
#47996=VECTOR ( 'NONE', #57416, 1000.000000000000000 ) ;
#48023=CARTESIAN_POINT ( 'NONE',  ( 10.71225461470299933, -4.973404788313100511, 7.252360304610999897 ) ) ;
#48040=CARTESIAN_POINT ( 'NONE',  ( 10.81021345716900051, -3.363461959113699606, 6.921280946186199934 ) ) ;
#48106=CARTESIAN_POINT ( 'NONE',  ( 11.87964291764649971, -5.268358781405000357, 7.656787697937099679 ) ) ;
#48154=CARTESIAN_POINT ( 'NONE',  ( 10.87041638348499895, -5.241705141469999774, 7.802464414828100381 ) ) ;
#48180=CARTESIAN_POINT ( 'NONE',  ( 11.82299956498189886, -5.207010770456999893, 7.825000000000000178 ) ) ;
#48189=CARTESIAN_POINT ( 'NONE',  ( 11.23213259636990102, -4.907524392912299582, 7.005495010505599751 ) ) ;
#48227=CARTESIAN_POINT ( 'NONE',  ( 12.17918044953561996, -2.988516238873000219, 6.972563939641199582 ) ) ;
#48232=CARTESIAN_POINT ( 'NONE',  ( 11.92834208742529967, -4.706521750018099581, 6.389420067180999752 ) ) ;
#48262=CARTESIAN_POINT ( 'NONE',  ( 9.231616107288068918, -3.999997736744774546, 6.618420992905502231 ) ) ;
#48269=CARTESIAN_POINT ( 'NONE',  ( 11.22333863405319931, -3.380905141010200232, 6.710270673950399889 ) ) ;
#48287=VECTOR ( 'NONE', #63075, 1000.000000000000000 ) ;
#48306=CARTESIAN_POINT ( 'NONE',  ( 11.03521345716899837, -3.075109701058799772, 6.659120737011199331 ) ) ;
#48316=CARTESIAN_POINT ( 'NONE',  ( 11.17826222744820086, -4.668580868411999596, 6.949274830123499669 ) ) ;
#48344=ORIENTED_EDGE ( 'NONE', *, *, #43902, .T. ) ;
#48363=CARTESIAN_POINT ( 'NONE',  ( 10.22898825978600001, -4.113440707072600233, 6.640442468193600511 ) ) ;
#48382=CARTESIAN_POINT ( 'NONE',  ( 11.02606775832648189, -4.343526402396090447, 8.303790528164435969 ) ) ;
#48395=CARTESIAN_POINT ( 'NONE',  ( 12.09999999999999964, -2.792989229543000107, 7.174999999999999822 ) ) ;
#48399=ORIENTED_EDGE ( 'NONE', *, *, #44196, .T. ) ;
#48403=EDGE_CURVE ( 'NONE', #7217, #46086, #16991, .T. ) ;
#48449=CARTESIAN_POINT ( 'NONE',  ( 10.77610941423800028, -3.155589807313900153, 8.266982106121901097 ) ) ;
#48469=AXIS2_PLACEMENT_3D ( 'NONE', #51131, #35739, #36076 ) ;
#48485=CARTESIAN_POINT ( 'NONE',  ( 9.320101285864000218, -4.823683599683300294, 8.478738839062499366 ) ) ;
#48500=CARTESIAN_POINT ( 'NONE',  ( 11.75656651104150008, -3.873914634362100262, 8.771777834828998976 ) ) ;
#48521=CARTESIAN_POINT ( 'NONE',  ( 11.99200216175158396, -4.419830582853482071, 6.297929225185963986 ) ) ;
#48536=CARTESIAN_POINT ( 'NONE',  ( 11.36190547754509872, -3.108323067758099967, 7.471700551735359852 ) ) ;
#48550=AXIS2_PLACEMENT_3D ( 'NONE', #6425, #49781, #38246 ) ;
#48553=B_SPLINE_CURVE_WITH_KNOTS ( 'NONE', 3,
 ( #29652, #64691, #11905, #45372 ),
 .UNSPECIFIED., .F., .F.,
 ( 4, 4 ),
 ( 0.000000000000000000, 1.000000000000000000 ),
 .UNSPECIFIED. ) ;
#48575=CARTESIAN_POINT ( 'NONE',  ( 11.42026088462129962, -3.997864853650589634, 8.503467136482999678 ) ) ;
#48583=CARTESIAN_POINT ( 'NONE',  ( 12.22433327354039889, -4.983220429128399687, 8.143111181492699302 ) ) ;
#48587=VERTEX_POINT ( 'NONE', #67974 ) ;
#48612=CARTESIAN_POINT ( 'NONE',  ( 10.23348307550462621, -4.114479073428862321, 6.632574608010647133 ) ) ;
#48651=CARTESIAN_POINT ( 'NONE',  ( 11.32035090130999855, -3.241273085157000189, 7.030721746772699454 ) ) ;
#48660=CARTESIAN_POINT ( 'NONE',  ( 11.43937577273821482, -4.461177266722074819, 6.300114087089554893 ) ) ;
#48664=CARTESIAN_POINT ( 'NONE',  ( 12.05610404293055993, -4.502836909561000134, 6.476063885290000322 ) ) ;
#48717=CARTESIAN_POINT ( 'NONE',  ( 9.646417874593998576, -4.797903641662700558, 7.160798403412399260 ) ) ;
#48726=DIRECTION ( 'NONE',  ( -1.000000000000000000, 0.000000000000000000, 0.000000000000000000 ) ) ;
#48736=CARTESIAN_POINT ( 'NONE',  ( 11.52287616594230002, -4.261927842557799551, 8.325646653015098764 ) ) ;
#48755=CARTESIAN_POINT ( 'NONE',  ( 12.07299956498157023, -2.792989229543000107, 7.174999999999999822 ) ) ;
#48799=CARTESIAN_POINT ( 'NONE',  ( 10.31101337669300122, -5.140392946802999852, 8.079558723821699928 ) ) ;
#48809=CARTESIAN_POINT ( 'NONE',  ( 11.75361999289386894, -4.544092497359195626, 8.657883396625688732 ) ) ;
#48847=CARTESIAN_POINT ( 'NONE',  ( 10.82118582084300051, -4.836160649475099937, 8.466515260542900378 ) ) ;
#48852=CARTESIAN_POINT ( 'NONE',  ( 9.864763540183334456, -5.217465845835395299, 7.172815144550902744 ) ) ;
#48870=EDGE_CURVE ( 'NONE', #36697, #7217, #33343, .T. ) ;
#48873=STYLED_ITEM ( 'NONE', ( #41298 ), #18558 ) ;
#48882=CARTESIAN_POINT ( 'NONE',  ( 11.27368717260499942, -4.539928529895099985, 6.618743573831199711 ) ) ;
#48920=CARTESIAN_POINT ( 'NONE',  ( 11.73610538575739959, -2.890527834009000152, 7.765257665594799796 ) ) ;
#48930=CARTESIAN_POINT ( 'NONE',  ( 11.51279632507520034, -3.375091146194399983, 6.341531314375999706 ) ) ;
#48957=CARTESIAN_POINT ( 'NONE',  ( 10.63874943042162613, -4.847937002157847175, 7.284280020558234980 ) ) ;
#48995=CARTESIAN_POINT ( 'NONE',  ( 9.779336721442295044, -4.163631234563185401, 8.749993199158904389 ) ) ;
#49009=CARTESIAN_POINT ( 'NONE',  ( 12.15456516821461008, -3.197083038490000195, 6.689681884064299311 ) ) ;
#49041=LINE ( 'NONE', #44158, #21719 ) ;
#49058=CARTESIAN_POINT ( 'NONE',  ( 9.572442991499999110, -4.063228561016970275, 8.502419298200999620 ) ) ;
#49059=CARTESIAN_POINT ( 'NONE',  ( 11.50000000000000000, -5.058572498595999889, 7.174999999999999822 ) ) ;
#49122=CARTESIAN_POINT ( 'NONE',  ( 11.22934687351609817, -4.163624617374463099, 8.750000000000000000 ) ) ;
#49141=CARTESIAN_POINT ( 'NONE',  ( 12.09999999999999964, -4.883784007588900522, 7.174999999999999822 ) ) ;
#49184=CARTESIAN_POINT ( 'NONE',  ( 11.83041235500449950, -4.942357465271699724, 8.363295307663500822 ) ) ;
#49203=VERTEX_POINT ( 'NONE', #7369 ) ;
#49212=CARTESIAN_POINT ( 'NONE',  ( 12.09999999999999964, -4.000000000000000000, 7.500000000000000000 ) ) ;
#49221=EDGE_CURVE ( 'NONE', #58532, #52202, #68624, .T. ) ;
#49236=CARTESIAN_POINT ( 'NONE',  ( 9.241072744221000335, -4.062652182992059657, 6.633566614602499634 ) ) ;
#49257=CARTESIAN_POINT ( 'NONE',  ( 11.80579707368350029, -4.634832087857400751, 8.609190966793999422 ) ) ;
#49264=CARTESIAN_POINT ( 'NONE',  ( 11.77234208742519961, -4.554746427620499638, 6.627995351445298944 ) ) ;
#49293=CARTESIAN_POINT ( 'NONE',  ( 10.78877584378239973, -3.533998264153197955, 6.763172759027205494 ) ) ;
#49397=CARTESIAN_POINT ( 'NONE',  ( 10.00102593514599825, -4.125890936441000356, 8.357822485499299958 ) ) ;
#49411=AXIS2_PLACEMENT_3D ( 'NONE', #1944, #44607, #65900 ) ;
#49416=CARTESIAN_POINT ( 'NONE',  ( 11.96595122972050085, -3.656201404350900130, 8.295047870239098842 ) ) ;
#49450=FACE_OUTER_BOUND ( 'NONE', #8711, .T. ) ;
#49481=CARTESIAN_POINT ( 'NONE',  ( 10.20969678796400082, -3.780328739572700325, 8.760209873321999297 ) ) ;
#49485=CARTESIAN_POINT ( 'NONE',  ( 12.09999999999999964, -3.674136214561153135, 6.377063228063083677 ) ) ;
#49523=LINE ( 'NONE', #7567, #5907 ) ;
#49527=CARTESIAN_POINT ( 'NONE',  ( 11.50000000000000000, -2.920245322398999921, 7.174999999999999822 ) ) ;
#49557=ORIENTED_EDGE ( 'NONE', *, *, #59360, .F. ) ;
#49559=EDGE_CURVE ( 'NONE', #50475, #1441, #67754, .T. ) ;
#49560=CARTESIAN_POINT ( 'NONE',  ( 11.05103166480599874, -5.000984463463999496, 7.429424106427209296 ) ) ;
#49602=CARTESIAN_POINT ( 'NONE',  ( 9.374784697135000400, -3.454948069423500190, 8.343659109631099469 ) ) ;
#49605=CARTESIAN_POINT ( 'NONE',  ( 11.26841504065830080, -3.085489673376300424, 8.181880472491098288 ) ) ;
#49606=ORIENTED_EDGE ( 'NONE', *, *, #59616, .T. ) ;
#49613=CARTESIAN_POINT ( 'NONE',  ( 11.52301463001509951, -3.452642973349600464, 8.376661845795100092 ) ) ;
#49643=CARTESIAN_POINT ( 'NONE',  ( 9.904204162135625822, -3.209635909649031671, 7.875309037467246753 ) ) ;
#49665=CARTESIAN_POINT ( 'NONE',  ( 9.756734463322999318, -3.909687748588949852, 6.637705594503099604 ) ) ;
#49710=CARTESIAN_POINT ( 'NONE',  ( 10.84184687351645593, -4.999583552997724389, 8.268183399968647151 ) ) ;
#49748=CARTESIAN_POINT ( 'NONE',  ( 10.68491290906799840, -4.548591194283900130, 6.828616613600999585 ) ) ;
#49767=CARTESIAN_POINT ( 'NONE',  ( 10.45769129028899869, -4.889436474118637577, 6.586710612921466534 ) ) ;
#49770=CARTESIAN_POINT ( 'NONE',  ( 11.59672200990539892, -4.817867935977999672, 7.785290430335599865 ) ) ;
#49781=DIRECTION ( 'NONE',  ( -1.000000000000000000, 0.000000000000000000, 0.000000000000000000 ) ) ;
#49827=CARTESIAN_POINT ( 'NONE',  ( 10.69810941423799910, -3.053977294209000437, 8.359277272599898723 ) ) ;
#49831=FACE_OUTER_BOUND ( 'NONE', #53516, .T. ) ;
#49832=CARTESIAN_POINT ( 'NONE',  ( 10.58963399569799968, -2.728594541839999721, 7.358888170452400068 ) ) ;
#49855=CARTESIAN_POINT ( 'NONE',  ( 11.89975833414730033, -3.203462856645999945, 7.825000000000000178 ) ) ;
#49866=B_SPLINE_CURVE_WITH_KNOTS ( 'NONE', 3,
 ( #62892, #52760, #35992, #68138, #46491, #41242, #19223, #31442, #20601, #47175, #31108, #56637, #35660, #19577, #41926, #13994, #35319, #9410, #46146, #8740, #15012, #30085, #68477, #51387, #4853, #9758, #3484, #67452, #62553, #30754 ),
 .UNSPECIFIED., .F., .F.,
 ( 4, 2, 1, 1, 2, 2, 2, 2, 2, 2, 2, 2, 2, 2, 2, 4 ),
 ( 0.000000000000000000, 0.1250000000000048017, 0.1875000000000072164, 0.2187500000000076883, 0.2343750000000070777, 0.2500000000000064948, 0.3750000000000048850, 0.4375000000000044409, 0.5000000000000038858, 0.5625000000000034417, 0.6250000000000028866, 0.6875000000000024425, 0.7500000000000018874, 0.8125000000000014433, 0.8750000000000009992, 1.000000000000000000 ),
 .UNSPECIFIED. ) ;
#49878=CARTESIAN_POINT ( 'NONE',  ( 9.599999931441001166, -2.935682118448999844, 6.844464000216799349 ) ) ;
#49887=CARTESIAN_POINT ( 'NONE',  ( 12.09999999999999964, -4.000000000000000000, 7.500000000000000000 ) ) ;
#49909=CARTESIAN_POINT ( 'NONE',  ( 12.23256516821459883, -3.293702443348299980, 6.787191910456499500 ) ) ;
#49949=CARTESIAN_POINT ( 'NONE',  ( 9.904684229509999938, -4.804883439508000897, 8.309874741421300115 ) ) ;
#49952=CARTESIAN_POINT ( 'NONE',  ( 11.12072335273220069, -3.602909566644000083, 6.430603299050000388 ) ) ;
#49954=CARTESIAN_POINT ( 'NONE',  ( 10.59393020684899867, -2.750000000000000000, 7.500000000000000000 ) ) ;
#49961=CARTESIAN_POINT ( 'NONE',  ( 11.68923293495519999, -5.032672437899000428, 7.541513160549049744 ) ) ;
#50008=EDGE_CURVE ( 'NONE', #48587, #26079, #37803, .T. ) ;
#50016=CARTESIAN_POINT ( 'NONE',  ( 10.61591290906799934, -4.635529777446699917, 6.722218404915299317 ) ) ;
#50040=CARTESIAN_POINT ( 'NONE',  ( 9.873082992855456652, -5.217431357650285761, 7.827172124334913939 ) ) ;
#50056=ORIENTED_EDGE ( 'NONE', *, *, #16520, .F. ) ;
#50074=CARTESIAN_POINT ( 'NONE',  ( 10.39393020684899938, -5.250000000000000000, 7.500000000000000000 ) ) ;
#50182=CARTESIAN_POINT ( 'NONE',  ( 10.71627973161000114, -3.885210315895700095, 8.774051692788999546 ) ) ;
#50256=CARTESIAN_POINT ( 'NONE',  ( 11.24795391537420031, -3.169881940022800215, 6.936213817702099327 ) ) ;
#50281=CARTESIAN_POINT ( 'NONE',  ( 9.198396402459000143, -4.369105567410300317, 6.701746336527099501 ) ) ;
#50298=CARTESIAN_POINT ( 'NONE',  ( 9.349455549952999434, -3.218304396998100003, 8.130709350565298976 ) ) ;
#50302=CARTESIAN_POINT ( 'NONE',  ( 11.16995391537419913, -3.056324258617099776, 6.859089544950699668 ) ) ;
#50311=CARTESIAN_POINT ( 'NONE',  ( 11.86333594839950045, -3.340240242524600056, 8.256087240512899328 ) ) ;
#50312=CARTESIAN_POINT ( 'NONE',  ( 11.86056039236529891, -3.108928759355700233, 7.456633480985620288 ) ) ;
#50362=CARTESIAN_POINT ( 'NONE',  ( 10.46393802597400047, -4.522194782554399772, 8.357994702431799539 ) ) ;
#50438=CARTESIAN_POINT ( 'NONE',  ( 9.418455549952998496, -3.325238030324599858, 8.044430187461498960 ) ) ;
#50439=CARTESIAN_POINT ( 'NONE',  ( 11.50000000000000000, -4.968589424331200100, 7.825000000000000178 ) ) ;
#50466=CARTESIAN_POINT ( 'NONE',  ( 10.58521345716900086, -3.075109701058799772, 6.659120737011199331 ) ) ;
#50471=VERTEX_POINT ( 'NONE', #27297 ) ;
#50475=VERTEX_POINT ( 'NONE', #5274 ) ;
#50482=CARTESIAN_POINT ( 'NONE',  ( 10.15434687351566723, -2.749999999999998668, 7.663624617374463988 ) ) ;
#50508=CARTESIAN_POINT ( 'NONE',  ( 9.210288521113000115, -4.352953559891299840, 6.715449042252499723 ) ) ;
#50522=CARTESIAN_POINT ( 'NONE',  ( 9.878405316141000370, -4.242421256336299962, 6.384219384258999597 ) ) ;
#50540=FILL_AREA_STYLE ('',( #45647 ) ) ;
#50597=CARTESIAN_POINT ( 'NONE',  ( 11.50000000000000000, -2.920245322398999921, 7.174999999999999822 ) ) ;
#50600=CARTESIAN_POINT ( 'NONE',  ( 12.19559063708295987, -2.913481137622000006, 7.194517870904999945 ) ) ;
#50603=EDGE_CURVE ( 'NONE', #19919, #55891, #35295, .T. ) ;
#50619=DIRECTION ( 'NONE',  ( 0.000000000000000000, 1.000000000000000000, 0.000000000000000000 ) ) ;
#50640=CARTESIAN_POINT ( 'NONE',  ( 9.678734463322999915, -3.895375416816699854, 6.501052555474699624 ) ) ;
#50643=CARTESIAN_POINT ( 'NONE',  ( 10.65303300763299887, -3.212834858289399964, 6.674373427955200277 ) ) ;
#50654=CARTESIAN_POINT ( 'NONE',  ( 11.76487482311540056, -3.069598554678400149, 7.124095752359899336 ) ) ;
#50655=CARTESIAN_POINT ( 'NONE',  ( 11.15413259636999932, -4.783377755405500587, 7.073141822156699732 ) ) ;
#50706=CARTESIAN_POINT ( 'NONE',  ( 9.427455549952998837, -3.325238030324599858, 8.044430187461498960 ) ) ;
#50716=ADVANCED_FACE ( 'NONE', ( #45106 ), #16065, .F. ) ;
#50718=CARTESIAN_POINT ( 'NONE',  ( 11.77769289846838241, -5.045673698156681652, 7.175017342370984430 ) ) ;
#50790=CARTESIAN_POINT ( 'NONE',  ( 9.519772138681998896, -4.322628849750500102, 8.304747519296199698 ) ) ;
#50802=ADVANCED_FACE ( 'NONE', ( #17764 ), #39082, .T. ) ;
#50813=VERTEX_POINT ( 'NONE', #59709 ) ;
#50820=CARTESIAN_POINT ( 'NONE',  ( 12.28594988689359901, -3.606563555963900214, 6.728309553046099012 ) ) ;
#50835=CARTESIAN_POINT ( 'NONE',  ( 10.66684687351566652, -3.231816600031351516, 8.499583552997723501 ) ) ;
#50868=CARTESIAN_POINT ( 'NONE',  ( 10.96755864497999866, -3.101067942814400347, 6.795973491698399371 ) ) ;
#50890=CARTESIAN_POINT ( 'NONE',  ( 11.97822875044625057, -3.830319670899316353, 8.360317195474184615 ) ) ;
#50909=CARTESIAN_POINT ( 'NONE',  ( 9.099999952505998024, -4.000000000000000000, 6.750000006358199300 ) ) ;
#50944=CARTESIAN_POINT ( 'NONE',  ( 11.19456919669529960, -2.906008650422999828, 7.176777099639999768 ) ) ;
#50983=CARTESIAN_POINT ( 'NONE',  ( 10.63922949779700033, -3.366547096154099972, 6.550014196338999284 ) ) ;
#50986=CARTESIAN_POINT ( 'NONE',  ( 11.01810807141099957, -3.940954591493389891, 6.223352037434000117 ) ) ;
#50995=CARTESIAN_POINT ( 'NONE',  ( 10.82949413291699869, -3.087070836781100169, 7.916546720849799712 ) ) ;
#51033=CARTESIAN_POINT ( 'NONE',  ( 11.42968717260509948, -4.687649763627899979, 6.377637058250999580 ) ) ;
#51047=CARTESIAN_POINT ( 'NONE',  ( 9.982684229509999341, -4.708027397558999461, 8.212418068717900255 ) ) ;
#51118=AXIS2_PLACEMENT_3D ( 'NONE', #2720, #65306, #50619 ) ;
#51131=CARTESIAN_POINT ( 'NONE',  ( 12.09999999999999964, -4.000000000000000000, 7.500000000000000000 ) ) ;
#51150=CARTESIAN_POINT ( 'NONE',  ( 11.18546886766499959, -4.566506264294200257, 8.529286361367999447 ) ) ;
#51167=CARTESIAN_POINT ( 'NONE',  ( 11.91672066707849886, -3.258843737379200078, 7.948314604624900248 ) ) ;
#51172=CARTESIAN_POINT ( 'NONE',  ( 10.71924205624999971, -4.310927436352299580, 6.690659495528099576 ) ) ;
#51212=CARTESIAN_POINT ( 'NONE',  ( 9.449822372493999367, -4.367693913457399546, 6.297150255604999636 ) ) ;
#51284=CARTESIAN_POINT ( 'NONE',  ( 10.94841638348500013, -5.108333310975999630, 7.769976643522699788 ) ) ;
#51324=CARTESIAN_POINT ( 'NONE',  ( 10.43458376188599956, -5.078750111091999919, 6.812480849273599759 ) ) ;
#51327=CARTESIAN_POINT ( 'NONE',  ( 10.57503300763299947, -3.118110956362800223, 6.575021251017499679 ) ) ;
#51337=CARTESIAN_POINT ( 'NONE',  ( 11.21918447801630059, -2.859536135895000442, 7.525145395936648995 ) ) ;
#51367=CARTESIAN_POINT ( 'NONE',  ( 9.321633776942626071, -3.275060658047592277, 7.010106850326409678 ) ) ;
#51372=CARTESIAN_POINT ( 'NONE',  ( 11.01925056272500036, -2.825232917634000085, 7.482589369563879877 ) ) ;
#51387=CARTESIAN_POINT ( 'NONE',  ( 12.10000000000000142, -4.531190383827668811, 8.305884920888427558 ) ) ;
#51410=CARTESIAN_POINT ( 'NONE',  ( 11.44487616594229884, -4.303437140848100029, 8.456491899811199531 ) ) ;
#51415=DIRECTION ( 'NONE',  ( -1.000000000000000000, 0.000000000000000000, 0.000000000000000000 ) ) ;
#51445=EDGE_CURVE ( 'NONE', #53853, #50471, #36889, .T. ) ;
#51454=LINE ( 'NONE', #29468, #27036 ) ;
#51483=CARTESIAN_POINT ( 'NONE',  ( 12.02166954483529970, -3.437903757373499847, 8.367285821793199574 ) ) ;
#51503=CARTESIAN_POINT ( 'NONE',  ( 10.82055864497999842, -3.317414799430800088, 6.965412239408199646 ) ) ;
#51545=CARTESIAN_POINT ( 'NONE',  ( 10.08103849359899939, -3.173653894988100355, 8.287963554181398962 ) ) ;
#51581=CARTESIAN_POINT ( 'NONE',  ( 12.04292372906209430, -2.967457464456210836, 6.730835578941808173 ) ) ;
#51620=CARTESIAN_POINT ( 'NONE',  ( 12.17918044953561996, -2.988516238873000219, 6.972563939641199582 ) ) ;
#51659=CARTESIAN_POINT ( 'NONE',  ( 10.61188779216199940, -2.816792857868000155, 7.073306690476799830 ) ) ;
#51665=CARTESIAN_POINT ( 'NONE',  ( 9.998096873515667227, -4.327184855449103473, 6.282534154164607365 ) ) ;
#51670=CARTESIAN_POINT ( 'NONE',  ( 12.13611496860034933, -2.828587461987000395, 8.100294210499798808 ) ) ;
#51672=CARTESIAN_POINT ( 'NONE',  ( 11.46533729122639933, -5.140346530769000388, 7.529998433785960010 ) ) ;
#51710=CARTESIAN_POINT ( 'NONE',  ( 11.55435090131019926, -2.880552878538999995, 6.807613609764599616 ) ) ;
#51750=CARTESIAN_POINT ( 'NONE',  ( 11.10441638348510018, -4.841589649988700117, 7.705001100909899314 ) ) ;
#51757=CARTESIAN_POINT ( 'NONE',  ( 12.34388784977539899, -5.255745690988000263, 7.571757098260779806 ) ) ;
#51764=VERTEX_POINT ( 'NONE', #34806 ) ;
#51781=CARTESIAN_POINT ( 'NONE',  ( 9.482564767455610166, -5.103418008754404767, 7.204352198296668064 ) ) ;
#51795=CARTESIAN_POINT ( 'NONE',  ( 11.79364426047339975, -3.533902447304699823, 6.769896129503799820 ) ) ;
#51823=CARTESIAN_POINT ( 'NONE',  ( 11.56967835872019990, -4.754733798270200928, 7.975673736933100777 ) ) ;
#51831=CARTESIAN_POINT ( 'NONE',  ( 11.55336220499919975, -4.965402920923000174, 7.174999999999999822 ) ) ;
#51840=CARTESIAN_POINT ( 'NONE',  ( 12.23671932425159881, -4.127012898954600217, 6.643164954553199664 ) ) ;
#51844=ORIENTED_EDGE ( 'NONE', *, *, #2360, .T. ) ;
#51845=CARTESIAN_POINT ( 'NONE',  ( 10.66858376188599955, -4.731143729777899765, 7.034020612385399218 ) ) ;
#51856=ORIENTED_EDGE ( 'NONE', *, *, #46199, .F. ) ;
#51885=CARTESIAN_POINT ( 'NONE',  ( 9.576468108405999047, -2.769196120524999749, 7.151422676278199830 ) ) ;
#51943=DIRECTION ( 'NONE',  ( 1.000000000000000000, 0.000000000000000000, 0.000000000000000000 ) ) ;
#51960=CARTESIAN_POINT ( 'NONE',  ( 10.75564828895399927, -3.119330945648699949, 7.018986873610899124 ) ) ;
#51984=CARTESIAN_POINT ( 'NONE',  ( 11.57273594314529142, -2.871094011463778184, 7.824979517142727659 ) ) ;
#51996=CARTESIAN_POINT ( 'NONE',  ( 9.271455549953000030, -3.111370763671500228, 8.216988513669100769 ) ) ;
#52001=CARTESIAN_POINT ( 'NONE',  ( 10.00851354018233152, -4.163624617374471093, 6.250000000000000888 ) ) ;
#52007=CARTESIAN_POINT ( 'NONE',  ( 11.01414141025500015, -3.384226587288500010, 6.403245959303999868 ) ) ;
#52009=CARTESIAN_POINT ( 'NONE',  ( 12.02733460557258915, -3.793662715184400014, 6.238754009183999472 ) ) ;
#52047=CARTESIAN_POINT ( 'NONE',  ( 12.17403632436368888, -4.976178716761900489, 7.727966254184200245 ) ) ;
#52089=CARTESIAN_POINT ( 'NONE',  ( 11.00595525820100029, -4.081787880721680750, 8.362327856951900173 ) ) ;
#52100=CARTESIAN_POINT ( 'NONE',  ( 11.61486084871780022, -2.792989229543000107, 7.825000000000000178 ) ) ;
#52136=CARTESIAN_POINT ( 'NONE',  ( 11.62133729122639991, -4.865898216891100247, 7.522778681411049995 ) ) ;
#52155=CARTESIAN_POINT ( 'NONE',  ( 11.50000000000000000, -5.058572498595999889, 7.174999999999999822 ) ) ;
#52171=CARTESIAN_POINT ( 'NONE',  ( 11.44501463001509833, -3.527519786474400121, 8.256737112932800216 ) ) ;
#52202=VERTEX_POINT ( 'NONE', #46992 ) ;
#52231=CARTESIAN_POINT ( 'NONE',  ( 9.371822372493999964, -4.328199826929600036, 6.426348619097999482 ) ) ;
#52258=FACE_OUTER_BOUND ( 'NONE', #975, .T. ) ;
#52272=CARTESIAN_POINT ( 'NONE',  ( 11.92394752546313796, -4.702246198360438889, 6.396140797112706444 ) ) ;
#52278=CIRCLE ( 'NONE', #13222, 0.7499999936418002555 ) ;
#52315=CARTESIAN_POINT ( 'NONE',  ( 11.48579841651039857, -4.449968941611500028, 6.303820944768999901 ) ) ;
#52348=CARTESIAN_POINT ( 'NONE',  ( 9.448759580228999866, -5.110528875107000601, 7.765443149353999708 ) ) ;
#52351=CARTESIAN_POINT ( 'NONE',  ( 10.94426222744800015, -4.986443098259000450, 6.687444528363699625 ) ) ;
#52361=CARTESIAN_POINT ( 'NONE',  ( 11.89189666366029918, -4.052152326617509459, 6.326270943800999191 ) ) ;
#52363=CARTESIAN_POINT ( 'NONE',  ( 12.00271932425157040, -4.187398418774900044, 6.235801371442999397 ) ) ;
#52383=CARTESIAN_POINT ( 'NONE',  ( 12.03828694957233303, -3.690393262785353734, 6.264939056470321788 ) ) ;
#52399=CARTESIAN_POINT ( 'NONE',  ( 11.14391429142989942, -3.977620450637519678, 8.674673860548999471 ) ) ;
#52437=CARTESIAN_POINT ( 'NONE',  ( 11.54333729122640051, -5.003122373830000136, 7.526388557597149642 ) ) ;
#52466=( NAMED_UNIT ( * ) SI_UNIT ( $, .STERADIAN. ) SOLID_ANGLE_UNIT ( ) );
#52484=CARTESIAN_POINT ( 'NONE',  ( 12.35979573085659844, -3.159987984332300215, 7.354650721737899133 ) ) ;
#52513=CARTESIAN_POINT ( 'NONE',  ( 11.94366954483529852, -3.514796851401900124, 8.248643701125299543 ) ) ;
#52531=CARTESIAN_POINT ( 'NONE',  ( 11.52287616594230002, -4.261927842557799551, 8.325646653015098764 ) ) ;
#52576=CARTESIAN_POINT ( 'NONE',  ( 10.23100081823899998, -4.888721525563999748, 7.032008172796599510 ) ) ;
#52592=CARTESIAN_POINT ( 'NONE',  ( 11.05068303964748111, -4.571908710946855692, 8.161067340483363353 ) ) ;
#52613=CARTESIAN_POINT ( 'NONE',  ( 12.00705667793316245, -3.398423525757989339, 6.338208022222376670 ) ) ;
#52655=CARTESIAN_POINT ( 'NONE',  ( 11.85502763632550050, -5.160433036184000066, 8.035454525731699604 ) ) ;
#52705=CARTESIAN_POINT ( 'NONE',  ( 12.22433327354039889, -4.983220429128399687, 8.143111181492699302 ) ) ;
#52707=CARTESIAN_POINT ( 'NONE',  ( 11.80995122972050027, -3.547233695387300045, 8.547040013405998948 ) ) ;
#52729=CARTESIAN_POINT ( 'NONE',  ( 11.75158531382729699, -3.727547057523674212, 8.749999999999996447 ) ) ;
#52730=CARTESIAN_POINT ( 'NONE',  ( 11.91486084871699802, -5.207010770456999893, 7.174999999999999822 ) ) ;
#52744=CARTESIAN_POINT ( 'NONE',  ( 11.86056039236529891, -3.108928759355700233, 7.456633480985620288 ) ) ;
#52760=CARTESIAN_POINT ( 'NONE',  ( 12.10000000000000142, -2.860800829850470350, 7.925587283338803246 ) ) ;
#52786=CARTESIAN_POINT ( 'NONE',  ( 11.81410538575740077, -3.024036709177600368, 7.733337754805098996 ) ) ;
#52820=CARTESIAN_POINT ( 'NONE',  ( 11.96021572556889012, -5.045751188959975764, 7.824997386306807634 ) ) ;
#52832=CARTESIAN_POINT ( 'NONE',  ( 12.06441235500451015, -4.638700978900200056, 8.085115074060599483 ) ) ;
#52847=B_SPLINE_CURVE_WITH_KNOTS ( 'NONE', 3,
 ( #53335, #21849, #68708, #16264 ),
 .UNSPECIFIED., .F., .F.,
 ( 4, 4 ),
 ( 0.000000000000000000, 1.000000000000000000 ),
 .UNSPECIFIED. ) ;
#52867=EDGE_CURVE ( 'NONE', #41725, #26079, #11467, .T. ) ;
#52880=CARTESIAN_POINT ( 'NONE',  ( 11.42441504065829960, -3.305585767322499979, 8.017771632862299214 ) ) ;
#52926=CARTESIAN_POINT ( 'NONE',  ( 9.673759580228999511, -4.976892840331100132, 7.733500918284399894 ) ) ;
#52934=CARTESIAN_POINT ( 'NONE',  ( 11.91486084871699802, -5.207010770456999893, 7.174999999999999822 ) ) ;
#52942=CARTESIAN_POINT ( 'NONE',  ( 10.89393020684999946, -5.250000000000000000, 7.500000000000000000 ) ) ;
#53006=CARTESIAN_POINT ( 'NONE',  ( 12.11759063708296047, -2.782734359457999851, 7.157757529645699890 ) ) ;
#53043=CARTESIAN_POINT ( 'NONE',  ( 9.446747021775999897, -4.961496216383199709, 6.656252755052399550 ) ) ;
#53054=CARTESIAN_POINT ( 'NONE',  ( 12.01145123989533126, -3.394760891061399999, 6.331134574721999364 ) ) ;
#53056=CARTESIAN_POINT ( 'NONE',  ( 11.65810538575740019, -2.757018958839999812, 7.797177576385699638 ) ) ;
#53090=CARTESIAN_POINT ( 'NONE',  ( 10.94635971519499940, -3.540377183549800133, 8.264615166761799969 ) ) ;
#53106=EDGE_LOOP ( 'NONE', ( #61725, #49606, #48344, #7826 ) ) ;
#53132=CARTESIAN_POINT ( 'NONE',  ( 11.58841369783139896, -4.057552111898620417, 6.360711682373000109 ) ) ;
#53139=CARTESIAN_POINT ( 'NONE',  ( 11.01414141025500015, -3.384226587288500010, 6.403245959303999868 ) ) ;
#53173=CARTESIAN_POINT ( 'NONE',  ( 11.98641235500450009, -4.739919807690899489, 8.177841818594698609 ) ) ;
#53206=CARTESIAN_POINT ( 'NONE',  ( 9.843930206850000530, -5.250000000000000000, 7.500000000000000000 ) ) ;
#53220=CARTESIAN_POINT ( 'NONE',  ( 11.98641235500450009, -4.739919807690899489, 8.177841818594698609 ) ) ;
#53234=ORIENTED_EDGE ( 'NONE', *, *, #26372, .F. ) ;
#53259=DIRECTION ( 'NONE',  ( 0.000000000000000000, 0.000000000000000000, -1.000000000000000000 ) ) ;
#53269=CARTESIAN_POINT ( 'NONE',  ( 10.02836764078099918, -3.526522998810799781, 8.385811396220899994 ) ) ;
#53277=CARTESIAN_POINT ( 'NONE',  ( 12.09999999999999964, -4.000000000000000000, 7.500000000000000000 ) ) ;
#53335=CARTESIAN_POINT ( 'NONE',  ( 9.251496707488000126, -3.918323994020610268, 6.643597378104299622 ) ) ;
#53351=CARTESIAN_POINT ( 'NONE',  ( 11.38733729122639993, -5.277570687708000641, 7.533608309972310124 ) ) ;
#53387=CARTESIAN_POINT ( 'NONE',  ( 9.345430433046999497, -5.088604610742000212, 8.171806809244198888 ) ) ;
#53400=CARTESIAN_POINT ( 'NONE',  ( 10.17726354018333090, -3.370476274536371442, 8.592232985442818105 ) ) ;
#53403=CARTESIAN_POINT ( 'NONE',  ( 11.14118447801630118, -2.722297859592000435, 7.528171279442569919 ) ) ;
#53407=CARTESIAN_POINT ( 'NONE',  ( 9.843930206850000530, -5.250000000000000000, 7.500000000000000000 ) ) ;
#53438=CARTESIAN_POINT ( 'NONE',  ( 11.39835090130999973, -3.121033016283800254, 6.956352367771000189 ) ) ;
#53477=CARTESIAN_POINT ( 'NONE',  ( 11.98225819896750011, -5.120994791668000090, 7.288668995979000087 ) ) ;
#53483=CARTESIAN_POINT ( 'NONE',  ( 11.76723293495529887, -5.173938955706000264, 7.547192037433419820 ) ) ;
#53509=B_SPLINE_CURVE_WITH_KNOTS ( 'NONE', 3,
 ( #36165, #9584, #43484, #52934 ),
 .UNSPECIFIED., .F., .F.,
 ( 4, 4 ),
 ( 0.000000000000000000, 1.000000000000000000 ),
 .UNSPECIFIED. ) ;
#53516=EDGE_LOOP ( 'NONE', ( #57012, #19523, #22773, #44886, #27260 ) ) ;
#53522=CARTESIAN_POINT ( 'NONE',  ( 11.32179975933729921, -3.051121678931899783, 7.826467126457498757 ) ) ;
#53564=CARTESIAN_POINT ( 'NONE',  ( 11.84287482311539996, -3.196874704906699893, 7.175518335304800210 ) ) ;
#53611=CARTESIAN_POINT ( 'NONE',  ( 10.73758376188599861, -4.847012523549299345, 6.960174024681499816 ) ) ;
#53630=CARTESIAN_POINT ( 'NONE',  ( 11.39529697814177744, -3.173432105636238454, 7.784385510031588851 ) ) ;
#53642=CARTESIAN_POINT ( 'NONE',  ( 10.38559687351649963, -5.092232985442824322, 6.870476274536375882 ) ) ;
#53648=ORIENTED_EDGE ( 'NONE', *, *, #61441, .F. ) ;
#53690=LINE ( 'NONE', #37603, #10452 ) ;
#53693=CARTESIAN_POINT ( 'NONE',  ( 11.53502897915239878, -3.672866099873000056, 6.264564938179000286 ) ) ;
#53727=CARTESIAN_POINT ( 'NONE',  ( 9.674709346416999978, -2.844451673749999632, 8.048718920009699573 ) ) ;
#53742=CARTESIAN_POINT ( 'NONE',  ( 11.55964426047339977, -3.312306505177499805, 6.422784126663999338 ) ) ;
#53776=CARTESIAN_POINT ( 'NONE',  ( 10.98280513895999988, -3.096689368913399854, 8.002155910165599906 ) ) ;
#53791=EDGE_LOOP ( 'NONE', ( #60630, #62780, #3211, #4662, #9859 ) ) ;
#53814=CARTESIAN_POINT ( 'NONE',  ( 10.75564828895399927, -3.119330945648699949, 7.018986873610899124 ) ) ;
#53820=CARTESIAN_POINT ( 'NONE',  ( 11.22702344389999851, -5.004394439171999664, 8.109550315577399360 ) ) ;
#53853=VERTEX_POINT ( 'NONE', #57573 ) ;
#53888=CARTESIAN_POINT ( 'NONE',  ( 9.701637546194749717, -3.727464796005204750, 8.730330573913894554 ) ) ;
#53892=CARTESIAN_POINT ( 'NONE',  ( 9.099999952505998024, -4.000000000000000000, 7.500000000000000000 ) ) ;
#53899=ORIENTED_EDGE ( 'NONE', *, *, #65670, .F. ) ;
#53901=CARTESIAN_POINT ( 'NONE',  ( 12.08071932425156980, -4.167269912168199753, 6.371589232479998977 ) ) ;
#53935=MANIFOLD_SOLID_BREP ( 'Stock-MAS-678-1', #9066 ) ;
#53948=CARTESIAN_POINT ( 'NONE',  ( 9.597772138681998300, -4.373757805842100055, 8.432280753260499750 ) ) ;
#53964=CARTESIAN_POINT ( 'NONE',  ( 11.49375810342577608, -3.998140074039970848, 8.374120210831636157 ) ) ;
#54033=CARTESIAN_POINT ( 'NONE',  ( 10.51364655415099847, -3.380689388027600106, 6.380697202105999999 ) ) ;
#54067=CARTESIAN_POINT ( 'NONE',  ( 9.269442991500000062, -4.080527519162810535, 8.776675254768999679 ) ) ;
#54112=VERTEX_POINT ( 'NONE', #55788 ) ;
#54116=CARTESIAN_POINT ( 'NONE',  ( 11.11257802013489915, -4.891884252872400474, 7.520762592984879369 ) ) ;
#54155=CARTESIAN_POINT ( 'NONE',  ( 11.10026222744819790, -4.774534945026900346, 6.861998062869400172 ) ) ;
#54162=CARTESIAN_POINT ( 'NONE',  ( 11.93345123989529988, -3.459769760840400110, 6.456682674800999777 ) ) ;
#54179=EDGE_CURVE ( 'NONE', #67539, #40612, #56697, .T. ) ;
#54222=CARTESIAN_POINT ( 'NONE',  ( 10.90769129028899798, -4.889436474118636689, 6.586710612921465646 ) ) ;
#54242=CARTESIAN_POINT ( 'NONE',  ( 10.70641772631199906, -3.568446272909699957, 6.611684804099500212 ) ) ;
#54294=CARTESIAN_POINT ( 'NONE',  ( 9.471126402771000485, -3.060189502158800146, 7.854398824525599565 ) ) ;
#54315=CARTESIAN_POINT ( 'NONE',  ( 12.26133460557259980, -3.860150918677800025, 6.645166161828299778 ) ) ;
#54382=CARTESIAN_POINT ( 'NONE',  ( 9.753772138682000659, -4.476015718025199597, 8.687347221188998603 ) ) ;
#54430=CARTESIAN_POINT ( 'NONE',  ( 10.91964694612699915, -5.186980343482999523, 7.026297514493899499 ) ) ;
#54505=CARTESIAN_POINT ( 'NONE',  ( 11.61302897915239818, -3.708003626182200030, 6.397263297997000109 ) ) ;
#54514=CARTESIAN_POINT ( 'NONE',  ( 11.81900581613029999, -3.249313226592100534, 7.017964743997199939 ) ) ;
#54546=CARTESIAN_POINT ( 'NONE',  ( 9.676241837494625742, -4.657637647145090654, 6.922899494040819945 ) ) ;
#54579=CARTESIAN_POINT ( 'NONE',  ( 10.84393020684900044, -5.250000000000000000, 7.500000000000000000 ) ) ;
#54589=CARTESIAN_POINT ( 'NONE',  ( 9.716839207166817260, -3.231820996160967407, 8.499566091636109988 ) ) ;
#54649=CARTESIAN_POINT ( 'NONE',  ( 10.63425461470299993, -4.840245908677600184, 7.286236678332599581 ) ) ;
#54717=CARTESIAN_POINT ( 'NONE',  ( 11.30226354018299872, -5.092232985442821658, 8.129523725463625894 ) ) ;
#54718=EDGE_CURVE ( 'NONE', #24435, #11483, #49866, .T. ) ;
#54733=CARTESIAN_POINT ( 'NONE',  ( 10.69095058442700008, -3.492264136285500253, 8.674133161175999973 ) ) ;
#54784=ORIENTED_EDGE ( 'NONE', *, *, #32579, .F. ) ;
#54789=CARTESIAN_POINT ( 'NONE',  ( 12.01961669203094196, -2.969723712172476215, 7.824983907773938263 ) ) ;
#54808=CARTESIAN_POINT ( 'NONE',  ( 11.64179841651039915, -4.353306409735099969, 6.560784671286499226 ) ) ;
#54850=CARTESIAN_POINT ( 'NONE',  ( 9.577417874593999514, -4.924352284713100047, 7.107043063332000088 ) ) ;
#54853=CARTESIAN_POINT ( 'NONE',  ( 11.95348876160960039, -4.885820101980599794, 6.578783887955899523 ) ) ;
#54860=CARTESIAN_POINT ( 'NONE',  ( 12.14633327354034797, -4.864904118400500188, 8.065722083251399610 ) ) ;
#54892=CARTESIAN_POINT ( 'NONE',  ( 10.76539516633362581, -3.766791217824746241, 6.656705459454948404 ) ) ;
#54900=EDGE_LOOP ( 'NONE', ( #33435, #56409, #459 ) ) ;
#54911=CARTESIAN_POINT ( 'NONE',  ( 9.402126402770999647, -3.188752782784400441, 7.805918119494599239 ) ) ;
#54918=CARTESIAN_POINT ( 'NONE',  ( 9.396714042595458949, -4.136150106425177775, 8.546714100015048388 ) ) ;
#54927=ORIENTED_EDGE ( 'NONE', *, *, #3959, .T. ) ;
#54957=CARTESIAN_POINT ( 'NONE',  ( 10.88351354018329431, -5.249999999999998224, 7.663624617374469317 ) ) ;
#54968=ADVANCED_FACE ( 'NONE', ( #45035 ), #1339, .T. ) ;
#54996=CARTESIAN_POINT ( 'NONE',  ( 9.798392757686999133, -3.414780058706900157, 6.860292594369099106 ) ) ;
#54998=CARTESIAN_POINT ( 'NONE',  ( 11.16476354018302430, -2.782534154164604256, 7.827184855449094592 ) ) ;
#55078=CARTESIAN_POINT ( 'NONE',  ( 9.703113844318000503, -3.676949563211899807, 8.737749087159000894 ) ) ;
#55082=CARTESIAN_POINT ( 'NONE',  ( 12.09999999999999609, -4.745632530848082453, 6.836536274993706641 ) ) ;
#55132=ORIENTED_EDGE ( 'NONE', *, *, #40725, .F. ) ;
#55153=CARTESIAN_POINT ( 'NONE',  ( 10.90333997687999990, -3.786145554879500441, 8.480416814141699788 ) ) ;
#55195=CARTESIAN_POINT ( 'NONE',  ( 9.980671671056999372, -5.126041103316000047, 7.310881302803900361 ) ) ;
#55198=CARTESIAN_POINT ( 'NONE',  ( 11.97810404293059960, -4.563346034752700398, 6.352848032645000309 ) ) ;
#55208=CARTESIAN_POINT ( 'NONE',  ( 12.09603632436369125, -4.842640371965599932, 7.696781148700499564 ) ) ;
#55239=CARTESIAN_POINT ( 'NONE',  ( 10.10683733959362662, -4.864872534707646246, 7.632392475727677095 ) ) ;
#55262=CARTESIAN_POINT ( 'NONE',  ( 9.932025935145999185, -4.145841638824199649, 8.493766832166899761 ) ) ;
#55286=CARTESIAN_POINT ( 'NONE',  ( 9.727255459545908423, -3.370461114521380530, 8.592254274082836929 ) ) ;
#55305=CARTESIAN_POINT ( 'NONE',  ( 10.87309687351658205, -5.217465845835394411, 7.827184855449101697 ) ) ;
#55343=CARTESIAN_POINT ( 'NONE',  ( 11.21684687351633869, -3.231816600031351516, 8.499583552997721725 ) ) ;
#55384=CARTESIAN_POINT ( 'NONE',  ( 11.60391045180384317, -2.870950512581996961, 6.885461205208885715 ) ) ;
#55395=ORIENTED_EDGE ( 'NONE', *, *, #22558, .T. ) ;
#55428=CARTESIAN_POINT ( 'NONE',  ( 10.23502593514599823, -4.185743043590700374, 8.765655525501999890 ) ) ;
#55497=CARTESIAN_POINT ( 'NONE',  ( 11.50008140503725329, -2.915874161187789859, 7.632269737612043414 ) ) ;
#55502=CARTESIAN_POINT ( 'NONE',  ( 11.78949010443639978, -2.999324937259999935, 7.425165037173959703 ) ) ;
#55529=B_SPLINE_CURVE_WITH_KNOTS ( 'NONE', 3,
 ( #49059, #56029, #18288, #50439 ),
 .UNSPECIFIED., .F., .F.,
 ( 4, 4 ),
 ( 0.000000000000000000, 1.000000000000000000 ),
 .UNSPECIFIED. ) ;
#55544=CARTESIAN_POINT ( 'NONE',  ( 9.552088727411000235, -5.000897406023000258, 7.416055476975279781 ) ) ;
#55547=CARTESIAN_POINT ( 'NONE',  ( 11.14533863405319991, -3.296214805808900028, 6.602238051205399749 ) ) ;
#55556=CARTESIAN_POINT ( 'NONE',  ( 11.90841235500450068, -4.841138636481000290, 8.270568563129298667 ) ) ;
#55557=CARTESIAN_POINT ( 'NONE',  ( 11.56967835872019990, -4.754733798270200928, 7.975673736933100777 ) ) ;
#55610=CARTESIAN_POINT ( 'NONE',  ( 10.76788779216199998, -3.070969952137800441, 7.164969140522200242 ) ) ;
#55616=CARTESIAN_POINT ( 'NONE',  ( 9.416525748329496182, -4.536323992761255752, 8.432246543101925340 ) ) ;
#55654=CARTESIAN_POINT ( 'NONE',  ( 10.77934687351620546, -4.163624617374463988, 8.750000000000001776 ) ) ;
#55710=CARTESIAN_POINT ( 'NONE',  ( 10.50551210286899995, -4.217228369037729685, 6.243812680477911492 ) ) ;
#55733=CARTESIAN_POINT ( 'NONE',  ( 11.47028665956023197, -4.742415037725370652, 6.450604656432373574 ) ) ;
#55773=CARTESIAN_POINT ( 'NONE',  ( 10.30900081823999948, -5.010295986746999830, 6.967988282883199602 ) ) ;
#55788=CARTESIAN_POINT ( 'NONE',  ( 11.57299956498199833, -2.792989229543000107, 7.174999999999999822 ) ) ;
#55847=CARTESIAN_POINT ( 'NONE',  ( 10.85410941423799791, -3.257202320419700037, 8.174686939644999484 ) ) ;
#55874=B_SPLINE_CURVE_WITH_KNOTS ( 'NONE', 3,
 ( #17707, #39030, #45310, #13834, #66616, #50890, #34819, #60345, #2985, #49855 ),
 .UNSPECIFIED., .F., .F.,
 ( 4, 2, 2, 2, 4 ),
 ( 0.000000000000000000, 0.2500000000000006661, 0.5000000000000013323, 0.7500000000000006661, 1.000000000000000000 ),
 .UNSPECIFIED. ) ;
#55890=CARTESIAN_POINT ( 'NONE',  ( 9.400113844317999678, -3.746347404385800051, 8.471855267550699509 ) ) ;
#55891=VERTEX_POINT ( 'NONE', #44453 ) ;
#55893=CARTESIAN_POINT ( 'NONE',  ( 11.29303032197930001, -3.336467919271199900, 8.427909097977700270 ) ) ;
#55902=CARTESIAN_POINT ( 'NONE',  ( 11.24795391537420031, -3.169881940022800215, 6.936213817702099327 ) ) ;
#55903=CARTESIAN_POINT ( 'NONE',  ( 11.32035090130999855, -3.241273085157000189, 7.030721746772699454 ) ) ;
#55934=VERTEX_POINT ( 'NONE', #29755 ) ;
#55938=CARTESIAN_POINT ( 'NONE',  ( 12.26077869730539938, -4.595338376575799799, 8.673950353177000139 ) ) ;
#55950=CARTESIAN_POINT ( 'NONE',  ( 9.856038493598999750, -3.273092657276900130, 8.193143574899998782 ) ) ;
#56029=CARTESIAN_POINT ( 'NONE',  ( 11.49999970531878546, -5.098631745860898512, 7.402706825368051469 ) ) ;
#56073=CARTESIAN_POINT ( 'NONE',  ( 10.77101354018233259, -4.768183399968641822, 8.499583552997725278 ) ) ;
#56107=CARTESIAN_POINT ( 'NONE',  ( 9.979721904869998994, -3.004358235431599855, 6.941043897400199114 ) ) ;
#56188=CARTESIAN_POINT ( 'NONE',  ( 11.56379841651039975, -4.401637675674300532, 6.432302808027999141 ) ) ;
#56227=CARTESIAN_POINT ( 'NONE',  ( 9.628076168957999670, -4.509700402263200125, 6.634524523592600254 ) ) ;
#56230=CARTESIAN_POINT ( 'NONE',  ( 10.94841638348500013, -5.108333310975999630, 7.769976643522699788 ) ) ;
#56242=CARTESIAN_POINT ( 'NONE',  ( 11.74025954179439957, -3.228187097503200320, 6.858707791728399172 ) ) ;
#56276=ORIENTED_EDGE ( 'NONE', *, *, #61590, .T. ) ;
#56296=CARTESIAN_POINT ( 'NONE',  ( 10.36262143724500007, -3.332852462363599777, 8.250837174995698575 ) ) ;
#56317=CARTESIAN_POINT ( 'NONE',  ( 11.91672066707849886, -3.258843737379200078, 7.948314604624900248 ) ) ;
#56378=CARTESIAN_POINT ( 'NONE',  ( 9.545101285863999863, -4.558267473659599389, 8.163359157892799089 ) ) ;
#56409=ORIENTED_EDGE ( 'NONE', *, *, #22558, .F. ) ;
#56413=CARTESIAN_POINT ( 'NONE',  ( 10.83744474310099903, -3.228742141949900279, 7.125715588371799747 ) ) ;
#56422=CARTESIAN_POINT ( 'NONE',  ( 10.63559687351566474, -2.907767014557175678, 8.129523725463618788 ) ) ;
#56455=CARTESIAN_POINT ( 'NONE',  ( 10.25834252387499923, -5.128664655368000425, 7.672773098917999413 ) ) ;
#56530=CARTESIAN_POINT ( 'NONE',  ( 10.82949413291699869, -3.087070836781100169, 7.916546720849799712 ) ) ;
#56553=AXIS2_PLACEMENT_3D ( 'NONE', #19686, #46943, #41008 ) ;
#56571=CARTESIAN_POINT ( 'NONE',  ( 9.398101285863999621, -4.735211557675400584, 8.373612278672599274 ) ) ;
#56574=CARTESIAN_POINT ( 'NONE',  ( 11.11656919669529842, -2.774362666861999838, 7.137881914002699446 ) ) ;
#56585=CARTESIAN_POINT ( 'NONE',  ( 11.83456651104149948, -3.887457492043800311, 8.635175889530000148 ) ) ;
#56610=CARTESIAN_POINT ( 'NONE',  ( 10.58521345716900086, -3.075109701058799772, 6.659120737011199331 ) ) ;
#56621=CARTESIAN_POINT ( 'NONE',  ( 11.59590547754519996, -2.684394667508000154, 7.458246194669389872 ) ) ;
#56637=CARTESIAN_POINT ( 'NONE',  ( 12.09999999999999964, -3.579171096429341503, 8.516100029838437280 ) ) ;
#56660=CARTESIAN_POINT ( 'NONE',  ( 11.46949144726329983, -4.580206776679999869, 8.318725197575499664 ) ) ;
#56697=B_SPLINE_CURVE_WITH_KNOTS ( 'NONE', 3,
 ( #14851, #36514, #63062, #15190, #57838, #30935, #8917, #36172, #20435, #26377, #57483, #9245, #10287, #31621, #9946, #26027, #19753, #52942 ),
 .UNSPECIFIED., .F., .F.,
 ( 4, 2, 2, 2, 2, 2, 2, 2, 4 ),
 ( 0.000000000000000000, 0.1250000000000000000, 0.2500000000000000000, 0.3750000000000000000, 0.5000000000000000000, 0.6250000000000000000, 0.7500000000000000000, 0.8750000000000000000, 1.000000000000000000 ),
 .UNSPECIFIED. ) ;
#56725=CARTESIAN_POINT ( 'NONE',  ( 9.494442991499999707, -4.054579081944059915, 8.365291319916600798 ) ) ;
#56726=CARTESIAN_POINT ( 'NONE',  ( 9.248004441081999261, -4.389076025353599420, 6.658556819429599649 ) ) ;
#56742=CARTESIAN_POINT ( 'NONE',  ( 11.98011496860029901, -3.080230834057799960, 7.971338736265699332 ) ) ;
#56758=CARTESIAN_POINT ( 'NONE',  ( 12.16287348028854964, -4.761955701524100526, 7.088026579158399620 ) ) ;
#56763=CARTESIAN_POINT ( 'NONE',  ( 10.56726717315599906, -4.659895246859299789, 8.062357722167599050 ) ) ;
#56775=ORIENTED_EDGE ( 'NONE', *, *, #43902, .F. ) ;
#56796=EDGE_LOOP ( 'NONE', ( #43307, #34593, #8963, #59235, #60246 ) ) ;
#56804=CARTESIAN_POINT ( 'NONE',  ( 9.650442991499998513, -4.071878040089889517, 8.639547276484998761 ) ) ;
#56875=CARTESIAN_POINT ( 'NONE',  ( 11.71149010443640037, -2.862435565199000109, 7.414927836855409460 ) ) ;
#56912=CARTESIAN_POINT ( 'NONE',  ( 10.20662143724499948, -3.150324864944999970, 8.456261759323901117 ) ) ;
#56923=CARTESIAN_POINT ( 'NONE',  ( 11.72056920625029974, -3.952687217764870198, 8.815417147437999645 ) ) ;
#56925=CARTESIAN_POINT ( 'NONE',  ( 10.84995525820099971, -4.107710726525199973, 8.635644537520001052 ) ) ;
#56960=CARTESIAN_POINT ( 'NONE',  ( 11.22702344389999851, -5.004394439171999664, 8.109550315577399360 ) ) ;
#56964=ADVANCED_FACE ( 'NONE', ( #52258 ), #24319, .T. ) ;
#56983=CARTESIAN_POINT ( 'NONE',  ( 11.83810207955129989, -3.203462856645999945, 7.174999999999999822 ) ) ;
#56999=CARTESIAN_POINT ( 'NONE',  ( 10.93210941423800087, -3.358814833524500276, 8.082391773166900606 ) ) ;
#57012=ORIENTED_EDGE ( 'NONE', *, *, #15309, .F. ) ;
#57028=CARTESIAN_POINT ( 'NONE',  ( 9.502376473208929752, -4.922128563344212004, 6.792422036439461408 ) ) ;
#57029=SURFACE_STYLE_FILL_AREA ( #46202 ) ;
#57042=CARTESIAN_POINT ( 'NONE',  ( 10.95672469555900008, -3.566534988568399900, 8.249937779480299938 ) ) ;
#57047=CARTESIAN_POINT ( 'NONE',  ( 9.099999952505998024, -4.749999993641800700, 7.500000000000000000 ) ) ;
#57057=CARTESIAN_POINT ( 'NONE',  ( 9.255786719645998417, -4.065290607273509771, 6.597079156813799194 ) ) ;
#57072=CARTESIAN_POINT ( 'NONE',  ( 10.94999293566599974, -3.279967330949900450, 6.616719557880299085 ) ) ;
#57091=CARTESIAN_POINT ( 'NONE',  ( 10.38996314287999922, -3.151633609938700342, 7.678836273503299559 ) ) ;
#57134=CARTESIAN_POINT ( 'NONE',  ( 10.63827973160999818, -3.897539901865500145, 8.637205511891998810 ) ) ;
#57136=CARTESIAN_POINT ( 'NONE',  ( 12.09610237318921655, -4.810409949404850671, 7.825049231485562196 ) ) ;
#57202=CARTESIAN_POINT ( 'NONE',  ( 9.234814475091134511, -3.943962993865710587, 6.616514917701350029 ) ) ;
#57205=CARTESIAN_POINT ( 'NONE',  ( 11.09610807141099897, -3.947296672195129918, 6.360477084256999980 ) ) ;
#57219=CARTESIAN_POINT ( 'NONE',  ( 9.261230081853240037, -3.478588282862478120, 6.718925885376237694 ) ) ;
#57241=CARTESIAN_POINT ( 'NONE',  ( 10.30793802597399988, -4.665064168510499876, 8.592736948783000983 ) ) ;
#57253=CARTESIAN_POINT ( 'NONE',  ( 11.26346886766499900, -4.634677072395899877, 8.653146038559000885 ) ) ;
#57255=CARTESIAN_POINT ( 'NONE',  ( 11.34226088462130022, -3.997572771977982775, 8.640738455926999961 ) ) ;
#57256=CARTESIAN_POINT ( 'NONE',  ( 10.90480513896000048, -3.220259576336399920, 7.933462475324499330 ) ) ;
#57280=CARTESIAN_POINT ( 'NONE',  ( 10.62435795695566476, -2.750000000000000000, 7.192559817601734906 ) ) ;
#57292=CARTESIAN_POINT ( 'NONE',  ( 11.26857802013510046, -5.174568897094999897, 7.527343341769989316 ) ) ;
#57333=CARTESIAN_POINT ( 'NONE',  ( 11.76487482311540056, -3.069598554678400149, 7.124095752359899336 ) ) ;
#57339=CARTESIAN_POINT ( 'NONE',  ( 12.33003632436370012, -5.243255406354000669, 7.790336465152099876 ) ) ;
#57361=SHAPE_REPRESENTATION_RELATIONSHIP ( 'NONE' , 'NONE' ,  #60729, #18558 ) ;
#57378=CARTESIAN_POINT ( 'NONE',  ( 12.01518179236249040, -4.180996681294200101, 8.347076615013298451 ) ) ;
#57390=CARTESIAN_POINT ( 'NONE',  ( 9.227215710425999973, -4.373963964882100264, 6.691239224408199071 ) ) ;
#57409=CARTESIAN_POINT ( 'NONE',  ( 11.93856039236529831, -2.967715280237000375, 7.449760924956519759 ) ) ;
#57410=B_SPLINE_CURVE_WITH_KNOTS ( 'NONE', 3,
 ( #41437, #62744, #14864, #53642, #26740, #27420, #42810, #58536, #21143, #38245, #37904, #69030, #42469, #5403, #22165, #63777, #59572, #16579 ),
 .UNSPECIFIED., .F., .F.,
 ( 4, 2, 2, 2, 2, 2, 2, 2, 4 ),
 ( 0.000000000000000000, 0.1250000000000000000, 0.2500000000000000000, 0.3750000000000000000, 0.5000000000000000000, 0.6250000000000000000, 0.7500000000000000000, 0.8750000000000000000, 1.000000000000000000 ),
 .UNSPECIFIED. ) ;
#57416=DIRECTION ( 'NONE',  ( -1.000000000000000000, 0.000000000000000000, 0.000000000000000000 ) ) ;
#57424=CARTESIAN_POINT ( 'NONE',  ( 12.18748876160954886, -4.600381688599499697, 6.875627981711399883 ) ) ;
#57428=CARTESIAN_POINT ( 'NONE',  ( 10.11134252387499899, -4.857027829858100887, 7.631191628371899682 ) ) ;
#57448=CARTESIAN_POINT ( 'NONE',  ( 11.83810207955129989, -3.203462856645999945, 7.174999999999999822 ) ) ;
#57469=CARTESIAN_POINT ( 'NONE',  ( 9.574455549952999078, -3.111370763671500228, 8.216988513669100769 ) ) ;
#57483=CARTESIAN_POINT ( 'NONE',  ( 10.99809687351654119, -4.327184855449103473, 6.282534154164607365 ) ) ;
#57524=VERTEX_POINT ( 'NONE', #49954 ) ;
#57537=ORIENTED_EDGE ( 'NONE', *, *, #50603, .T. ) ;
#57551=CARTESIAN_POINT ( 'NONE',  ( 11.60887482311539998, -2.815046254222000055, 7.021250586468399391 ) ) ;
#57573=CARTESIAN_POINT ( 'NONE',  ( 9.310863317747999801, -3.039136629551499880, 7.499999999926881600 ) ) ;
#57586=CARTESIAN_POINT ( 'NONE',  ( 9.550076168958000267, -4.579425901182000658, 6.516130052788599691 ) ) ;
#57592=LINE ( 'NONE', #60876, #10008 ) ;
#57598=CARTESIAN_POINT ( 'NONE',  ( 11.96989666366029859, -4.058428102321880004, 6.185029684353999357 ) ) ;
#57601=CARTESIAN_POINT ( 'NONE',  ( 10.70226357027499908, -2.879914860223000250, 7.283900408233900059 ) ) ;
#57638=CARTESIAN_POINT ( 'NONE',  ( 11.31013259637009938, -5.031671030421000168, 6.937848198857199833 ) ) ;
#57676=CARTESIAN_POINT ( 'NONE',  ( 11.64179841651039915, -4.353306409735099969, 6.560784671286499226 ) ) ;
#57705=VERTEX_POINT ( 'NONE', #23726 ) ;
#57711=EDGE_CURVE ( 'NONE', #43682, #4376, #65443, .T. ) ;
#57724=CARTESIAN_POINT ( 'NONE',  ( 11.67056785386840012, -4.718624889240500053, 7.016391833292499491 ) ) ;
#57737=ORIENTED_EDGE ( 'NONE', *, *, #60574, .F. ) ;
#57754=CARTESIAN_POINT ( 'NONE',  ( 11.06591429142999949, -3.980313504646230349, 8.533318907609000803 ) ) ;
#57771=CARTESIAN_POINT ( 'NONE',  ( 11.00595525820100029, -4.081787880721680750, 8.362327856951900173 ) ) ;
#57819=CARTESIAN_POINT ( 'NONE',  ( 9.447809814040999399, -3.301541394817099739, 6.596733927440100231 ) ) ;
#57838=CARTESIAN_POINT ( 'NONE',  ( 11.09184687351642751, -3.000416447002275167, 6.731816600031356401 ) ) ;
#57891=CARTESIAN_POINT ( 'NONE',  ( 11.64975833414749928, -4.796537143354000499, 7.174999999999999822 ) ) ;
#57906=CARTESIAN_POINT ( 'NONE',  ( 11.83041235500449950, -4.942357465271699724, 8.363295307663500822 ) ) ;
#57943=CARTESIAN_POINT ( 'NONE',  ( 9.626063610504999701, -3.531653260805799999, 6.458661544034999480 ) ) ;
#57956=CARTESIAN_POINT ( 'NONE',  ( 12.33003632436370012, -5.243255406354000669, 7.790336465152099876 ) ) ;
#57958=CARTESIAN_POINT ( 'NONE',  ( 11.09610807141099897, -3.947296672195129918, 6.360477084256999980 ) ) ;
#57979=CARTESIAN_POINT ( 'NONE',  ( 11.87299956498129916, -5.207010770456999893, 7.825000000000000178 ) ) ;
#57993=CARTESIAN_POINT ( 'NONE',  ( 12.10988784977536525, -4.851105903694400645, 7.548634759728509280 ) ) ;
#58036=CARTESIAN_POINT ( 'NONE',  ( 11.03057053952199951, -4.340412141385700195, 8.296503712697200328 ) ) ;
#58043=CARTESIAN_POINT ( 'NONE',  ( 12.26077869730539938, -4.595338376575799799, 8.673950353177000139 ) ) ;
#58080=CARTESIAN_POINT ( 'NONE',  ( 11.59672200990539892, -4.817867935977999672, 7.785290430335599865 ) ) ;
#58108=CARTESIAN_POINT ( 'NONE',  ( 12.14633327354034797, -4.864904118400500188, 8.065722083251399610 ) ) ;
#58115=FACE_OUTER_BOUND ( 'NONE', #62384, .T. ) ;
#58125=CARTESIAN_POINT ( 'NONE',  ( 11.93718179236249988, -4.209680326224799707, 8.481317998227099864 ) ) ;
#58136=CARTESIAN_POINT ( 'NONE',  ( 9.565735834902588053, -3.588654020114534049, 6.337235623390005124 ) ) ;
#58170=CARTESIAN_POINT ( 'NONE',  ( 9.724417874593999755, -4.924352284713100047, 7.107043063332000088 ) ) ;
#58195=ORIENTED_EDGE ( 'NONE', *, *, #31322, .F. ) ;
#58218=CARTESIAN_POINT ( 'NONE',  ( 9.307788144226000426, -3.909067355573210278, 6.546538158064899804 ) ) ;
#58244=CARTESIAN_POINT ( 'NONE',  ( 10.67764828895399987, -2.998858038575999974, 6.953185708700699408 ) ) ;
#58285=CARTESIAN_POINT ( 'NONE',  ( 10.10226354018233330, -2.907767014557176566, 6.870476274536374106 ) ) ;
#58291=CARTESIAN_POINT ( 'NONE',  ( 11.59590547754519996, -2.684394667508000154, 7.458246194669389872 ) ) ;
#58293=CARTESIAN_POINT ( 'NONE',  ( 10.96887750876899936, -4.692271380433699512, 6.425720373262999274 ) ) ;
#58300=CARTESIAN_POINT ( 'NONE',  ( 9.099999986286999132, -4.750000013710600655, 7.500000000038047787 ) ) ;
#58310=EDGE_CURVE ( 'NONE', #68324, #50475, #47001, .T. ) ;
#58314=ORIENTED_EDGE ( 'NONE', *, *, #15474, .T. ) ;
#58330=CARTESIAN_POINT ( 'NONE',  ( 11.89700581613019992, -3.130347327833300053, 6.941573685175900010 ) ) ;
#58370=CARTESIAN_POINT ( 'NONE',  ( 11.95764291764649911, -5.132124077409000229, 7.639947095788999221 ) ) ;
#58376=CARTESIAN_POINT ( 'NONE',  ( 12.01145123989533126, -3.394760891061399999, 6.331134574721999364 ) ) ;
#58414=CARTESIAN_POINT ( 'NONE',  ( 11.22749279009020107, -4.225282629687599822, 6.663611138821799784 ) ) ;
#58461=CARTESIAN_POINT ( 'NONE',  ( 12.03564291764652872, -4.995889373412399692, 7.623106493640399606 ) ) ;
#58507=CARTESIAN_POINT ( 'NONE',  ( 10.61093802597399893, -4.522194782554399772, 8.357994702431799539 ) ) ;
#58532=VERTEX_POINT ( 'NONE', #26399 ) ;
#58536=CARTESIAN_POINT ( 'NONE',  ( 10.44809687351624916, -4.327184855449103473, 6.282534154164604701 ) ) ;
#58590=CARTESIAN_POINT ( 'NONE',  ( 11.78118179236250107, -4.267047616085000605, 8.749800764654999341 ) ) ;
#58637=CARTESIAN_POINT ( 'NONE',  ( 10.99349279008999858, -4.332388355267299929, 6.265968249244999733 ) ) ;
#58643=ORIENTED_EDGE ( 'NONE', *, *, #1740, .F. ) ;
#58649=B_SPLINE_SURFACE_WITH_KNOTS ( 'NONE', 3, 3, ( 
 ( #51757, #57339, #63267, #58043, #10144, #46179, #67486, #64646, #58722, #58376, #68860, #48232, #22349, #42318, #21999, #6262, #20982, #27600, #47901, #32850, #37742, #48930, #338, #10482, #31820, #27259, #37064, #42988, #26918, #17098, #43342, #4889, #16752, #16411, #53139 ),
 ( #26579, #38080, #48583, #37401, #20726, #11856, #1036, #10826, #33195, #54162, #43687, #64297, #5917, #53483, #21655, #21318, #26230, #15736, #38431, #687, #32170, #59406, #11506, #64983, #47559, #42647, #53820, #63619, #59754, #5239, #5576, #63958, #16068, #59069, #11170 ),
 ( #32505, #38783, #54860, #60110, #60797, #2411, #12214, #6615, #6962, #45416, #2075, #49264, #28293, #49961, #66376, #8007, #17812, #49613, #66030, #29343, #65339, #23734, #33544, #13263, #44733, #18500, #1720, #34588, #18154, #39825, #23393, #23040, #44389, #17458, #65689 ),
 ( #27953, #55208, #45072, #61145, #39128, #39475, #24079, #50312, #54514, #7308, #60454, #12910, #40171, #34238, #55557, #12559, #33891, #7657, #28650, #61487, #55903, #22692, #13605, #29003, #50655, #2755, #66725, #18845, #1374, #44036, #57256, #41529, #35613, #25797, #20551 ) ),
 .UNSPECIFIED., .F., .F., .F.,
 ( 4, 4 ),
 ( 4, 1, 1, 1, 1, 1, 1, 1, 1, 1, 1, 1, 1, 1, 1, 1, 1, 1, 1, 1, 1, 1, 1, 1, 1, 1, 1, 1, 1, 1, 1, 1, 4 ),
 ( -0.02000000000000000042, 1.020000000000000018 ),
 ( 0.1633025096610999927, 0.1899619885200000136, 0.2166214673788000034, 0.2432809462376999965, 0.2699404250964999585, 0.2965999039553000038, 0.3232593828141999692, 0.3499188616730000145, 0.3765783405318000043, 0.4032378193906999697, 0.4298972982494999595, 0.4565567771083000048, 0.4832162559671999702, 0.5098757348260000155, 0.5365352136848999809, 0.5631946925437000262, 0.5898541714025000715, 0.6165136502614000369, 0.6431731291201999712, 0.6698326079790000165, 0.6964920868378999819, 0.7231515656967000272, 0.7498110445554999615, 0.7764705234143999268, 0.8031300022731999722, 0.8297894811320000175, 0.8564489599908999828, 0.8831084388497000282, 0.9097679177085999935, 0.9364273965674000388, 0.9630868754261999731, 0.9897463542851000495, 1.016405833144000015 ),
 .UNSPECIFIED. ) ;
#58676=CARTESIAN_POINT ( 'NONE',  ( 11.52301463001509951, -3.452642973349600464, 8.376661845795100092 ) ) ;
#58715=B_SPLINE_CURVE_WITH_KNOTS ( 'NONE', 3,
 ( #30136, #47839, #19630, #35711, #16008, #57028, #9128, #51781, #28584, #27540 ),
 .UNSPECIFIED., .F., .F.,
 ( 4, 2, 2, 2, 4 ),
 ( 0.3934091950370091628, 0.5450568962777568860, 0.6967045975185046647, 0.8483522987592523323, 1.000000000000000000 ),
 .UNSPECIFIED. ) ;
#58716=CARTESIAN_POINT ( 'NONE',  ( 12.10533460557258323, -3.815825449682300086, 6.374224726731999802 ) ) ;
#58722=CARTESIAN_POINT ( 'NONE',  ( 12.05300581613033906, -2.892415530317000272, 6.788791567531699656 ) ) ;
#58742=CARTESIAN_POINT ( 'NONE',  ( 12.08810207955109917, -4.796537143354000499, 7.825000000000000178 ) ) ;
#58756=CARTESIAN_POINT ( 'NONE',  ( 11.49410672858429905, -4.801902424331299990, 8.103244025831999764 ) ) ;
#58791=CARTESIAN_POINT ( 'NONE',  ( 11.02946886766499901, -4.430164648092599577, 8.281567006984099422 ) ) ;
#58802=CARTESIAN_POINT ( 'NONE',  ( 11.47755399909358154, -3.866653594937912608, 6.221473734489901375 ) ) ;
#58806=CARTESIAN_POINT ( 'NONE',  ( 11.62133729122639991, -4.865898216891100247, 7.522778681411049995 ) ) ;
#58827=ADVANCED_FACE ( 'NONE', ( #25627 ), #2183, .F. ) ;
#58853=CARTESIAN_POINT ( 'NONE',  ( 10.45896314288000006, -3.017187828228399926, 7.707177545471399327 ) ) ;
#58938=CARTESIAN_POINT ( 'NONE',  ( 11.70733594839949809, -3.159733897807000425, 8.462948211532999920 ) ) ;
#58975=CARTESIAN_POINT ( 'NONE',  ( 9.624051052051999733, -2.744602294987000146, 7.254315263553399618 ) ) ;
#58978=DIRECTION ( 'NONE',  ( 0.000000000000000000, 1.000000000000000000, 0.000000000000000000 ) ) ;
#58990=CARTESIAN_POINT ( 'NONE',  ( 11.73195122972050086, -3.492749840905900349, 8.673036084990000560 ) ) ;
#59017=PRODUCT_DEFINITION ( 'UNKNOWN', '', #32954, #68144 ) ;
#59024=CARTESIAN_POINT ( 'NONE',  ( 11.93856039236529831, -2.967715280237000375, 7.449760924956519759 ) ) ;
#59062=CARTESIAN_POINT ( 'NONE',  ( 11.05103166480599874, -5.000984463463999496, 7.429424106427209296 ) ) ;
#59069=CARTESIAN_POINT ( 'NONE',  ( 10.94999293566599974, -3.279967330949900450, 6.616719557880299085 ) ) ;
#59075=CARTESIAN_POINT ( 'NONE',  ( 9.099999986286999132, -3.249999986289399789, 7.499999999961952213 ) ) ;
#59128=B_SPLINE_CURVE_WITH_KNOTS ( 'NONE', 3,
 ( #31219, #5996, #59485, #6340, #48660, #58802, #10562, #21059, #26307, #4974 ),
 .UNSPECIFIED., .F., .F.,
 ( 4, 2, 2, 2, 4 ),
 ( 0.000000000000000000, 0.2500000000000000000, 0.5000000000000000000, 0.7500000000000000000, 1.000000000000000000 ),
 .UNSPECIFIED. ) ;
#59133=CARTESIAN_POINT ( 'NONE',  ( 10.79399293566600093, -3.453258297007899991, 6.829299525004299376 ) ) ;
#59146=CARTESIAN_POINT ( 'NONE',  ( 11.79364426047339975, -3.533902447304699823, 6.769896129503799820 ) ) ;
#59166=VECTOR ( 'NONE', #38605, 1000.000000000000227 ) ;
#59178=ADVANCED_FACE ( 'NONE', ( #46264 ), #5880, .F. ) ;
#59196=CARTESIAN_POINT ( 'NONE',  ( 10.58359632033899977, -4.802737635155300389, 7.827597670336898794 ) ) ;
#59215=CARTESIAN_POINT ( 'NONE',  ( 12.23671932425159881, -4.127012898954600217, 6.643164954553199664 ) ) ;
#59235=ORIENTED_EDGE ( 'NONE', *, *, #51445, .T. ) ;
#59272=CARTESIAN_POINT ( 'NONE',  ( 10.82118582084300051, -4.836160649475099937, 8.466515260542900378 ) ) ;
#59278=CARTESIAN_POINT ( 'NONE',  ( 9.956405316140999773, -4.271593136661399726, 6.249951378708000327 ) ) ;
#59311=CARTESIAN_POINT ( 'NONE',  ( 9.066809814040999171, -3.217492037304399588, 6.488038963273999649 ) ) ;
#59326=CARTESIAN_POINT ( 'NONE',  ( 10.62426357027499968, -2.745128867668000350, 7.257895958275299542 ) ) ;
#59360=EDGE_CURVE ( 'NONE', #41424, #54112, #41913, .T. ) ;
#59361=CARTESIAN_POINT ( 'NONE',  ( 11.15413259636999932, -4.783377755405500587, 7.073141822156699732 ) ) ;
#59400=CARTESIAN_POINT ( 'NONE',  ( 11.71149010443640037, -2.862435565199000109, 7.414927836855409460 ) ) ;
#59406=CARTESIAN_POINT ( 'NONE',  ( 11.43479632507519916, -3.442212747724900268, 6.465962698293999722 ) ) ;
#59436=CARTESIAN_POINT ( 'NONE',  ( 10.61342028323962872, -4.872854478606138073, 7.560475846972328995 ) ) ;
#59474=CARTESIAN_POINT ( 'NONE',  ( 11.11257802013489915, -4.891884252872400474, 7.520762592984879369 ) ) ;
#59485=CARTESIAN_POINT ( 'NONE',  ( 11.38210843320517007, -5.137688304401064165, 6.901605483505062644 ) ) ;
#59489=CARTESIAN_POINT ( 'NONE',  ( 10.78026357027499849, -3.014700852776899698, 7.309904858193100097 ) ) ;
#59499=VECTOR ( 'NONE', #22823, 1000.000000000000000 ) ;
#59544=CARTESIAN_POINT ( 'NONE',  ( 9.496455549952999675, -3.218304396998100003, 8.130709350565298976 ) ) ;
#59554=CARTESIAN_POINT ( 'NONE',  ( 11.66486084871730000, -2.792989229543000107, 7.825000000000000178 ) ) ;
#59558=CARTESIAN_POINT ( 'NONE',  ( 11.56623059009865528, -4.687762524153129995, 8.035958501307058910 ) ) ;
#59563=CARTESIAN_POINT ( 'NONE',  ( 11.99056651104150006, -3.914543207408039738, 8.361971998931499783 ) ) ;
#59572=CARTESIAN_POINT ( 'NONE',  ( 10.58351354018237345, -2.750000000000000000, 7.336375382625531572 ) ) ;
#59616=EDGE_CURVE ( 'NONE', #35697, #43682, #32835, .T. ) ;
#59625=CARTESIAN_POINT ( 'NONE',  ( 10.59964828895399869, -2.878385131502000149, 6.887384543790600056 ) ) ;
#59630=CARTESIAN_POINT ( 'NONE',  ( 9.779101285863999848, -4.823683599683300294, 8.478738839062499366 ) ) ;
#59673=CARTESIAN_POINT ( 'NONE',  ( 10.09393020685000053, -2.750000000000000000, 7.500000000000000000 ) ) ;
#59675=CARTESIAN_POINT ( 'NONE',  ( 11.41195257254739914, -5.227167235646000165, 7.143100915737699452 ) ) ;
#59687=CARTESIAN_POINT ( 'NONE',  ( 11.89975833414730033, -3.203462856645999945, 7.825000000000000178 ) ) ;
#59709=CARTESIAN_POINT ( 'NONE',  ( 11.34393020684979980, -5.250000000000000000, 7.500000000000000000 ) ) ;
#59716=CARTESIAN_POINT ( 'NONE',  ( 10.81021345716900051, -3.363461959113699606, 6.921280946186199934 ) ) ;
#59747=CARTESIAN_POINT ( 'NONE',  ( 11.80995122972050027, -3.547233695387300045, 8.547040013405998948 ) ) ;
#59754=CARTESIAN_POINT ( 'NONE',  ( 11.14391429142989942, -3.977620450637519678, 8.674673860548999471 ) ) ;
#59784=CARTESIAN_POINT ( 'NONE',  ( 10.03084989804662719, -4.391573077584247642, 8.282433891029866047 ) ) ;
#59795=CARTESIAN_POINT ( 'NONE',  ( 11.51456785386839954, -4.946394603182100447, 6.863111178199799767 ) ) ;
#59820=ADVANCED_FACE ( 'NONE', ( #19354 ), #14464, .F. ) ;
#59826=CARTESIAN_POINT ( 'NONE',  ( 11.07102344389999971, -4.762665848028800220, 7.962849245488699879 ) ) ;
#59849=CARTESIAN_POINT ( 'NONE',  ( 10.64393020684899938, -2.750000000000000000, 7.500000000000000000 ) ) ;
#59871=DIRECTION ( 'NONE',  ( -0.5000000000000150990, 0.08222066253632250021, -0.8621135439442261239 ) ) ;
#59886=CARTESIAN_POINT ( 'NONE',  ( 10.48227973160899928, -3.922199073804859992, 8.363513150096299142 ) ) ;
#59888=CARTESIAN_POINT ( 'NONE',  ( 11.34184687351628540, -4.999583552997724389, 8.268183399968647151 ) ) ;
#59933=CARTESIAN_POINT ( 'NONE',  ( 10.19601354018233330, -3.000416447002272058, 8.268183399968641822 ) ) ;
#59973=CARTESIAN_POINT ( 'NONE',  ( 11.57907162307749971, -4.814611760850799449, 7.825000000000000178 ) ) ;
#59974=CARTESIAN_POINT ( 'NONE',  ( 10.38700081824000065, -5.131870447930000800, 6.903968392969799694 ) ) ;
#60026=CARTESIAN_POINT ( 'NONE',  ( 9.948096873516666605, -4.327184855449103473, 6.282534154164604701 ) ) ;
#60056=FACE_OUTER_BOUND ( 'NONE', #45327, .T. ) ;
#60058=CARTESIAN_POINT ( 'NONE',  ( 11.12487750876920067, -4.543557328885200697, 6.656497609330299881 ) ) ;
#60063=CIRCLE ( 'NONE', #62307, 0.7499999936418002555 ) ;
#60097=CARTESIAN_POINT ( 'NONE',  ( 10.18330484851600026, -2.961576783819000358, 7.025224608805800131 ) ) ;
#60100=CARTESIAN_POINT ( 'NONE',  ( 11.51041369783139956, -4.064477673403060543, 6.223614866029000048 ) ) ;
#60110=CARTESIAN_POINT ( 'NONE',  ( 12.10477869730532774, -4.467447516829900600, 8.421761806503198500 ) ) ;
#60138=CARTESIAN_POINT ( 'NONE',  ( 10.36012881141662767, -3.130392736003965393, 7.403483289911290122 ) ) ;
#60153=COLOUR_RGB ( '', 0.31764706, 0.68627451, 0.89019608) ;
#60162=CARTESIAN_POINT ( 'NONE',  ( 9.250151519676999001, -3.981249765141819719, 6.633192605878799775 ) ) ;
#60243=CARTESIAN_POINT ( 'NONE',  ( 10.07701337669299946, -4.772923352651200268, 7.892807122431200639 ) ) ;
#60245=CARTESIAN_POINT ( 'NONE',  ( 11.19601354018301365, -3.000416447002272058, 8.268183399968641822 ) ) ;
#60246=ORIENTED_EDGE ( 'NONE', *, *, #36263, .T. ) ;
#60287=ORIENTED_EDGE ( 'NONE', *, *, #6524, .F. ) ;
#60308=CARTESIAN_POINT ( 'NONE',  ( 11.50000000000000000, -4.968589424331200100, 7.825000000000000178 ) ) ;
#60310=CARTESIAN_POINT ( 'NONE',  ( 11.16684687351590277, -3.231816600031351516, 8.499583552997723501 ) ) ;
#60324=CARTESIAN_POINT ( 'NONE',  ( 10.28568422951000016, -4.901739481456999670, 8.407331414124799451 ) ) ;
#60345=CARTESIAN_POINT ( 'NONE',  ( 11.93114108301962162, -3.379311755690166841, 8.119401481368297979 ) ) ;
#60369=CARTESIAN_POINT ( 'NONE',  ( 11.54752711762115958, -2.837609288610280167, 7.175009463222314032 ) ) ;
#60402=CARTESIAN_POINT ( 'NONE',  ( 11.42026088462129962, -3.997864853650589634, 8.503467136482999678 ) ) ;
#60440=CARTESIAN_POINT ( 'NONE',  ( 10.05665911260400058, -4.496147888241900148, 6.471616938597000157 ) ) ;
#60443=CARTESIAN_POINT ( 'NONE',  ( 10.89918582084299992, -4.746348444722899629, 8.362701637490498996 ) ) ;
#60454=CARTESIAN_POINT ( 'NONE',  ( 11.73589666366019912, -4.039600775206940497, 6.608753462694600067 ) ) ;
#60482=CARTESIAN_POINT ( 'NONE',  ( 10.05617904522862638, -4.616765641734932757, 8.120590373834733811 ) ) ;
#60501=CARTESIAN_POINT ( 'NONE',  ( 10.31196314287999982, -3.017187828228399926, 7.707177545471399327 ) ) ;
#60512=CARTESIAN_POINT ( 'NONE',  ( 10.95551210286900101, -4.217228369037729685, 6.243812680477911492 ) ) ;
#60574=EDGE_CURVE ( 'NONE', #28137, #34321, #5011, .T. ) ;
#60586=CARTESIAN_POINT ( 'NONE',  ( 9.302265421554999136, -4.188500707411799695, 6.524915741324599949 ) ) ;
#60604=CARTESIAN_POINT ( 'NONE',  ( 11.69518313518939934, -4.537300658085600347, 6.820583637845799352 ) ) ;
#60617=FACE_OUTER_BOUND ( 'NONE', #53106, .T. ) ;
#60626=CARTESIAN_POINT ( 'NONE',  ( 11.62299956498149989, -2.792989229543000107, 7.174999999999999822 ) ) ;
#60630=ORIENTED_EDGE ( 'NONE', *, *, #44290, .T. ) ;
#60665=CARTESIAN_POINT ( 'NONE',  ( 10.08305105205200114, -2.744602294987000146, 7.254315263553399618 ) ) ;
#60709=CARTESIAN_POINT ( 'NONE',  ( 9.614639751325485761, -2.815014287255568348, 7.040280035170891182 ) ) ;
#60729=SHAPE_REPRESENTATION ( 'Terminal Screw', ( #9676 ), #9731 ) ;
#60741=CARTESIAN_POINT ( 'NONE',  ( 11.88795122972049967, -3.601717549869600354, 8.421043941822800249 ) ) ;
#60782=CARTESIAN_POINT ( 'NONE',  ( 9.803367640780999537, -3.461752753411900141, 8.506987760366000018 ) ) ;
#60786=CARTESIAN_POINT ( 'NONE',  ( 11.68272066707849888, -2.906477115133000222, 8.161456030935699602 ) ) ;
#60789=ORIENTED_EDGE ( 'NONE', *, *, #44680, .T. ) ;
#60796=CARTESIAN_POINT ( 'NONE',  ( 11.93302763632549990, -5.035790660926999784, 7.977941233841399971 ) ) ;
#60797=CARTESIAN_POINT ( 'NONE',  ( 12.06322412107030928, -3.945399343424460525, 8.532060764998998792 ) ) ;
#60849=CARTESIAN_POINT ( 'NONE',  ( 10.75944474310099963, -3.106516218291800246, 7.066400461213500073 ) ) ;
#60876=CARTESIAN_POINT ( 'NONE',  ( 11.87299956498129916, -5.207010770456999893, 7.825000000000000178 ) ) ;
#60933=CARTESIAN_POINT ( 'NONE',  ( 9.469113844317998741, -3.781046324972699768, 8.338908357746399602 ) ) ;
#60936=ORIENTED_EDGE ( 'NONE', *, *, #54718, .F. ) ;
#60943=UNCERTAINTY_MEASURE_WITH_UNIT (LENGTH_MEASURE( 1.000000000000000082E-05 ), #20656, 'distance_accuracy_value', 'NONE');
#60973=CARTESIAN_POINT ( 'NONE',  ( 11.48937577273788690, -4.461177266722074819, 6.300114087089553117 ) ) ;
#60977=CARTESIAN_POINT ( 'NONE',  ( 10.28976354018233152, -4.327184855449096368, 8.717465845835395299 ) ) ;
#61014=CARTESIAN_POINT ( 'NONE',  ( 10.99288779216199963, -2.943881405003000218, 7.119137915499500480 ) ) ;
#61025=CARTESIAN_POINT ( 'NONE',  ( 11.78830977893788301, -4.976598135215292373, 8.326430086672807818 ) ) ;
#61032=CARTESIAN_POINT ( 'NONE',  ( 10.14393020684900115, -2.750000000000000000, 7.500000000000000000 ) ) ;
#61089=CARTESIAN_POINT ( 'NONE',  ( 12.03564291764652872, -4.995889373412399692, 7.623106493640399606 ) ) ;
#61105=EDGE_LOOP ( 'NONE', ( #55395, #27959, #65086 ) ) ;
#61121=CIRCLE ( 'NONE', #30986, 1.250000000000000444 ) ;
#61132=CARTESIAN_POINT ( 'NONE',  ( 9.197480666858998788, -3.665111009453500213, 6.553061479084200336 ) ) ;
#61135=CARTESIAN_POINT ( 'NONE',  ( 11.92887348028849992, -5.124210964533999935, 6.892162778124999889 ) ) ;
#61144=CARTESIAN_POINT ( 'NONE',  ( 11.56795257254739973, -4.963546614172099858, 7.219770138693499817 ) ) ;
#61145=CARTESIAN_POINT ( 'NONE',  ( 12.02677869730533011, -4.403502086956500250, 8.295667533166499297 ) ) ;
#61182=CARTESIAN_POINT ( 'NONE',  ( 12.30233327354039830, -5.101536739857000846, 8.220500279733599314 ) ) ;
#61195=CARTESIAN_POINT ( 'NONE',  ( 9.830709346416998784, -3.092687088662700035, 7.930842873041400232 ) ) ;
#61256=STYLED_ITEM ( 'NONE', ( #34814 ), #53935 ) ;
#61262=LINE ( 'NONE', #9142, #42945 ) ;
#61281=VERTEX_POINT ( 'NONE', #52155 ) ;
#61321=CARTESIAN_POINT ( 'NONE',  ( 10.34184687351566545, -4.999583552997724389, 8.268183399968647151 ) ) ;
#61356=CARTESIAN_POINT ( 'NONE',  ( 10.94222949779799947, -3.366547096154099972, 6.550014196338999284 ) ) ;
#61401=CARTESIAN_POINT ( 'NONE',  ( 10.30226354018333268, -5.092232985442821658, 8.129523725463625894 ) ) ;
#61432=VERTEX_POINT ( 'NONE', #23792 ) ;
#61433=CARTESIAN_POINT ( 'NONE',  ( 11.73610538575739959, -2.890527834009000152, 7.765257665594799796 ) ) ;
#61441=EDGE_CURVE ( 'NONE', #4376, #64614, #18556, .T. ) ;
#61473=CARTESIAN_POINT ( 'NONE',  ( 10.41126717315600025, -4.869050473540199597, 8.240598219300300897 ) ) ;
#61476=CARTESIAN_POINT ( 'NONE',  ( 11.24379975933729980, -2.921317947059999920, 7.871126858273000515 ) ) ;
#61486=CARTESIAN_POINT ( 'NONE',  ( 10.80487885159599948, -3.003595720052600448, 7.618867373350600047 ) ) ;
#61487=CARTESIAN_POINT ( 'NONE',  ( 11.36190547754509872, -3.108323067758099967, 7.471700551735359852 ) ) ;
#61518=CARTESIAN_POINT ( 'NONE',  ( 9.625583543129627273, -4.871885936991885657, 7.426875573188317148 ) ) ;
#61536=CARTESIAN_POINT ( 'NONE',  ( 10.28663399569799886, -3.001718438313799808, 7.389201877599999690 ) ) ;
#61566=EDGE_CURVE ( 'NONE', #52202, #41699, #30116, .T. ) ;
#61590=EDGE_CURVE ( 'NONE', #36450, #53853, #5073, .T. ) ;
#61647=CARTESIAN_POINT ( 'NONE',  ( 12.01518179236249040, -4.180996681294200101, 8.347076615013298451 ) ) ;
#61654=CARTESIAN_POINT ( 'NONE',  ( 10.03535508232799955, -4.388021368982800041, 8.275336934318801241 ) ) ;
#61663=CARTESIAN_POINT ( 'NONE',  ( 10.67726354018233259, -3.370476274536371442, 8.592232985442818105 ) ) ;
#61694=CARTESIAN_POINT ( 'NONE',  ( 10.20768422950999899, -4.804883439508000897, 8.309874741421300115 ) ) ;
#61725=ORIENTED_EDGE ( 'NONE', *, *, #16417, .F. ) ;
#61769=CARTESIAN_POINT ( 'NONE',  ( 11.68687482311540116, -2.942322404451000128, 7.072673169413499217 ) ) ;
#61811=CARTESIAN_POINT ( 'NONE',  ( 9.702051052051999136, -2.879444846832000415, 7.280704316743199733 ) ) ;
#61814=CARTESIAN_POINT ( 'NONE',  ( 11.16579975933730040, -2.791514215189000225, 7.915786590091300035 ) ) ;
#61824=CARTESIAN_POINT ( 'NONE',  ( 11.27256919669530077, -3.037654633983899899, 7.215672285280100517 ) ) ;
#61859=CARTESIAN_POINT ( 'NONE',  ( 12.22433327354039889, -4.983220429128399687, 8.143111181492699302 ) ) ;
#61883=CARTESIAN_POINT ( 'NONE',  ( 9.893930206848999376, -5.250000000000000000, 7.500000000000000000 ) ) ;
#61901=CARTESIAN_POINT ( 'NONE',  ( 11.51872200990539952, -4.947480442174099657, 7.830502140005199507 ) ) ;
#61906=CYLINDRICAL_SURFACE ( 'NONE', #13720, 1.250000000000000222 ) ;
#61933=( NAMED_UNIT ( * ) PLANE_ANGLE_UNIT ( ) SI_UNIT ( $, .RADIAN. ) );
#61944=CARTESIAN_POINT ( 'NONE',  ( 11.39393020684959978, -5.250000000000000000, 7.500000000000000000 ) ) ;
#61964=CARTESIAN_POINT ( 'NONE',  ( 9.262289945692000259, -4.238022715896200054, 6.588711079851200303 ) ) ;
#61980=CARTESIAN_POINT ( 'NONE',  ( 10.93614141025500075, -3.450366949021700158, 6.521048559232099251 ) ) ;
#62004=CARTESIAN_POINT ( 'NONE',  ( 11.41301932002725650, -5.250000000000000888, 7.200148911387370454 ) ) ;
#62010=CARTESIAN_POINT ( 'NONE',  ( 10.70851354018233437, -3.836375382625528019, 8.749999999999996447 ) ) ;
#62040=CARTESIAN_POINT ( 'NONE',  ( 9.903734463322999559, -3.881063085044400118, 6.364399516445999438 ) ) ;
#62112=CARTESIAN_POINT ( 'NONE',  ( 12.20379573085659963, -2.893744357957000357, 7.308581953418300081 ) ) ;
#62152=CARTESIAN_POINT ( 'NONE',  ( 9.776025935146000378, -4.185743043590700374, 8.765655525501999890 ) ) ;
#62155=CARTESIAN_POINT ( 'NONE',  ( 10.84580110216399973, -5.090698144635000588, 8.166103548914600552 ) ) ;
#62164=CARTESIAN_POINT ( 'NONE',  ( 11.07149279008999976, -4.296686446741600385, 6.398515879103999993 ) ) ;
#62202=CARTESIAN_POINT ( 'NONE',  ( 11.26346886766499900, -4.634677072395899877, 8.653146038559000885 ) ) ;
#62243=CARTESIAN_POINT ( 'NONE',  ( 10.79262282008599882, -3.548418513060800361, 6.771613406921599854 ) ) ;
#62246=( GEOMETRIC_REPRESENTATION_CONTEXT ( 3 ) GLOBAL_UNCERTAINTY_ASSIGNED_CONTEXT ( ( #26892 ) ) GLOBAL_UNIT_ASSIGNED_CONTEXT ( ( #36045, #61933, #52466 ) ) REPRESENTATION_CONTEXT ( 'NONE', 'WORKASPACE' ) );
#62291=CARTESIAN_POINT ( 'NONE',  ( 11.94133594839949986, -3.430493414882899827, 8.152656755002400502 ) ) ;
#62307=AXIS2_PLACEMENT_3D ( 'NONE', #53892, #21057, #11244 ) ;
#62321=CARTESIAN_POINT ( 'NONE',  ( 10.89969598649000027, -3.111999510220800236, 6.971269690999399415 ) ) ;
#62327=CARTESIAN_POINT ( 'NONE',  ( 11.64975833414749928, -4.796537143354000499, 7.174999999999999822 ) ) ;
#62340=CARTESIAN_POINT ( 'NONE',  ( 9.807392757686999474, -3.414780058706799792, 6.860292594369099106 ) ) ;
#62381=CARTESIAN_POINT ( 'NONE',  ( 10.91690035061499842, -3.695660922043800145, 6.399494776650000105 ) ) ;
#62384=EDGE_LOOP ( 'NONE', ( #51856, #21113, #20814, #2635, #31019, #36989, #4366 ) ) ;
#62418=ORIENTED_EDGE ( 'NONE', *, *, #18176, .T. ) ;
#62453=CARTESIAN_POINT ( 'NONE',  ( 11.14533863405319991, -3.296214805808900028, 6.602238051205399749 ) ) ;
#62487=CARTESIAN_POINT ( 'NONE',  ( 9.600734463322998735, -3.881063085044400118, 6.364399516445999438 ) ) ;
#62498=CARTESIAN_POINT ( 'NONE',  ( 12.21922412107039868, -3.930460928605089777, 8.814426450544999625 ) ) ;
#62500=CARTESIAN_POINT ( 'NONE',  ( 10.89918582084299992, -4.746348444722899629, 8.362701637490498996 ) ) ;
#62504=ORIENTED_EDGE ( 'NONE', *, *, #39392, .T. ) ;
#62539=CARTESIAN_POINT ( 'NONE',  ( 11.43479632507519916, -3.442212747724900268, 6.465962698293999722 ) ) ;
#62553=CARTESIAN_POINT ( 'NONE',  ( 12.10000000000000142, -4.794859953698269450, 7.924485708373448567 ) ) ;
#62579=CARTESIAN_POINT ( 'NONE',  ( 10.85826357027499967, -3.149486845331399998, 7.335909308151700614 ) ) ;
#62621=CARTESIAN_POINT ( 'NONE',  ( 11.39979975933730039, -3.180925410802600162, 7.781807394638899922 ) ) ;
#62656=CARTESIAN_POINT ( 'NONE',  ( 11.35679632507500081, -3.509334349252600127, 6.590394082213600235 ) ) ;
#62675=CARTESIAN_POINT ( 'NONE',  ( 10.49127973160899963, -3.922199073804859992, 8.363513150096299142 ) ) ;
#62678=CARTESIAN_POINT ( 'NONE',  ( 11.39393020684959978, -5.250000000000000000, 7.500000000000000000 ) ) ;
#62713=CARTESIAN_POINT ( 'NONE',  ( 9.851063610504999346, -3.588011994494999968, 6.583971515917899531 ) ) ;
#62733=ORIENTED_EDGE ( 'NONE', *, *, #16717, .T. ) ;
#62744=CARTESIAN_POINT ( 'NONE',  ( 10.35434687351662575, -5.250000000000000000, 7.336375382625534236 ) ) ;
#62751=CARTESIAN_POINT ( 'NONE',  ( 11.86486084871759950, -5.207010770456999893, 7.174999999999999822 ) ) ;
#62764=CARTESIAN_POINT ( 'NONE',  ( 9.575651506909606425, -2.765563590215046830, 7.432209138388947700 ) ) ;
#62768=ORIENTED_EDGE ( 'NONE', *, *, #49221, .T. ) ;
#62780=ORIENTED_EDGE ( 'NONE', *, *, #16417, .T. ) ;
#62790=CARTESIAN_POINT ( 'NONE',  ( 12.15456516821461008, -3.197083038490000195, 6.689681884064299311 ) ) ;
#62827=CARTESIAN_POINT ( 'NONE',  ( 10.05464655415100061, -3.380689388027600106, 6.380697202105999999 ) ) ;
#62830=CARTESIAN_POINT ( 'NONE',  ( 10.74733997688000109, -3.727636250918499705, 8.748653021963999521 ) ) ;
#62839=CARTESIAN_POINT ( 'NONE',  ( 11.47635090131019986, -3.000792947412299849, 6.881982988766500497 ) ) ;
#62841=CARTESIAN_POINT ( 'NONE',  ( 11.51456785386839954, -4.946394603182100447, 6.863111178199799767 ) ) ;
#62864=CARTESIAN_POINT ( 'NONE',  ( 12.08457173739308388, -3.062774903199518839, 6.638117766810081477 ) ) ;
#62876=CARTESIAN_POINT ( 'NONE',  ( 11.01414141025500015, -3.384226587288500010, 6.403245959303999868 ) ) ;
#62892=CARTESIAN_POINT ( 'NONE',  ( 12.09999999999999964, -2.820501972398000046, 7.825000000000000178 ) ) ;
#62916=CARTESIAN_POINT ( 'NONE',  ( 11.35056919669530018, -3.169300617545700138, 7.254567470917099747 ) ) ;
#62957=DIRECTION ( 'NONE',  ( -0.5000000000000150990, -0.08222066253632250021, 0.8621135439442261239 ) ) ;
#62958=CARTESIAN_POINT ( 'NONE',  ( 10.88287885159599888, -3.139900861731399928, 7.602606670248799325 ) ) ;
#62970=CARTESIAN_POINT ( 'NONE',  ( 9.220712484379999907, -4.219532685969900498, 6.659501631675699862 ) ) ;
#62987=CARTESIAN_POINT ( 'NONE',  ( 11.52301463001509951, -3.452642973349600464, 8.376661845795100092 ) ) ;
#63003=CARTESIAN_POINT ( 'NONE',  ( 11.54749144726329924, -4.500836215462999945, 8.206726025856399431 ) ) ;
#63036=AXIS2_PLACEMENT_3D ( 'NONE', #35107, #35783, #68264 ) ;
#63039=ORIENTED_EDGE ( 'NONE', *, *, #29688, .T. ) ;
#63048=CARTESIAN_POINT ( 'NONE',  ( 10.76291290906799958, -4.635529777446699917, 6.722218404915299317 ) ) ;
#63062=CARTESIAN_POINT ( 'NONE',  ( 11.12309687351639020, -2.782534154164605145, 7.172815144550900968 ) ) ;
#63072=EDGE_CURVE ( 'NONE', #24435, #49203, #67470, .T. ) ;
#63075=DIRECTION ( 'NONE',  ( -1.000000000000000000, 0.000000000000000000, 0.000000000000000000 ) ) ;
#63100=CARTESIAN_POINT ( 'NONE',  ( 9.356495485442707150, -3.650546589001255171, 6.546761994161411913 ) ) ;
#63130=CARTESIAN_POINT ( 'NONE',  ( 10.91964694612699915, -5.186980343482999523, 7.026297514493899499 ) ) ;
#63165=CARTESIAN_POINT ( 'NONE',  ( 10.51057120343299900, -4.062009413492949861, 6.222291352336999815 ) ) ;
#63178=CARTESIAN_POINT ( 'NONE',  ( 11.72567835872029995, -4.993948309075300074, 8.126439557340900066 ) ) ;
#63180=CARTESIAN_POINT ( 'NONE',  ( 11.92887348028849992, -5.124210964533999935, 6.892162778124999889 ) ) ;
#63196=DIRECTION ( 'NONE',  ( -1.000000000000000000, 0.000000000000000000, 0.000000000000000000 ) ) ;
#63216=CARTESIAN_POINT ( 'NONE',  ( 11.09725056272499977, -2.683866746800999792, 7.480494252843770120 ) ) ;
#63260=CARTESIAN_POINT ( 'NONE',  ( 11.66641369783139837, -4.050626550392200542, 6.497808498716000081 ) ) ;
#63267=CARTESIAN_POINT ( 'NONE',  ( 12.30233327354039830, -5.101536739857000846, 8.220500279733599314 ) ) ;
#63274=CARTESIAN_POINT ( 'NONE',  ( 9.599999931441001166, -4.000000000000000000, 7.500000000000000000 ) ) ;
#63283=AXIS2_PLACEMENT_3D ( 'NONE', #67984, #36523, #45653 ) ;
#63305=CARTESIAN_POINT ( 'NONE',  ( 11.69518313518939934, -4.537300658085600347, 6.820583637845799352 ) ) ;
#63335=CARTESIAN_POINT ( 'NONE',  ( 11.77745123989519982, -3.589787500396900199, 6.707778874960499849 ) ) ;
#63352=CARTESIAN_POINT ( 'NONE',  ( 12.01102763632551884, -4.911148285670300595, 7.920427941950599404 ) ) ;
#63370=ORIENTED_EDGE ( 'NONE', *, *, #216, .T. ) ;
#63402=CARTESIAN_POINT ( 'NONE',  ( 10.58560887879199974, -4.227457260387500249, 8.478317686146800369 ) ) ;
#63417=CARTESIAN_POINT ( 'NONE',  ( 11.00145247700548268, -4.082536117276985621, 8.370216864706282678 ) ) ;
#63429=CARTESIAN_POINT ( 'NONE',  ( 11.82299956498189886, -5.207010770456999893, 7.825000000000000178 ) ) ;
#63481=CARTESIAN_POINT ( 'NONE',  ( 11.65810538575740019, -2.757018958839999812, 7.797177576385699638 ) ) ;
#63521=CARTESIAN_POINT ( 'NONE',  ( 9.016151519676999015, -3.972335373863620234, 6.221087886525999089 ) ) ;
#63535=CARTESIAN_POINT ( 'NONE',  ( 11.38813259637009878, -5.155817667926999803, 6.870201387206400057 ) ) ;
#63537=CARTESIAN_POINT ( 'NONE',  ( 11.71149010443640037, -2.862435565199000109, 7.414927836855409460 ) ) ;
#63555=EDGE_LOOP ( 'NONE', ( #25986, #2219, #4704, #51844 ) ) ;
#63572=CARTESIAN_POINT ( 'NONE',  ( 11.27879632507499963, -3.576455950783300253, 6.714825466131699727 ) ) ;
#63612=CARTESIAN_POINT ( 'NONE',  ( 11.29718447801629999, -2.996774412198000448, 7.522119512433738997 ) ) ;
#63619=CARTESIAN_POINT ( 'NONE',  ( 11.18546886766499959, -4.566506264294200257, 8.529286361367999447 ) ) ;
#63647=CARTESIAN_POINT ( 'NONE',  ( 9.210288521113000115, -4.352953559891299840, 6.715449042252499723 ) ) ;
#63654=CARTESIAN_POINT ( 'NONE',  ( 12.03979707368350027, -4.430269712815499972, 8.251775607861899786 ) ) ;
#63696=LINE ( 'NONE', #15811, #27019 ) ;
#63701=CARTESIAN_POINT ( 'NONE',  ( 12.15871932425157098, -4.147141405561299621, 6.507377093516500288 ) ) ;
#63706=ORIENTED_EDGE ( 'NONE', *, *, #61566, .T. ) ;
#63724=AXIS2_PLACEMENT_3D ( 'NONE', #53277, #48726, #11307 ) ;
#63738=EDGE_LOOP ( 'NONE', ( #14230, #2338, #63370 ) ) ;
#63740=CARTESIAN_POINT ( 'NONE',  ( 9.349999778958000718, -4.000000000000000000, 7.500000000000000000 ) ) ;
#63746=CARTESIAN_POINT ( 'NONE',  ( 9.498468108405999644, -2.901397043998999781, 7.188863445572599709 ) ) ;
#63777=CARTESIAN_POINT ( 'NONE',  ( 10.57309687351575000, -2.782534154164605589, 7.172815144550900968 ) ) ;
#63825=CARTESIAN_POINT ( 'NONE',  ( 11.55964426047339977, -3.312306505177499805, 6.422784126663999338 ) ) ;
#63859=CARTESIAN_POINT ( 'NONE',  ( 9.598721904869998767, -2.884547197234000215, 6.873781641694999500 ) ) ;
#63873=CARTESIAN_POINT ( 'NONE',  ( 11.06733863405299800, -3.211524470605299886, 6.494205428462000107 ) ) ;
#63905=EDGE_CURVE ( 'NONE', #30682, #11605, #9836, .T. ) ;
#63912=CARTESIAN_POINT ( 'NONE',  ( 11.98011496860029901, -3.080230834057799960, 7.971338736265699332 ) ) ;
#63951=CARTESIAN_POINT ( 'NONE',  ( 11.37103032197929942, -3.416314376401300201, 8.316248703309600643 ) ) ;
#63958=CARTESIAN_POINT ( 'NONE',  ( 11.01925056272500036, -2.825232917634000085, 7.482589369563879877 ) ) ;
#63992=CARTESIAN_POINT ( 'NONE',  ( 11.81410538575740077, -3.024036709177600368, 7.733337754805098996 ) ) ;
#64024=CARTESIAN_POINT ( 'NONE',  ( 9.772783876522375124, -4.789858247946766845, 8.481892410946455740 ) ) ;
#64030=CARTESIAN_POINT ( 'NONE',  ( 11.14393020684970104, -2.750000000000000000, 7.500000000000000000 ) ) ;
#64035=CARTESIAN_POINT ( 'NONE',  ( 11.64595257254739913, -4.831736303435800295, 7.258104750172799768 ) ) ;
#64063=CARTESIAN_POINT ( 'NONE',  ( 11.66544712921906779, -4.732401051283384952, 7.017906594554381705 ) ) ;
#64085=CARTESIAN_POINT ( 'NONE',  ( 9.775076168957999911, -4.509700402263200125, 6.634524523592600254 ) ) ;
#64168=CARTESIAN_POINT ( 'NONE',  ( 10.63662282008600002, -3.405288783432600219, 6.540749699823199315 ) ) ;
#64175=CARTESIAN_POINT ( 'NONE',  ( 12.09999999999999787, -4.689830048140305685, 6.761031184901315605 ) ) ;
#64191=ORIENTED_EDGE ( 'NONE', *, *, #12414, .T. ) ;
#64215=CARTESIAN_POINT ( 'NONE',  ( 11.04272335273199879, -3.555125495332600138, 6.301916924546999255 ) ) ;
#64250=B_SPLINE_CURVE_WITH_KNOTS ( 'NONE', 3,
 ( #67583, #67240, #40680, #56422, #3278, #50835, #61663, #2930, #62010, #8527, #35447, #24258, #56073, #13442, #14467, #46279, #45598, #14122 ),
 .UNSPECIFIED., .F., .F.,
 ( 4, 2, 2, 2, 2, 2, 2, 2, 4 ),
 ( 0.000000000000000000, 0.1250000000000003331, 0.2500000000000006661, 0.3750000000000009992, 0.5000000000000013323, 0.6250000000000009992, 0.7500000000000006661, 0.8750000000000003331, 1.000000000000000000 ),
 .UNSPECIFIED. ) ;
#64253=CARTESIAN_POINT ( 'NONE',  ( 11.94366954483529852, -3.514796851401900124, 8.248643701125299543 ) ) ;
#64289=CARTESIAN_POINT ( 'NONE',  ( 10.85410941423799791, -3.257202320419700037, 8.174686939644999484 ) ) ;
#64292=EDGE_CURVE ( 'NONE', #51764, #21230, #40540, .T. ) ;
#64297=CARTESIAN_POINT ( 'NONE',  ( 11.85034208742530026, -4.630634088820300143, 6.508707709313799050 ) ) ;
#64329=CARTESIAN_POINT ( 'NONE',  ( 10.79262282008599882, -3.548418513060800361, 6.771613406921599854 ) ) ;
#64353=CARTESIAN_POINT ( 'NONE',  ( 10.85987047770900382, -5.250000000000000000, 7.249610810850630749 ) ) ;
#64371=EDGE_CURVE ( 'NONE', #2412, #19919, #28935, .T. ) ;
#64376=CARTESIAN_POINT ( 'NONE',  ( 11.57210672858429845, -4.692204557952299737, 8.020722037455799480 ) ) ;
#64417=DIRECTION ( 'NONE',  ( 1.000000000000000000, 0.000000000000000000, 0.000000000000000000 ) ) ;
#64425=CARTESIAN_POINT ( 'NONE',  ( 10.78622949779699880, -3.519000825516800379, 6.778648208007999720 ) ) ;
#64427=CARTESIAN_POINT ( 'NONE',  ( 11.14393020684970104, -2.750000000000000000, 7.500000000000000000 ) ) ;
#64440=CARTESIAN_POINT ( 'NONE',  ( 11.44452754078377588, -3.491551460122512385, 8.211034235888378774 ) ) ;
#64510=CARTESIAN_POINT ( 'NONE',  ( 10.10838019923399855, -2.730774061183999901, 7.659530259549099718 ) ) ;
#64513=DIRECTION ( 'NONE',  ( 0.000000000000000000, -1.000000000000000000, 0.000000000000000000 ) ) ;
#64545=CARTESIAN_POINT ( 'NONE',  ( 9.168126402770999661, -2.803062940908000122, 7.951360234587600218 ) ) ;
#64559=CARTESIAN_POINT ( 'NONE',  ( 11.16579975933730040, -2.791514215189000225, 7.915786590091300035 ) ) ;
#64596=CARTESIAN_POINT ( 'NONE',  ( 11.56967835872019990, -4.754733798270200928, 7.975673736933100777 ) ) ;
#64614=VERTEX_POINT ( 'NONE', #47328 ) ;
#64639=CARTESIAN_POINT ( 'NONE',  ( 12.00687348028854906, -5.003459210197000573, 6.957450711802899868 ) ) ;
#64646=CARTESIAN_POINT ( 'NONE',  ( 12.09456039236534330, -2.685288321999000249, 7.436015812896529020 ) ) ;
#64675=CARTESIAN_POINT ( 'NONE',  ( 10.58809113605762597, -4.810085401003767913, 7.830596297620237678 ) ) ;
#64691=CARTESIAN_POINT ( 'NONE',  ( 11.71022026213526779, -2.954246606487285209, 7.175001674908393134 ) ) ;
#64710=CARTESIAN_POINT ( 'NONE',  ( 10.90480513896000048, -3.220259576336399920, 7.933462475324499330 ) ) ;
#64723=CARTESIAN_POINT ( 'NONE',  ( 11.71564426047340035, -3.460037133261700149, 6.654192128557399499 ) ) ;
#64768=ADVANCED_FACE ( 'NONE', ( #30481 ), #5314, .F. ) ;
#64774=CARTESIAN_POINT ( 'NONE',  ( 9.975696787962998968, -3.851113559088000127, 8.354131589521699652 ) ) ;
#64776=CARTESIAN_POINT ( 'NONE',  ( 11.15434687351636356, -2.749999999999998668, 7.663624617374463988 ) ) ;
#64782=CYLINDRICAL_SURFACE ( 'NONE', #63724, 1.250000000000000222 ) ;
#64852=CARTESIAN_POINT ( 'NONE',  ( 10.57503300763299947, -3.118110956362800223, 6.575021251017499679 ) ) ;
#64861=CARTESIAN_POINT ( 'NONE',  ( 12.10000000000000142, -4.471166781226292741, 6.561154158729442187 ) ) ;
#64870=CARTESIAN_POINT ( 'NONE',  ( 10.81021345716900051, -3.363461959113699606, 6.921280946186199934 ) ) ;
#64871=EDGE_CURVE ( 'NONE', #40612, #48587, #4748, .T. ) ;
#64884=ORIENTED_EDGE ( 'NONE', *, *, #13366, .T. ) ;
#64889=CARTESIAN_POINT ( 'NONE',  ( 9.396088727410999653, -5.274736981944999847, 7.393088754863899936 ) ) ;
#64903=CARTESIAN_POINT ( 'NONE',  ( 11.53502897915239878, -3.672866099873000056, 6.264564938179000286 ) ) ;
#64923=CARTESIAN_POINT ( 'NONE',  ( 11.50000000000000000, -3.008232475376599879, 7.825000000000000178 ) ) ;
#64937=CARTESIAN_POINT ( 'NONE',  ( 11.73078751119019891, -4.915752892793999962, 7.020904658857499925 ) ) ;
#64976=CARTESIAN_POINT ( 'NONE',  ( 11.39564560330030041, -3.692495237344800341, 8.455191956516999952 ) ) ;
#64983=CARTESIAN_POINT ( 'NONE',  ( 11.35168717260510007, -4.613789146762799831, 6.498190316041999814 ) ) ;
#65086=ORIENTED_EDGE ( 'NONE', *, *, #28179, .F. ) ;
#65097=ORIENTED_EDGE ( 'NONE', *, *, #66212, .F. ) ;
#65118=CARTESIAN_POINT ( 'NONE',  ( 9.293822372493998785, -4.288705740401799638, 6.555546982591299532 ) ) ;
#65136=CARTESIAN_POINT ( 'NONE',  ( 10.39393020684899938, -5.250000000000000000, 7.500000000000000000 ) ) ;
#65167=CARTESIAN_POINT ( 'NONE',  ( 10.38351354018233508, -5.249999999999998224, 7.663624617374469317 ) ) ;
#65192=CARTESIAN_POINT ( 'NONE',  ( 11.27101354018290102, -4.768183399968641822, 8.499583552997725278 ) ) ;
#65208=CARTESIAN_POINT ( 'NONE',  ( 10.48831740696900106, -3.762080884004200154, 6.243107450209000042 ) ) ;
#65264=CARTESIAN_POINT ( 'NONE',  ( 9.896013540183334456, -4.999583552997726166, 6.731816600031358178 ) ) ;
#65281=CARTESIAN_POINT ( 'NONE',  ( 9.289886373836322875, -3.999992178805580334, 6.560153657526066162 ) ) ;
#65300=DIRECTION ( 'NONE',  ( -0.4999999999999719669, 0.6407827956774649891, -0.5825782426110679424 ) ) ;
#65306=DIRECTION ( 'NONE',  ( -1.000000000000000000, 0.000000000000000000, 0.000000000000000000 ) ) ;
#65328=CARTESIAN_POINT ( 'NONE',  ( 10.48725461470299969, -5.106563667948999630, 7.218483930889299849 ) ) ;
#65331=CARTESIAN_POINT ( 'NONE',  ( 10.77610941423800028, -3.155589807313900153, 8.266982106121901097 ) ) ;
#65339=CARTESIAN_POINT ( 'NONE',  ( 11.39835090130999973, -3.121033016283800254, 6.956352367771000189 ) ) ;
#65369=CARTESIAN_POINT ( 'NONE',  ( 9.726900131858625898, -4.185762427694958987, 6.645000240129933289 ) ) ;
#65443=B_SPLINE_CURVE_WITH_KNOTS ( 'NONE', 3,
 ( #34579, #23034, #17804, #58285, #42221, #19856, #41185, #26134, #30357, #52001, #51665, #3760, #46085, #3424, #20885, #30692, #35935, #40834 ),
 .UNSPECIFIED., .F., .F.,
 ( 4, 2, 2, 2, 2, 2, 2, 2, 4 ),
 ( 0.000000000000000000, 0.1250000000000000000, 0.2500000000000000000, 0.3750000000000000000, 0.5000000000000000000, 0.6250000000000000000, 0.7500000000000000000, 0.8750000000000000000, 1.000000000000000000 ),
 .UNSPECIFIED. ) ;
#65470=CARTESIAN_POINT ( 'NONE',  ( 9.773063610504999943, -3.644370728184199937, 6.709281487801199262 ) ) ;
#65472=CARTESIAN_POINT ( 'NONE',  ( 11.28976354018297634, -4.327184855449096368, 8.717465845835395299 ) ) ;
#65484=VERTEX_POINT ( 'NONE', #69156 ) ;
#65491=CARTESIAN_POINT ( 'NONE',  ( 11.79364426047339975, -3.533902447304699823, 6.769896129503799820 ) ) ;
#65537=ORIENTED_EDGE ( 'NONE', *, *, #49559, .T. ) ;
#65543=CARTESIAN_POINT ( 'NONE',  ( 11.26059687351620298, -4.629523725463621453, 8.592232985442825210 ) ) ;
#65558=CARTESIAN_POINT ( 'NONE',  ( 10.36167167105699960, -5.261543809652999393, 7.288123611975898974 ) ) ;
#65569=CARTESIAN_POINT ( 'NONE',  ( 11.64955063476181429, -3.023401864784705850, 8.326430086672806041 ) ) ;
#65601=DIRECTION ( 'NONE',  ( -1.000000000000000000, 0.000000000000000000, -2.609704304917999919E-14 ) ) ;
#65634=CARTESIAN_POINT ( 'NONE',  ( 11.61718313518939993, -4.622449961306399402, 6.712912394634500401 ) ) ;
#65670=EDGE_CURVE ( 'NONE', #61281, #41424, #53690, .T. ) ;
#65676=CARTESIAN_POINT ( 'NONE',  ( 10.10731740696899905, -3.787635830142400462, 6.378110563671000044 ) ) ;
#65679=CARTESIAN_POINT ( 'NONE',  ( 11.73195122972050086, -3.492749840905900349, 8.673036084990000560 ) ) ;
#65689=CARTESIAN_POINT ( 'NONE',  ( 10.85814141025499957, -3.516507310755200066, 6.638851159159999682 ) ) ;
#65739=CARTESIAN_POINT ( 'NONE',  ( 9.351468108405999402, -3.165798890946399879, 7.263744984161399465 ) ) ;
#65761=CARTESIAN_POINT ( 'NONE',  ( 9.810585478579779917, -4.629544268302966614, 8.592274333092912997 ) ) ;
#65819=CARTESIAN_POINT ( 'NONE',  ( 10.50760887879199856, -4.196341783741199372, 8.344486736701099971 ) ) ;
#65828=DIRECTION ( 'NONE',  ( -1.000000000000000000, 0.000000000000000000, 0.000000000000000000 ) ) ;
#65835=B_SPLINE_CURVE_WITH_KNOTS ( 'NONE', 3,
 ( #21387, #42720, #7732, #7039, #12290, #54589, #55286, #1451, #17172, #48995, #66108, #65761, #27681, #1107, #33272, #50040, #22419, #18225 ),
 .UNSPECIFIED., .F., .F.,
 ( 4, 2, 2, 2, 2, 2, 2, 2, 4 ),
 ( 0.1494581667962518179, 0.2557758959467203441, 0.3620936250971888981, 0.4684113542476573411, 0.5747290833981258951, 0.6810468125485944491, 0.7873645416990628920, 0.8936822708495314460, 1.000000000000000000 ),
 .UNSPECIFIED. ) ;
#65840=CARTESIAN_POINT ( 'NONE',  ( 11.71979841651039855, -4.304975143798100312, 6.689266534545799558 ) ) ;
#65852=CYLINDRICAL_SURFACE ( 'NONE', #48550, 1.250000000000000222 ) ;
#65857=ORIENTED_EDGE ( 'NONE', *, *, #1401, .F. ) ;
#65864=CARTESIAN_POINT ( 'NONE',  ( 10.32101354018233152, -4.768183399968640934, 8.499583552997727054 ) ) ;
#65900=DIRECTION ( 'NONE',  ( 0.000000000000000000, 1.000000000000000000, 0.000000000000000000 ) ) ;
#65902=CARTESIAN_POINT ( 'NONE',  ( 9.627126402771001068, -2.803062940908000122, 7.951360234587600218 ) ) ;
#65951=CYLINDRICAL_SURFACE ( 'NONE', #14718, 1.250000000000000222 ) ;
#65952=ORIENTED_EDGE ( 'NONE', *, *, #21140, .T. ) ;
#65976=CARTESIAN_POINT ( 'NONE',  ( 10.87872469555899890, -3.497841151814999883, 8.368784980615899372 ) ) ;
#66016=CARTESIAN_POINT ( 'NONE',  ( 9.526759580228999269, -4.976892840331100132, 7.733500918284399894 ) ) ;
#66020=CARTESIAN_POINT ( 'NONE',  ( 11.63349010443640097, -2.725546193138000284, 7.404690636538299842 ) ) ;
#66029=CARTESIAN_POINT ( 'NONE',  ( 12.03148876160955005, -4.790673964186999534, 6.677731919207799294 ) ) ;
#66030=CARTESIAN_POINT ( 'NONE',  ( 11.48146005378009882, -3.088328798999600000, 7.986817550794899745 ) ) ;
#66063=CARTESIAN_POINT ( 'NONE',  ( 10.81021345716900051, -3.363461959113699606, 6.921280946186199934 ) ) ;
#66081=CARTESIAN_POINT ( 'NONE',  ( 10.74255864497999902, -3.209241371122599773, 6.880692865553299953 ) ) ;
#66108=CARTESIAN_POINT ( 'NONE',  ( 9.789752973821551407, -4.327172861449236407, 8.717426404466646517 ) ) ;
#66136=ORIENTED_EDGE ( 'NONE', *, *, #7760, .T. ) ;
#66168=CARTESIAN_POINT ( 'NONE',  ( 9.393126402770999306, -3.188752782784400441, 7.805918119494599239 ) ) ;
#66205=CARTESIAN_POINT ( 'NONE',  ( 11.58482133862618468, -3.057020944820409092, 6.626386139742057146 ) ) ;
#66212=EDGE_CURVE ( 'NONE', #11605, #11483, #24763, .T. ) ;
#66222=CARTESIAN_POINT ( 'NONE',  ( 11.66486084871730000, -2.792989229543000107, 7.825000000000000178 ) ) ;
#66249=CARTESIAN_POINT ( 'NONE',  ( 10.61295058442699890, -3.546800160410199965, 8.548019252390998801 ) ) ;
#66323=CARTESIAN_POINT ( 'NONE',  ( 12.13410404293056999, -4.442327784369100030, 6.599279737936000423 ) ) ;
#66352=B_SPLINE_CURVE_WITH_KNOTS ( 'NONE', 3,
 ( #1510, #11997, #1859, #12693, #59888, #33680, #33334, #65472, #38924, #1166, #22481, #34030, #55343, #60245, #43823, #54998, #64776, #64427 ),
 .UNSPECIFIED., .F., .F.,
 ( 4, 2, 2, 2, 2, 2, 2, 2, 4 ),
 ( 0.000000000000000000, 0.1250000000000000000, 0.2500000000000000000, 0.3750000000000000000, 0.5000000000000000000, 0.6250000000000000000, 0.7500000000000000000, 0.8750000000000000000, 1.000000000000000000 ),
 .UNSPECIFIED. ) ;
#66363=CARTESIAN_POINT ( 'NONE',  ( 10.66455864497999961, -3.101067942814400347, 6.795973491698399371 ) ) ;
#66366=CARTESIAN_POINT ( 'NONE',  ( 11.36687616594229944, -4.344946439135400240, 8.587337146608000182 ) ) ;
#66375=CARTESIAN_POINT ( 'NONE',  ( 11.95764291764649911, -5.132124077409000229, 7.639947095788999221 ) ) ;
#66376=CARTESIAN_POINT ( 'NONE',  ( 11.64767835872009982, -4.874341053673500568, 8.051056647135798272 ) ) ;
#66409=CARTESIAN_POINT ( 'NONE',  ( 9.473608660036624940, -3.779042157900793786, 8.346587208109317757 ) ) ;
#66415=CARTESIAN_POINT ( 'NONE',  ( 12.34388784977539899, -5.255745690988000263, 7.571757098260779806 ) ) ;
#66428=CARTESIAN_POINT ( 'NONE',  ( 10.05867167105700055, -4.990538396979200542, 7.333638993632098924 ) ) ;
#66522=EDGE_CURVE ( 'NONE', #24287, #67539, #66352, .T. ) ;
#66563=ORIENTED_EDGE ( 'NONE', *, *, #39622, .T. ) ;
#66585=EDGE_LOOP ( 'NONE', ( #56775, #4357, #24598, #44186 ) ) ;
#66593=CARTESIAN_POINT ( 'NONE',  ( 10.05570934641700021, -2.968569381205999669, 7.989780896525600085 ) ) ;
#66616=CARTESIAN_POINT ( 'NONE',  ( 12.00962052873067876, -4.169679534937900556, 8.360247930805771333 ) ) ;
#66647=CARTESIAN_POINT ( 'NONE',  ( 11.58810207955139937, -4.796537143354000499, 7.825000000000000178 ) ) ;
#66669=CARTESIAN_POINT ( 'NONE',  ( 11.90841235500450068, -4.841138636481000290, 8.270568563129298667 ) ) ;
#66672=CARTESIAN_POINT ( 'NONE',  ( 10.82169598649000086, -3.233475335853099875, 7.043598424555200133 ) ) ;
#66710=CARTESIAN_POINT ( 'NONE',  ( 10.36060887879200010, -4.258572737033900601, 8.612148635591999835 ) ) ;
#66714=CARTESIAN_POINT ( 'NONE',  ( 11.75656651104150008, -3.873914634362100262, 8.771777834828998976 ) ) ;
#66724=CARTESIAN_POINT ( 'NONE',  ( 11.22333863405319931, -3.380905141010200232, 6.710270673950399889 ) ) ;
#66725=CARTESIAN_POINT ( 'NONE',  ( 11.07102344389999971, -4.762665848028800220, 7.962849245488699879 ) ) ;
#66764=PRODUCT_DEFINITION_SHAPE ( 'NONE', 'NONE',  #59017 ) ;
#66770=ORIENTED_EDGE ( 'NONE', *, *, #16717, .F. ) ;
#66778=CARTESIAN_POINT ( 'NONE',  ( 9.554101285864000204, -4.558267473659599389, 8.163359157892799089 ) ) ;
#66857=FACE_OUTER_BOUND ( 'NONE', #3311, .T. ) ;
#66892=CARTESIAN_POINT ( 'NONE',  ( 10.76990035061499995, -3.768906505327899836, 6.664354444139199529 ) ) ;
#66935=CARTESIAN_POINT ( 'NONE',  ( 10.81558376188599802, -4.962881317320600338, 6.886327436977599525 ) ) ;
#66951=SURFACE_SIDE_STYLE ('',( #18730 ) ) ;
#67001=ORIENTED_EDGE ( 'NONE', *, *, #64371, .F. ) ;
#67011=CARTESIAN_POINT ( 'NONE',  ( 12.05610404293055993, -4.502836909561000134, 6.476063885290000322 ) ) ;
#67051=CARTESIAN_POINT ( 'NONE',  ( 9.801355082327999568, -4.572497688003699601, 8.643954013369999245 ) ) ;
#67063=CARTESIAN_POINT ( 'NONE',  ( 12.17918044953561996, -2.988516238873000219, 6.972563939641199582 ) ) ;
#67095=CARTESIAN_POINT ( 'NONE',  ( 9.448279512853625661, -3.525202972512352595, 8.234914996158446243 ) ) ;
#67101=CARTESIAN_POINT ( 'NONE',  ( 11.51790547754520055, -2.825704134258000266, 7.462730980357120458 ) ) ;
#67135=CARTESIAN_POINT ( 'NONE',  ( 10.95672469555900008, -3.566534988568399900, 8.249937779480299938 ) ) ;
#67167=SURFACE_STYLE_USAGE ( .BOTH. , #46550 ) ;
#67210=CARTESIAN_POINT ( 'NONE',  ( 12.10988784977536525, -4.851105903694400645, 7.548634759728509280 ) ) ;
#67231=CARTESIAN_POINT ( 'NONE',  ( 10.64325461470300027, -4.840245908677600184, 7.286236678332599581 ) ) ;
#67232=CARTESIAN_POINT ( 'NONE',  ( 11.14393020684970104, -2.750000000000000000, 7.500000000000000000 ) ) ;
#67240=CARTESIAN_POINT ( 'NONE',  ( 10.60434687351566474, -2.749999999999998224, 7.663624617374462211 ) ) ;
#67242=ADVANCED_FACE ( 'NONE', ( #36298 ), #42581, .T. ) ;
#67273=CARTESIAN_POINT ( 'NONE',  ( 10.15702593514599883, -4.165792341207500193, 8.629711178834000407 ) ) ;
#67338=CARTESIAN_POINT ( 'NONE',  ( 11.83810207955129989, -3.203462856645999945, 7.174999999999999822 ) ) ;
#67348=CARTESIAN_POINT ( 'NONE',  ( 11.76072066707849828, -3.023932655881500065, 8.090408888831799317 ) ) ;
#67387=CARTESIAN_POINT ( 'NONE',  ( 9.826684229510000534, -4.901739481456999670, 8.407331414124799451 ) ) ;
#67390=CARTESIAN_POINT ( 'NONE',  ( 10.89503166480599994, -5.274847857784000560, 7.410114961806599787 ) ) ;
#67398=CARTESIAN_POINT ( 'NONE',  ( 11.34657802013509986, -5.315911219205999849, 7.530633716161349689 ) ) ;
#67400=CARTESIAN_POINT ( 'NONE',  ( 11.58841369783139896, -4.057552111898620417, 6.360711682373000109 ) ) ;
#67431=CARTESIAN_POINT ( 'NONE',  ( 11.91486084871699802, -5.207010770456999893, 7.174999999999999822 ) ) ;
#67436=CARTESIAN_POINT ( 'NONE',  ( 12.18788784977535933, -4.985985832792199979, 7.556342205905759890 ) ) ;
#67452=CARTESIAN_POINT ( 'NONE',  ( 12.09999999999999964, -4.755880058522735432, 8.017883087166149281 ) ) ;
#67469=ADVANCED_FACE ( 'NONE', ( #30186 ), #3588, .F. ) ;
#67470=B_SPLINE_CURVE_WITH_KNOTS ( 'NONE', 3,
 ( #6543, #54789, #38362, #59687 ),
 .UNSPECIFIED., .F., .F.,
 ( 4, 4 ),
 ( 0.000000000000000000, 1.000000000000000000 ),
 .UNSPECIFIED. ) ;
#67479=CARTESIAN_POINT ( 'NONE',  ( 12.01102763632551884, -4.911148285670300595, 7.920427941950599404 ) ) ;
#67486=CARTESIAN_POINT ( 'NONE',  ( 12.13611496860034933, -2.828587461987000395, 8.100294210499798808 ) ) ;
#67524=CARTESIAN_POINT ( 'NONE',  ( 10.98133997688000107, -3.815400206859000054, 8.346298710230199092 ) ) ;
#67539=VERTEX_POINT ( 'NONE', #64030 ) ;
#67553=CARTESIAN_POINT ( 'NONE',  ( 11.14391429142989942, -3.977620450637519678, 8.674673860548999471 ) ) ;
#67573=CARTESIAN_POINT ( 'NONE',  ( 10.18732996542200020, -4.602191201513400109, 6.876242273533999416 ) ) ;
#67583=CARTESIAN_POINT ( 'NONE',  ( 10.59393020684899867, -2.750000000000000000, 7.500000000000000000 ) ) ;
#67612=CARTESIAN_POINT ( 'NONE',  ( 9.551138961223999857, -2.940105638081000006, 6.783753885003399375 ) ) ;
#67679=CARTESIAN_POINT ( 'NONE',  ( 12.09999999999999964, -4.817420948848700313, 7.825000000000000178 ) ) ;
#67690=CARTESIAN_POINT ( 'NONE',  ( 12.00687348028854906, -5.003459210197000573, 6.957450711802899868 ) ) ;
#67727=CARTESIAN_POINT ( 'NONE',  ( 9.296784697134999220, -3.380386586585000241, 8.459069166353199165 ) ) ;
#67730=CARTESIAN_POINT ( 'NONE',  ( 11.41195257254739914, -5.227167235646000165, 7.143100915737699452 ) ) ;
#67738=CARTESIAN_POINT ( 'NONE',  ( 12.25203632436370071, -5.109717061557999429, 7.759151359668400083 ) ) ;
#67740=CARTESIAN_POINT ( 'NONE',  ( 10.87457053952200070, -4.448306506338299826, 8.548957288282998945 ) ) ;
#67754=B_SPLINE_CURVE_WITH_KNOTS ( 'NONE', 3,
 ( #40561, #50718, #2812, #45473 ),
 .UNSPECIFIED., .F., .F.,
 ( 4, 4 ),
 ( 0.000000000000000000, 1.000000000000000000 ),
 .UNSPECIFIED. ) ;
#67777=CARTESIAN_POINT ( 'NONE',  ( 12.09999999999999964, -2.820501972398000046, 7.825000000000000178 ) ) ;
#67780=CARTESIAN_POINT ( 'NONE',  ( 11.05569598648999907, -2.869047858956000230, 6.826612223887499553 ) ) ;
#67820=CARTESIAN_POINT ( 'NONE',  ( 11.12903166480609940, -4.864052766304100217, 7.439078678739090122 ) ) ;
#67869=CARTESIAN_POINT ( 'NONE',  ( 11.96595122972050085, -3.656201404350900130, 8.295047870239098842 ) ) ;
#67884=CARTESIAN_POINT ( 'NONE',  ( 9.283078676347997771, -4.247267730859300094, 6.553315803938899897 ) ) ;
#67902=CARTESIAN_POINT ( 'NONE',  ( 11.68923293495519999, -5.032672437899000428, 7.541513160549049744 ) ) ;
#67916=CARTESIAN_POINT ( 'NONE',  ( 12.06441235500451015, -4.638700978900200056, 8.085115074060599483 ) ) ;
#67921=CARTESIAN_POINT ( 'NONE',  ( 9.934038493598999153, -3.372531419565699906, 8.098323595618600379 ) ) ;
#67955=VERTEX_POINT ( 'NONE', #16670 ) ;
#67963=CARTESIAN_POINT ( 'NONE',  ( 9.977709346417000802, -3.092687088662700035, 7.930842873041400232 ) ) ;
#67974=CARTESIAN_POINT ( 'NONE',  ( 10.64393020684899938, -2.750000000000000000, 7.500000000000000000 ) ) ;
#67984=CARTESIAN_POINT ( 'NONE',  ( 11.50000000000000000, -4.000000000000000000, 7.500000000000000000 ) ) ;
#68038=CARTESIAN_POINT ( 'NONE',  ( 11.04687750876899877, -4.617914354660699772, 6.541108991297599928 ) ) ;
#68071=CARTESIAN_POINT ( 'NONE',  ( 9.195468108405998819, -2.901397043998999781, 7.188863445572599709 ) ) ;
#68074=CARTESIAN_POINT ( 'NONE',  ( 10.69810941423799910, -3.053977294209000437, 8.359277272599898723 ) ) ;
#68083=CARTESIAN_POINT ( 'NONE',  ( 11.80878751119029957, -5.041025164610000608, 6.955365841266999638 ) ) ;
#68085=CARTESIAN_POINT ( 'NONE',  ( 10.80072469555900128, -3.429147315060100176, 8.487632181750699445 ) ) ;
#68123=CARTESIAN_POINT ( 'NONE',  ( 11.06080513895999928, -2.973119161490000106, 8.070849345005600028 ) ) ;
#68138=CARTESIAN_POINT ( 'NONE',  ( 12.09999999999999964, -3.011522968892934138, 8.147838400233645473 ) ) ;
#68144=PRODUCT_DEFINITION_CONTEXT ( 'detailed design', #28926, 'design' ) ;
#68162=CARTESIAN_POINT ( 'NONE',  ( 10.90749413291699987, -3.211956830789300277, 7.859564368461399830 ) ) ;
#68205=CARTESIAN_POINT ( 'NONE',  ( 11.12903166480609940, -4.864052766304100217, 7.439078678739090122 ) ) ;
#68237=CARTESIAN_POINT ( 'NONE',  ( 11.89700581613019992, -3.130347327833300053, 6.941573685175900010 ) ) ;
#68254=CARTESIAN_POINT ( 'NONE',  ( 12.28179573085659904, -3.026866171144600326, 7.331616337578100051 ) ) ;
#68264=DIRECTION ( 'NONE',  ( 0.000000000000000000, 1.000000000000000000, 0.000000000000000000 ) ) ;
#68280=CARTESIAN_POINT ( 'NONE',  ( 11.71253483539785734, -4.338990010211682069, 6.691360637068767936 ) ) ;
#68299=CARTESIAN_POINT ( 'NONE',  ( 9.473138961223998677, -3.053949131563199693, 6.860686042446299204 ) ) ;
#68315=CARTESIAN_POINT ( 'NONE',  ( 11.58126742035590695, -4.768619073576777723, 7.893373809886144343 ) ) ;
#68324=VERTEX_POINT ( 'NONE', #48755 ) ;
#68361=DIRECTION ( 'NONE',  ( 0.7071067617951957152, 0.000000000000000000, -0.7071068005778986532 ) ) ;
#68377=CARTESIAN_POINT ( 'NONE',  ( 11.16579975933730040, -2.791514215189000225, 7.915786590091300035 ) ) ;
#68390=CARTESIAN_POINT ( 'NONE',  ( 9.298455008774132224, -3.051544939223430397, 7.263673592043552674 ) ) ;
#68411=CARTESIAN_POINT ( 'NONE',  ( 9.877342523874999003, -5.264483068122999931, 7.693563834190999984 ) ) ;
#68425=CARTESIAN_POINT ( 'NONE',  ( 11.09725056272499977, -2.683866746800999792, 7.480494252843770120 ) ) ;
#68427=CARTESIAN_POINT ( 'NONE',  ( 10.82533997688000049, -3.756890902898200046, 8.614534918052999757 ) ) ;
#68461=CARTESIAN_POINT ( 'NONE',  ( 12.18277869730536977, -4.531392946702499813, 8.547856079839998955 ) ) ;
#68477=CARTESIAN_POINT ( 'NONE',  ( 12.10000000000000497, -4.447112190091931261, 8.372281669763946610 ) ) ;
#68496=EDGE_CURVE ( 'NONE', #16603, #24287, #30325, .T. ) ;
#68505=CARTESIAN_POINT ( 'NONE',  ( 11.17826222744820086, -4.668580868411999596, 6.949274830123499669 ) ) ;
#68536=CARTESIAN_POINT ( 'NONE',  ( 12.03192018828833731, -4.908970299435360118, 7.824998071251875409 ) ) ;
#68550=CARTESIAN_POINT ( 'NONE',  ( 11.84287482311539996, -3.196874704906699893, 7.175518335304800210 ) ) ;
#68581=CARTESIAN_POINT ( 'NONE',  ( 12.06833327354034857, -4.746587807672299597, 7.988332985010599963 ) ) ;
#68598=CARTESIAN_POINT ( 'NONE',  ( 12.10948876160955479, -4.695527826393099957, 6.776679950459500112 ) ) ;
#68624=B_SPLINE_CURVE_WITH_KNOTS ( 'NONE', 3,
 ( #54579, #64353, #37805, #54222, #38141, #60512, #23101, #43750, #22753, #1096 ),
 .UNSPECIFIED., .F., .F.,
 ( 4, 2, 2, 2, 4 ),
 ( 0.000000000000000000, 0.2500000000000000000, 0.5000000000000000000, 0.7500000000000000000, 1.000000000000000000 ),
 .UNSPECIFIED. ) ;
#68646=CARTESIAN_POINT ( 'NONE',  ( 10.50962143724499853, -3.332852462363599777, 8.250837174995698575 ) ) ;
#68660=CARTESIAN_POINT ( 'NONE',  ( 11.91486084871699802, -5.207010770456999893, 7.174999999999999822 ) ) ;
#68663=CARTESIAN_POINT ( 'NONE',  ( 10.87837607040048127, -3.132032243413395367, 7.603545367532808186 ) ) ;
#68673=ORIENTED_EDGE ( 'NONE', *, *, #48403, .T. ) ;
#68699=CARTESIAN_POINT ( 'NONE',  ( 9.478248830702476369, -3.044910121894152333, 6.882626671536596241 ) ) ;
#68708=CARTESIAN_POINT ( 'NONE',  ( 9.224024145839393896, -4.217522721361648408, 6.654559194835224289 ) ) ;
#68725=CARTESIAN_POINT ( 'NONE',  ( 11.51041369783139956, -4.064477673403060543, 6.223614866029000048 ) ) ;
#68746=ORIENTED_EDGE ( 'NONE', *, *, #7760, .F. ) ;
#68774=CARTESIAN_POINT ( 'NONE',  ( 12.09966954483535773, -3.361010663344000005, 8.485927942460499196 ) ) ;
#68776=CARTESIAN_POINT ( 'NONE',  ( 11.87964291764649971, -5.268358781405000357, 7.656787697937099679 ) ) ;
#68777=EDGE_LOOP ( 'NONE', ( #36192, #64884, #1630 ) ) ;
#68794=ORIENTED_EDGE ( 'NONE', *, *, #48870, .F. ) ;
#68812=CARTESIAN_POINT ( 'NONE',  ( 11.31524174883999834, -4.028418853626810403, 6.466884287543999577 ) ) ;
#68854=CARTESIAN_POINT ( 'NONE',  ( 10.92795525820100089, -4.094749303624469761, 8.498986197235801399 ) ) ;
#68860=CARTESIAN_POINT ( 'NONE',  ( 11.96989666366029859, -4.058428102321880004, 6.185029684353999357 ) ) ;
#68902=CARTESIAN_POINT ( 'NONE',  ( 11.76902897915239876, -3.778278678798900447, 6.662660017635100296 ) ) ;
#68935=CARTESIAN_POINT ( 'NONE',  ( 10.86325056272499978, -3.107965259299500183, 7.486779603004729111 ) ) ;
#68941=CARTESIAN_POINT ( 'NONE',  ( 11.63459739833729856, -4.823158118387800286, 7.174999999999999822 ) ) ;
#68951=CARTESIAN_POINT ( 'NONE',  ( 10.93210941423800087, -3.358814833524500276, 8.082391773166900606 ) ) ;
#68963=CARTESIAN_POINT ( 'NONE',  ( 9.557169810767971896, -3.796486612318636933, 6.292830123317686208 ) ) ;
#68998=CARTESIAN_POINT ( 'NONE',  ( 9.623101285863999266, -4.646739515667500875, 8.268485718282699182 ) ) ;
#69030=CARTESIAN_POINT ( 'NONE',  ( 10.51059687351600225, -3.370476274536376771, 6.407767014557176566 ) ) ;
#69079=CARTESIAN_POINT ( 'NONE',  ( 10.94426222744800015, -4.986443098259000450, 6.687444528363699625 ) ) ;
#69092=ADVANCED_FACE ( 'NONE', ( #49450 ), #47675, .T. ) ;
#69110=EDGE_LOOP ( 'NONE', ( #5582, #53234, #28286, #3360, #62733, #43925, #8633, #5677, #30531, #8414 ) ) ;
#69129=CARTESIAN_POINT ( 'NONE',  ( 11.58425954179440076, -3.017023678917100327, 6.683254058608399717 ) ) ;
#69156=CARTESIAN_POINT ( 'NONE',  ( 9.099999952505998024, -3.250000006358199744, 7.500000000000000000 ) ) ;
#69162=CARTESIAN_POINT ( 'NONE',  ( 12.02166954483529970, -3.437903757373499847, 8.367285821793199574 ) ) ;
ENDSEC;
END-ISO-10303-21;
